ISO-10303-21;
HEADER;
FILE_DESCRIPTION (('STEP AP214'),
    '1' );
FILE_NAME ('Foot Base.step',
    '2026-10-09T12:05:53',
    ( '' ),
    ( '' ),
    'SwSTEP 2.0',
    'SolidWorks 2026',
    '' );
FILE_SCHEMA (( 'AUTOMOTIVE_DESIGN' ));
ENDSEC;

DATA;
#4=ORIENTED_EDGE ( 'NONE', *, *, #7554, .T. ) ;
#5=CARTESIAN_POINT ( 'NONE',  ( 23.57448381426064188, -48.85252042381474524, -34.86893418027932512 ) ) ;
#7=DIRECTION ( 'NONE',  ( 0.6933752452815363787, 0.7071067811865472397, -0.1386750490563077587 ) ) ;
#8=CYLINDRICAL_SURFACE ( 'NONE', #48063, 2.000000000000000000 ) ;
#9=ORIENTED_EDGE ( 'NONE', *, *, #6010, .T. ) ;
#10=DIRECTION ( 'NONE',  ( 0.5516667872527539762, 0.8340645993220338061, 0.000000000000000000 ) ) ;
#13=CARTESIAN_POINT ( 'NONE',  ( 2.422196078461449797, -25.82482932757800143, -35.02873218748179340 ) ) ;
#14=EDGE_CURVE ( 'NONE', #41828, #44695, #32317, .T. ) ;
#17=CARTESIAN_POINT ( 'NONE',  ( 46.35510799002431526, -38.18910727465775068, -58.54413787839046535 ) ) ;
#24=CARTESIAN_POINT ( 'NONE',  ( 0.03808610503982521461, -8.381889819517736484, -34.73334895013598356 ) ) ;
#28=DIRECTION ( 'NONE',  ( 0.000000000000000000, 0.000000000000000000, 1.000000000000000000 ) ) ;
#48=CARTESIAN_POINT ( 'NONE',  ( -0.2431464996536397138, -45.41879842705380810, -34.97812159119441588 ) ) ;
#59=CARTESIAN_POINT ( 'NONE',  ( 14.28038030992539476, 1.245406012443915467, -34.79644291222909658 ) ) ;
#72=ORIENTED_EDGE ( 'NONE', *, *, #36227, .F. ) ;
#74=CARTESIAN_POINT ( 'NONE',  ( 42.22422596689015251, 6.426959746402536311, -79.19854329468917342 ) ) ;
#78=CARTESIAN_POINT ( 'NONE',  ( 45.17641135619509640, 2.139553668185640412, -34.89907071124209637 ) ) ;
#90=AXIS2_PLACEMENT_3D ( 'NONE', #30342, #50541, #46365 ) ;
#113=LINE ( 'NONE', #8225, #22864 ) ;
#115=ORIENTED_EDGE ( 'NONE', *, *, #5512, .F. ) ;
#116=DIRECTION ( 'NONE',  ( -0.2846079131720438693, 0.9586440088791325920, 0.000000000000000000 ) ) ;
#117=DIRECTION ( 'NONE',  ( 0.000000000000000000, 0.000000000000000000, 1.000000000000000000 ) ) ;
#125=AXIS2_PLACEMENT_3D ( 'NONE', #16725, #32947, #12811 ) ;
#127=ORIENTED_EDGE ( 'NONE', *, *, #25238, .T. ) ;
#129=ORIENTED_EDGE ( 'NONE', *, *, #8832, .T. ) ;
#140=DIRECTION ( 'NONE',  ( 0.000000000000000000, -1.000000000000000000, 0.000000000000000000 ) ) ;
#143=EDGE_LOOP ( 'NONE', ( #42632, #34972, #31733, #32112, #15786, #3340, #43438, #7469 ) ) ;
#148=CARTESIAN_POINT ( 'NONE',  ( 42.65284985753929448, -39.83221199758776976, -73.17816600590020926 ) ) ;
#161=ORIENTED_EDGE ( 'NONE', *, *, #48216, .F. ) ;
#165=ORIENTED_EDGE ( 'NONE', *, *, #23269, .F. ) ;
#168=CARTESIAN_POINT ( 'NONE',  ( 42.18478254462388577, 8.551920610105096188, -75.43933843070429646 ) ) ;
#170=CARTESIAN_POINT ( 'NONE',  ( 29.13393739769619728, 4.555383930574479656, -84.63196841427449613 ) ) ;
#175=ORIENTED_EDGE ( 'NONE', *, *, #21315, .T. ) ;
#182=ORIENTED_EDGE ( 'NONE', *, *, #38895, .T. ) ;
#193=AXIS2_PLACEMENT_3D ( 'NONE', #44707, #32884, #28448 ) ;
#203=EDGE_CURVE ( 'NONE', #41459, #2348, #29936, .T. ) ;
#213=CARTESIAN_POINT ( 'NONE',  ( 14.63393739769620083, -23.61618894467940066, -35.14999999999999858 ) ) ;
#214=CARTESIAN_POINT ( 'NONE',  ( 0.5774960717374295616, -8.799493537124943643, -34.81767276520690757 ) ) ;
#218=VERTEX_POINT ( 'NONE', #20999 ) ;
#222=ORIENTED_EDGE ( 'NONE', *, *, #47182, .T. ) ;
#223=CARTESIAN_POINT ( 'NONE',  ( 45.74232523797041239, 6.648894618224240105, -61.55666661952047036 ) ) ;
#241=CARTESIAN_POINT ( 'NONE',  ( -0.007164427059776000244, -10.48291004383190028, -34.77269723891829756 ) ) ;
#242=EDGE_LOOP ( 'NONE', ( #21413, #44958, #1944, #11021, #47868 ) ) ;
#251=( BOUNDED_CURVE ( )  B_SPLINE_CURVE ( 3, ( #35430, #43565, #7666, #27816 ),
 .UNSPECIFIED., .F., .T. ) 
 B_SPLINE_CURVE_WITH_KNOTS ( ( 4, 4 ),
 ( 2.356194490192377700, 3.141592653589793116 ),
 .UNSPECIFIED. ) 
 CURVE ( )  GEOMETRIC_REPRESENTATION_ITEM ( )  RATIONAL_B_SPLINE_CURVE ( ( 1.000000000000000000, 0.9492530216741954519, 0.9492530216741954519, 1.000000000000000000 ) ) 
 REPRESENTATION_ITEM ( '' )  );
#252=ORIENTED_EDGE ( 'NONE', *, *, #43387, .T. ) ;
#258=DIRECTION ( 'NONE',  ( 0.000000000000000000, 0.000000000000000000, -1.000000000000000000 ) ) ;
#261=VECTOR ( 'NONE', #32679, 1000.000000000000000 ) ;
#265=EDGE_CURVE ( 'NONE', #15142, #11807, #37468, .T. ) ;
#267=DIRECTION ( 'NONE',  ( -0.04332574401194498603, 0.02501412996813599451, 0.9987478026047158508 ) ) ;
#282=CARTESIAN_POINT ( 'NONE',  ( 2.558369240368460140, -6.046280207075140467, -34.64999999999999858 ) ) ;
#293=CARTESIAN_POINT ( 'NONE',  ( 16.13393739769620083, -15.61618894467929941, -34.64999999999999858 ) ) ;
#294=ORIENTED_EDGE ( 'NONE', *, *, #6376, .T. ) ;
#299=CARTESIAN_POINT ( 'NONE',  ( 0.4047412638265869833, -22.38804348994680282, -35.14999999999999858 ) ) ;
#304=AXIS2_PLACEMENT_3D ( 'NONE', #29304, #41620, #1792 ) ;
#306=LINE ( 'NONE', #33028, #47756 ) ;
#315=ORIENTED_EDGE ( 'NONE', *, *, #51572, .T. ) ;
#322=CARTESIAN_POINT ( 'NONE',  ( 42.10929425512229329, -37.64097509248548334, -79.77316519949246754 ) ) ;
#324=ORIENTED_EDGE ( 'NONE', *, *, #5080, .T. ) ;
#330=EDGE_CURVE ( 'NONE', #24503, #9584, #50468, .T. ) ;
#331=VECTOR ( 'NONE', #5456, 1000.000000000000227 ) ;
#336=VERTEX_POINT ( 'NONE', #49836 ) ;
#351=CARTESIAN_POINT ( 'NONE',  ( 18.13393739769620083, -41.61618894467930119, -54.64999999999999858 ) ) ;
#369=ORIENTED_EDGE ( 'NONE', *, *, #42644, .T. ) ;
#381=LINE ( 'NONE', #40735, #27640 ) ;
#382=ORIENTED_EDGE ( 'NONE', *, *, #47664, .T. ) ;
#385=CYLINDRICAL_SURFACE ( 'NONE', #20080, 0.4999999999999984457 ) ;
#388=AXIS2_PLACEMENT_3D ( 'NONE', #14443, #6852, #15224 ) ;
#392=CARTESIAN_POINT ( 'NONE',  ( 38.67452568954060155, -15.61618894467929941, -81.65000000000000568 ) ) ;
#396=DIRECTION ( 'NONE',  ( -0.8090169943749478954, -0.5877852522924724710, 0.000000000000000000 ) ) ;
#397=VECTOR ( 'NONE', #38374, 1000.000000000000000 ) ;
#401=CARTESIAN_POINT ( 'NONE',  ( 43.60315030137302728, -39.92105456565624877, -68.58134689406078621 ) ) ;
#408=EDGE_CURVE ( 'NONE', #24575, #50266, #21250, .T. ) ;
#414=CARTESIAN_POINT ( 'NONE',  ( 29.13393739769619728, -36.11618894467930119, -81.65000000000000568 ) ) ;
#416=LINE ( 'NONE', #12475, #13701 ) ;
#418=CARTESIAN_POINT ( 'NONE',  ( 42.16784573056604302, 8.550091971082537157, -75.52128294923836904 ) ) ;
#419=LINE ( 'NONE', #4352, #37390 ) ;
#425=VERTEX_POINT ( 'NONE', #29383 ) ;
#435=CARTESIAN_POINT ( 'NONE',  ( -0.09557254528323877452, 14.34657913917513383, -34.84921897185084561 ) ) ;
#440=ORIENTED_EDGE ( 'NONE', *, *, #16005, .F. ) ;
#441=DIRECTION ( 'NONE',  ( 0.5897727341282541502, 0.3900873262218164661, 0.7071067811865459074 ) ) ;
#447=EDGE_CURVE ( 'NONE', #13016, #4886, #50086, .T. ) ;
#448=CARTESIAN_POINT ( 'NONE',  ( -22.81805345843360655, -13.96957243270927762, -54.73201327936519789 ) ) ;
#454=DIRECTION ( 'NONE',  ( 0.000000000000000000, 0.000000000000000000, -1.000000000000000000 ) ) ;
#456=CARTESIAN_POINT ( 'NONE',  ( -11.39236625349560050, -33.81790884424879806, -54.64999999999999858 ) ) ;
#457=EDGE_CURVE ( 'NONE', #11026, #50723, #11770, .T. ) ;
#465=DIRECTION ( 'NONE',  ( -0.8660254037844380415, 0.5000000000000012212, -1.387778780781449373E-16 ) ) ;
#470=EDGE_CURVE ( 'NONE', #16490, #36140, #45386, .T. ) ;
#476=LINE ( 'NONE', #31653, #22692 ) ;
#490=CARTESIAN_POINT ( 'NONE',  ( 0.1294298976607914931, -10.50415099917325534, -34.68804011290710321 ) ) ;
#491=ADVANCED_FACE ( 'NONE', ( #29634 ), #45639, .T. ) ;
#493=ORIENTED_EDGE ( 'NONE', *, *, #30281, .F. ) ;
#498=CYLINDRICAL_SURFACE ( 'NONE', #18331, 0.4999999999999997224 ) ;
#501=ORIENTED_EDGE ( 'NONE', *, *, #33687, .T. ) ;
#502=CARTESIAN_POINT ( 'NONE',  ( 17.07096049057481935, -43.84596607001319768, -60.51477253168923909 ) ) ;
#504=CARTESIAN_POINT ( 'NONE',  ( 20.63393739769620083, -41.61618894467930119, -35.14999999999999858 ) ) ;
#517=DIRECTION ( 'NONE',  ( 0.000000000000000000, 0.000000000000000000, 1.000000000000000000 ) ) ;
#522=DIRECTION ( 'NONE',  ( 1.000000000000000000, 0.000000000000000000, 0.000000000000000000 ) ) ;
#528=CARTESIAN_POINT ( 'NONE',  ( 43.79854539025301818, -40.04024745141481390, -67.21557273064806282 ) ) ;
#536=CARTESIAN_POINT ( 'NONE',  ( 18.13393739769639978, 10.38381105532070059, -35.14999999999999858 ) ) ;
#548=( BOUNDED_CURVE ( )  B_SPLINE_CURVE ( 3, ( #24797, #5437, #12517, #44221 ),
 .UNSPECIFIED., .F., .T. ) 
 B_SPLINE_CURVE_WITH_KNOTS ( ( 4, 4 ),
 ( 8.754247816369622087E-15, 0.7853981633974498333 ),
 .UNSPECIFIED. ) 
 CURVE ( )  GEOMETRIC_REPRESENTATION_ITEM ( )  RATIONAL_B_SPLINE_CURVE ( ( 1.000000000000000000, 0.9492530216741921212, 0.9492530216741921212, 1.000000000000000000 ) ) 
 REPRESENTATION_ITEM ( '' )  );
#561=DIRECTION ( 'NONE',  ( -0.05643417272666772372, 0.04100182651872436718, -0.9975640502598241977 ) ) ;
#573=CARTESIAN_POINT ( 'NONE',  ( 41.62617804670394861, -37.56246594912547465, -82.18879675496150128 ) ) ;
#579=ADVANCED_FACE ( 'NONE', ( #43010 ), #7355, .T. ) ;
#580=AXIS2_PLACEMENT_3D ( 'NONE', #5691, #33953, #49719 ) ;
#583=CARTESIAN_POINT ( 'NONE',  ( 33.83216070239956252, -11.80875449455119686, -34.79644660940672907 ) ) ;
#596=CIRCLE ( 'NONE', #18187, 2.999999999999999112 ) ;
#597=LINE ( 'NONE', #27860, #18665 ) ;
#608=DIRECTION ( 'NONE',  ( -0.3863301728269261659, -0.9223605572461982538, 0.000000000000000000 ) ) ;
#611=VERTEX_POINT ( 'NONE', #35648 ) ;
#619=ORIENTED_EDGE ( 'NONE', *, *, #38375, .T. ) ;
#620=EDGE_CURVE ( 'NONE', #33379, #44397, #12840, .T. ) ;
#621=VERTEX_POINT ( 'NONE', #7872 ) ;
#623=ORIENTED_EDGE ( 'NONE', *, *, #20200, .F. ) ;
#627=EDGE_CURVE ( 'NONE', #14961, #24006, #37678, .T. ) ;
#638=ORIENTED_EDGE ( 'NONE', *, *, #46821, .F. ) ;
#653=FACE_OUTER_BOUND ( 'NONE', #143, .T. ) ;
#657=CARTESIAN_POINT ( 'NONE',  ( 43.14443873153287967, -39.87986852203775356, -70.80016690477312125 ) ) ;
#670=FACE_OUTER_BOUND ( 'NONE', #7098, .T. ) ;
#673=CARTESIAN_POINT ( 'NONE',  ( 41.86108004392503545, 8.517095955210312042, -77.00193962239630707 ) ) ;
#677=VERTEX_POINT ( 'NONE', #44536 ) ;
#690=CARTESIAN_POINT ( 'NONE',  ( -1.513652225697619480, 19.20845123580577862, -36.54854460006156103 ) ) ;
#712=VECTOR ( 'NONE', #37434, 1000.000000000000114 ) ;
#723=FACE_OUTER_BOUND ( 'NONE', #48146, .T. ) ;
#729=DIRECTION ( 'NONE',  ( -1.000000000000000000, 0.000000000000000000, 0.000000000000000000 ) ) ;
#737=ORIENTED_EDGE ( 'NONE', *, *, #29270, .F. ) ;
#738=ADVANCED_FACE ( 'NONE', ( #19903 ), #8902, .F. ) ;
#745=AXIS2_PLACEMENT_3D ( 'NONE', #37331, #17418, #21326 ) ;
#747=AXIS2_PLACEMENT_3D ( 'NONE', #6843, #22792, #38812 ) ;
#756=B_SPLINE_CURVE_WITH_KNOTS ( 'NONE', 3,
 ( #30827, #46855, #26908, #42915, #7013, #22962, #44705, #23982, #31855, #12478, #16146, #48648, #5148, #16938, #51795, #8554, #20320 ),
 .UNSPECIFIED., .F., .F.,
 ( 4, 2, 1, 1, 1, 1, 1, 1, 1, 2, 2, 4 ),
 ( 0.000000000000000000, 0.2499999999999850120, 0.3749999999999775180, 0.4374999999999742428, 0.4687499999999726330, 0.4843749999999718003, 0.4921874999999713562, 0.4960937499999711897, 0.4980468749999710787, 0.4990234374999710232, 0.4999999999999710232, 1.000000000000000000 ),
 .UNSPECIFIED. ) ;
#759=ORIENTED_EDGE ( 'NONE', *, *, #38571, .T. ) ;
#761=CARTESIAN_POINT ( 'NONE',  ( 44.13393739769620083, 1.883811055320659955, -54.35294145922169662 ) ) ;
#765=EDGE_CURVE ( 'NONE', #26981, #3226, #22665, .T. ) ;
#774=CARTESIAN_POINT ( 'NONE',  ( 0.08375394646315241498, 19.63944928676770019, -34.70982966457259522 ) ) ;
#782=CARTESIAN_POINT ( 'NONE',  ( 30.64062214880055635, -35.66006875884785643, -84.61512769226293074 ) ) ;
#783=AXIS2_PLACEMENT_3D ( 'NONE', #43677, #40000, #12218 ) ;
#787=ORIENTED_EDGE ( 'NONE', *, *, #16197, .F. ) ;
#806=CARTESIAN_POINT ( 'NONE',  ( 18.20779226974428511, -12.71339276770203419, -643.2998782751060389 ) ) ;
#822=TOROIDAL_SURFACE ( 'NONE', #30097, 34.47562460986249988, 0.5000000000000000000 ) ;
#825=EDGE_LOOP ( 'NONE', ( #43165, #3802, #896, #30458 ) ) ;
#827=CARTESIAN_POINT ( 'NONE',  ( 42.58169510332613328, 6.482798360464016696, -77.41114634390734750 ) ) ;
#835=CARTESIAN_POINT ( 'NONE',  ( 42.48963204042236441, -37.70124347511775653, -77.87149162280671533 ) ) ;
#845=EDGE_CURVE ( 'NONE', #16471, #16095, #2067, .T. ) ;
#861=DIRECTION ( 'NONE',  ( 0.000000000000000000, 0.000000000000000000, -1.000000000000000000 ) ) ;
#862=TOROIDAL_SURFACE ( 'NONE', #18448, 2.500000000000000000, 0.5000000000000000000 ) ;
#867=CARTESIAN_POINT ( 'NONE',  ( 45.14832757675640096, -33.29289077328009938, -35.14999999999999858 ) ) ;
#880=PLANE ( 'NONE',  #44373 ) ;
#885=VERTEX_POINT ( 'NONE', #37447 ) ;
#896=ORIENTED_EDGE ( 'NONE', *, *, #47691, .T. ) ;
#906=AXIS2_PLACEMENT_3D ( 'NONE', #10117, #42084, #27124 ) ;
#916=CARTESIAN_POINT ( 'NONE',  ( 18.11511214869369724, 1.359379830875159900, -35.01387690002259490 ) ) ;
#917=EDGE_CURVE ( 'NONE', #26382, #7979, #49518, .T. ) ;
#922=CARTESIAN_POINT ( 'NONE',  ( 41.72973598950768093, -39.73518457503501367, -77.63497562485849812 ) ) ;
#923=FACE_OUTER_BOUND ( 'NONE', #19528, .T. ) ;
#930=PLANE ( 'NONE',  #31441 ) ;
#932=VECTOR ( 'NONE', #14664, 1000.000000000000000 ) ;
#937=CONICAL_SURFACE ( 'NONE', #46980, 0.7350000000000003197, 0.06981317007977388966 ) ;
#941=CARTESIAN_POINT ( 'NONE',  ( 42.56606161249485609, 8.591259806789389941, -73.59713884681082163 ) ) ;
#950=ORIENTED_EDGE ( 'NONE', *, *, #33591, .F. ) ;
#954=CARTESIAN_POINT ( 'NONE',  ( 16.13393739769620083, -15.61618894467929941, -34.64999999999999858 ) ) ;
#955=ORIENTED_EDGE ( 'NONE', *, *, #18756, .T. ) ;
#957=CARTESIAN_POINT ( 'NONE',  ( -0.1541415209190244717, 14.27647038466169072, -34.90033495507538674 ) ) ;
#960=DIRECTION ( 'NONE',  ( 1.000000000000000000, 0.000000000000000000, 0.000000000000000000 ) ) ;
#966=CARTESIAN_POINT ( 'NONE',  ( 9.026390854479029002, -47.84168788784550230, -54.64999999999999858 ) ) ;
#972=CARTESIAN_POINT ( 'NONE',  ( 4.133937397696209715, -8.687985714403829718, -47.64999999999999858 ) ) ;
#975=VECTOR ( 'NONE', #21208, 1000.000000000000000 ) ;
#980=ORIENTED_EDGE ( 'NONE', *, *, #37134, .F. ) ;
#982=ADVANCED_FACE ( 'NONE', ( #7292 ), #46621, .T. ) ;
#989=FACE_OUTER_BOUND ( 'NONE', #29432, .T. ) ;
#991=LINE ( 'NONE', #25333, #29805 ) ;
#1000=CYLINDRICAL_SURFACE ( 'NONE', #37757, 0.4999999999999994449 ) ;
#1011=ORIENTED_EDGE ( 'NONE', *, *, #6265, .F. ) ;
#1016=( BOUNDED_CURVE ( )  B_SPLINE_CURVE ( 3, ( #5150, #1461, #12749, #13532 ),
 .UNSPECIFIED., .F., .T. ) 
 B_SPLINE_CURVE_WITH_KNOTS ( ( 4, 4 ),
 ( 1.570796326794890341, 2.356194490192361712 ),
 .UNSPECIFIED. ) 
 CURVE ( )  GEOMETRIC_REPRESENTATION_ITEM ( )  RATIONAL_B_SPLINE_CURVE ( ( 1.000000000000000000, 0.9492530216741881244, 0.9492530216741881244, 1.000000000000000000 ) ) 
 REPRESENTATION_ITEM ( '' )  );
#1018=B_SPLINE_CURVE_WITH_KNOTS ( 'NONE', 3,
 ( #28435, #44435, #8543, #24487 ),
 .UNSPECIFIED., .F., .F.,
 ( 4, 4 ),
 ( 0.000000000000000000, 1.000000000000000000 ),
 .UNSPECIFIED. ) ;
#1020=ORIENTED_EDGE ( 'NONE', *, *, #4336, .F. ) ;
#1039=EDGE_LOOP ( 'NONE', ( #45803, #13275, #26617, #7920 ) ) ;
#1045=EDGE_CURVE ( 'NONE', #40975, #16369, #33519, .T. ) ;
#1051=CARTESIAN_POINT ( 'NONE',  ( 15.88317419833548350, -49.61618860914077089, -83.24417156247753269 ) ) ;
#1054=CARTESIAN_POINT ( 'NONE',  ( 39.92856797414579262, -39.83700212839830357, -84.94016436021760796 ) ) ;
#1055=PLANE ( 'NONE',  #5926 ) ;
#1069=ORIENTED_EDGE ( 'NONE', *, *, #44169, .F. ) ;
#1070=EDGE_CURVE ( 'NONE', #22505, #43323, #43724, .T. ) ;
#1075=CARTESIAN_POINT ( 'NONE',  ( 4.133937397696209715, -8.687985714403829718, -47.64999999999999858 ) ) ;
#1079=CARTESIAN_POINT ( 'NONE',  ( -13.39236625349559873, -30.35380722911099838, -54.64999999999999858 ) ) ;
#1094=CARTESIAN_POINT ( 'NONE',  ( 17.98749448546718455, 1.245406012443906807, -34.79644291222912500 ) ) ;
#1095=DIRECTION ( 'NONE',  ( 1.000000000000000000, 0.000000000000000000, 0.000000000000000000 ) ) ;
#1098=CARTESIAN_POINT ( 'NONE',  ( 42.99289099728417085, -37.77664616342443082, -75.35523169207313288 ) ) ;
#1104=EDGE_CURVE ( 'NONE', #41238, #12186, #39011, .T. ) ;
#1125=DIRECTION ( 'NONE',  ( 0.000000000000000000, 0.000000000000000000, 1.000000000000000000 ) ) ;
#1127=DIRECTION ( 'NONE',  ( -0.3863301728269291635, 0.9223605572461970326, 0.000000000000000000 ) ) ;
#1137=CARTESIAN_POINT ( 'NONE',  ( -0.2550193211043536579, -10.79508889112895176, -34.98823006203678432 ) ) ;
#1139=DIRECTION ( 'NONE',  ( -1.000000000000000000, 0.000000000000000000, 0.000000000000000000 ) ) ;
#1141=ORIENTED_EDGE ( 'NONE', *, *, #24172, .F. ) ;
#1146=VERTEX_POINT ( 'NONE', #43704 ) ;
#1159=AXIS2_PLACEMENT_3D ( 'NONE', #40714, #49114, #17132 ) ;
#1168=B_SPLINE_CURVE_WITH_KNOTS ( 'NONE', 3,
 ( #28138, #20529, #8502, #4559 ),
 .UNSPECIFIED., .F., .F.,
 ( 4, 4 ),
 ( 0.000000000000000000, 1.000000000000000000 ),
 .UNSPECIFIED. ) ;
#1201=CARTESIAN_POINT ( 'NONE',  ( 44.85572791398350745, 8.787869211225075361, -62.51294508393674931 ) ) ;
#1220=CARTESIAN_POINT ( 'NONE',  ( 20.63393739769620083, -41.61618894467930119, -34.64999999999999858 ) ) ;
#1225=LINE ( 'NONE', #20861, #8389 ) ;
#1230=CARTESIAN_POINT ( 'NONE',  ( 14.19338055721680014, -32.55558437065590027, -34.90839531524139971 ) ) ;
#1239=ADVANCED_FACE ( 'NONE', ( #41062 ), #34410, .T. ) ;
#1244=ORIENTED_EDGE ( 'NONE', *, *, #6440, .F. ) ;
#1247=FACE_OUTER_BOUND ( 'NONE', #46803, .T. ) ;
#1260=ORIENTED_EDGE ( 'NONE', *, *, #31950, .T. ) ;
#1261=CARTESIAN_POINT ( 'NONE',  ( 2.528703657258680515, -5.910750250813970652, -34.65800258959620095 ) ) ;
#1263=FACE_OUTER_BOUND ( 'NONE', #41665, .T. ) ;
#1276=FACE_OUTER_BOUND ( 'NONE', #37122, .T. ) ;
#1279=CARTESIAN_POINT ( 'NONE',  ( -18.95254157709769771, -32.86309081617850580, -51.24642923610910117 ) ) ;
#1281=EDGE_CURVE ( 'NONE', #4886, #6632, #5540, .T. ) ;
#1283=CARTESIAN_POINT ( 'NONE',  ( 14.13393739769649571, 3.536827985081051562, -43.67210484879171872 ) ) ;
#1284=CYLINDRICAL_SURFACE ( 'NONE', #28414, 0.4999999999999983347 ) ;
#1285=EDGE_CURVE ( 'NONE', #4176, #35594, #17330, .T. ) ;
#1286=CARTESIAN_POINT ( 'NONE',  ( 22.37268434111649995, -53.60841447722789610, -34.64999999999999858 ) ) ;
#1289=CARTESIAN_POINT ( 'NONE',  ( 10.07017945894041944, 22.77497238916370748, -34.80997524099235818 ) ) ;
#1290=VERTEX_POINT ( 'NONE', #1075 ) ;
#1296=AXIS2_PLACEMENT_3D ( 'NONE', #24869, #13128, #25137 ) ;
#1317=DIRECTION ( 'NONE',  ( 0.000000000000000000, 0.000000000000000000, -1.000000000000000000 ) ) ;
#1320=ORIENTED_EDGE ( 'NONE', *, *, #330, .T. ) ;
#1324=CIRCLE ( 'NONE', #34746, 2.000000000000000000 ) ;
#1331=CARTESIAN_POINT ( 'NONE',  ( -0.03447620312152044342, -8.421650097910747590, -34.79644660940672196 ) ) ;
#1344=CARTESIAN_POINT ( 'NONE',  ( 14.13393739769619906, -45.61618894467940066, -49.33749999999999858 ) ) ;
#1356=AXIS2_PLACEMENT_3D ( 'NONE', #51549, #3598, #31601 ) ;
#1357=CARTESIAN_POINT ( 'NONE',  ( 28.13393739769619728, -8.687985714403851034, -47.64999999999999858 ) ) ;
#1360=CARTESIAN_POINT ( 'NONE',  ( 0.07463975747371710823, -20.73676263863309899, -34.71188928912349780 ) ) ;
#1361=CARTESIAN_POINT ( 'NONE',  ( 42.35187137306987637, -37.67955064941986620, -78.56033206297207983 ) ) ;
#1368=EDGE_CURVE ( 'NONE', #36393, #16544, #23804, .T. ) ;
#1373=LINE ( 'NONE', #13441, #5556 ) ;
#1375=ORIENTED_EDGE ( 'NONE', *, *, #48401, .F. ) ;
#1381=EDGE_LOOP ( 'NONE', ( #21922, #21116, #28793, #39356 ) ) ;
#1398=FACE_OUTER_BOUND ( 'NONE', #43122, .T. ) ;
#1425=B_SPLINE_CURVE_WITH_KNOTS ( 'NONE', 3,
 ( #31340, #10683, #43425, #42654, #2821, #23216, #31596, #30572, #47366, #46594 ),
 .UNSPECIFIED., .F., .F.,
 ( 4, 2, 2, 2, 4 ),
 ( -0.1857717838168330138, -0.1853436703574470046, -0.1652145016249799980, -0.1459149143056970022, -0.1350635247393814631 ),
 .UNSPECIFIED. ) ;
#1429=ADVANCED_FACE ( 'NONE', ( #23547 ), #3670, .T. ) ;
#1432=CARTESIAN_POINT ( 'NONE',  ( 38.67452568954060155, -37.56081407618430035, -84.65000000000000568 ) ) ;
#1436=CIRCLE ( 'NONE', #12283, 2.000000000000000000 ) ;
#1446=DIRECTION ( 'NONE',  ( 1.000000000000000000, 0.000000000000000000, 0.000000000000000000 ) ) ;
#1450=DIRECTION ( 'NONE',  ( 0.000000000000000000, 0.000000000000000000, -1.000000000000000000 ) ) ;
#1459=CARTESIAN_POINT ( 'NONE',  ( 42.97465247888425210, 8.631328837227204787, -71.62199823571720003 ) ) ;
#1461=CARTESIAN_POINT ( 'NONE',  ( 11.87719327230665023, -41.98180839364705008, -34.64999999999999858 ) ) ;
#1466=ORIENTED_EDGE ( 'NONE', *, *, #48803, .T. ) ;
#1480=CARTESIAN_POINT ( 'NONE',  ( -8.439161468533404431, 14.66851012883797267, -42.49231428658828236 ) ) ;
#1481=DIRECTION ( 'NONE',  ( 0.000000000000000000, 0.000000000000000000, 1.000000000000000000 ) ) ;
#1484=CARTESIAN_POINT ( 'NONE',  ( 29.13393739769619728, 2.762490711761015572, -83.77132034355965118 ) ) ;
#1486=DIRECTION ( 'NONE',  ( 0.9222478369447116853, 7.578800512648213833E-13, 0.3865991816478668297 ) ) ;
#1494=ADVANCED_FACE ( 'NONE', ( #1276 ), #17267, .F. ) ;
#1504=DIRECTION ( 'NONE',  ( -0.9752630547974272535, -0.2208726750153868490, 0.008788366101716807433 ) ) ;
#1508=ADVANCED_FACE ( 'NONE', ( #18029 ), #5983, .T. ) ;
#1512=CARTESIAN_POINT ( 'NONE',  ( 23.24148394091340109, -47.84168788784550230, -54.64999999999999858 ) ) ;
#1523=CARTESIAN_POINT ( 'NONE',  ( 2.458146360389407370, -5.580163940743402051, -34.79644291222906105 ) ) ;
#1530=PLANE ( 'NONE',  #33213 ) ;
#1536=CARTESIAN_POINT ( 'NONE',  ( -22.52006847887419738, -21.48129748781419934, -54.44818321674360106 ) ) ;
#1538=CYLINDRICAL_SURFACE ( 'NONE', #19772, 0.4999999999999985012 ) ;
#1564=LINE ( 'NONE', #6280, #30665 ) ;
#1570=CARTESIAN_POINT ( 'NONE',  ( 41.04642893364459866, -37.84180074923700232, -85.09326562515050796 ) ) ;
#1574=ADVANCED_FACE ( 'NONE', ( #45821 ), #21805, .T. ) ;
#1616=CARTESIAN_POINT ( 'NONE',  ( 43.33544367895569849, -37.82612097586055455, -73.64240385444296066 ) ) ;
#1621=VECTOR ( 'NONE', #13500, 1000.000000000000000 ) ;
#1627=( BOUNDED_CURVE ( )  B_SPLINE_CURVE ( 3, ( #43430, #27168, #23222, #43177 ),
 .UNSPECIFIED., .F., .T. ) 
 B_SPLINE_CURVE_WITH_KNOTS ( ( 4, 4 ),
 ( 5.122516320926171041, 5.907914484323606885 ),
 .UNSPECIFIED. ) 
 CURVE ( )  GEOMETRIC_REPRESENTATION_ITEM ( )  RATIONAL_B_SPLINE_CURVE ( ( 1.000000000000000000, 0.9492530216741927873, 0.9492530216741927873, 1.000000000000000000 ) ) 
 REPRESENTATION_ITEM ( '' )  );
#1631=ORIENTED_EDGE ( 'NONE', *, *, #47061, .F. ) ;
#1640=ORIENTED_EDGE ( 'NONE', *, *, #24705, .T. ) ;
#1657=DIRECTION ( 'NONE',  ( -0.5516667872527389882, -0.8340645993220435761, 8.326672684688666658E-17 ) ) ;
#1660=AXIS2_PLACEMENT_3D ( 'NONE', #44288, #32994, #47977 ) ;
#1668=EDGE_CURVE ( 'NONE', #28134, #25290, #15167, .T. ) ;
#1673=CARTESIAN_POINT ( 'NONE',  ( 0.1457841021255935343, -4.451138319363987073, -34.68167779225149161 ) ) ;
#1677=CARTESIAN_POINT ( 'NONE',  ( 46.92881658497164210, 7.010978364822217479, -55.67557228759626042 ) ) ;
#1683=DIRECTION ( 'NONE',  ( 0.3863301728269245006, -0.9223605572461989199, -3.608224830031755305E-16 ) ) ;
#1690=AXIS2_PLACEMENT_3D ( 'NONE', #39632, #7917, #51683 ) ;
#1703=DIRECTION ( 'NONE',  ( -0.9223605572461961444, -0.3863301728269312174, 0.000000000000000000 ) ) ;
#1709=FACE_OUTER_BOUND ( 'NONE', #41195, .T. ) ;
#1715=ORIENTED_EDGE ( 'NONE', *, *, #43152, .T. ) ;
#1720=CARTESIAN_POINT ( 'NONE',  ( 44.14631460519247952, 8.734076427534667175, -65.95149200678194745 ) ) ;
#1723=CARTESIAN_POINT ( 'NONE',  ( 10.12953414448040057, -54.14192202099170004, -35.04035092416999220 ) ) ;
#1724=EDGE_LOOP ( 'NONE', ( #5035, #39103, #10123, #27654 ) ) ;
#1732=FACE_OUTER_BOUND ( 'NONE', #40043, .T. ) ;
#1733=CONICAL_SURFACE ( 'NONE', #5065, 1.154999999999999361, 0.08090409915523018303 ) ;
#1735=VECTOR ( 'NONE', #35100, 1000.000000000000000 ) ;
#1739=CARTESIAN_POINT ( 'NONE',  ( 45.34397758664299971, -33.92854118026809829, -34.64999999999999858 ) ) ;
#1741=CARTESIAN_POINT ( 'NONE',  ( 44.12711257345860361, 1.883811055320659955, -54.38706558040959749 ) ) ;
#1744=CARTESIAN_POINT ( 'NONE',  ( 2.446837772604975925, -5.526216967578156947, -34.84133294386909085 ) ) ;
#1754=ADVANCED_FACE ( 'NONE', ( #18798 ), #34777, .T. ) ;
#1767=CARTESIAN_POINT ( 'NONE',  ( 23.62413055734869971, -48.75525398023999912, -35.14999999999999858 ) ) ;
#1770=ORIENTED_EDGE ( 'NONE', *, *, #27594, .T. ) ;
#1772=ORIENTED_EDGE ( 'NONE', *, *, #29438, .T. ) ;
#1781=CARTESIAN_POINT ( 'NONE',  ( 8.693390981131763340, -48.85252042381475235, -34.86893418027933933 ) ) ;
#1784=ORIENTED_EDGE ( 'NONE', *, *, #12856, .F. ) ;
#1789=CARTESIAN_POINT ( 'NONE',  ( 17.06835202619926406, -16.29508091107710754, 36.77166666666649775 ) ) ;
#1790=ORIENTED_EDGE ( 'NONE', *, *, #1281, .T. ) ;
#1791=CARTESIAN_POINT ( 'NONE',  ( -19.04335822585570170, -33.05973225684409300, -51.59769406952909776 ) ) ;
#1792=DIRECTION ( 'NONE',  ( -1.000000000000000000, 0.000000000000000000, 0.000000000000000000 ) ) ;
#1806=VECTOR ( 'NONE', #48834, 1000.000000000000000 ) ;
#1811=VERTEX_POINT ( 'NONE', #23357 ) ;
#1816=CARTESIAN_POINT ( 'NONE',  ( 13.13393739769619906, -49.61618894467939356, -35.14999999999999858 ) ) ;
#1829=CARTESIAN_POINT ( 'NONE',  ( -5.143445851551899928, 17.08457437255530209, -39.23905930810909126 ) ) ;
#1831=CARTESIAN_POINT ( 'NONE',  ( 41.86067813338569721, -38.82080758994548830, -81.03536039894463272 ) ) ;
#1839=CARTESIAN_POINT ( 'NONE',  ( 41.49481243519896623, 8.512502644196153767, -78.61658674046471162 ) ) ;
#1843=CARTESIAN_POINT ( 'NONE',  ( 29.10094820555050177, -26.72778965252999939, -34.97139175453740023 ) ) ;
#1850=ADVANCED_FACE ( 'NONE', ( #16293, #39130, #3994 ), #48017, .T. ) ;
#1861=ORIENTED_EDGE ( 'NONE', *, *, #23152, .F. ) ;
#1870=LINE ( 'NONE', #21514, #15867 ) ;
#1872=DIRECTION ( 'NONE',  ( 0.000000000000000000, 0.000000000000000000, -1.000000000000000000 ) ) ;
#1873=EDGE_CURVE ( 'NONE', #49018, #13116, #51763, .T. ) ;
#1877=CARTESIAN_POINT ( 'NONE',  ( 43.77103348427062457, -37.88684466609633006, -71.46451074123150704 ) ) ;
#1897=CARTESIAN_POINT ( 'NONE',  ( 41.51381057164023503, -39.71056979448638202, -78.67767418718656813 ) ) ;
#1916=ORIENTED_EDGE ( 'NONE', *, *, #17794, .T. ) ;
#1917=DIRECTION ( 'NONE',  ( 0.000000000000000000, 0.000000000000000000, 1.000000000000000000 ) ) ;
#1919=AXIS2_PLACEMENT_3D ( 'NONE', #24596, #39654, #51201 ) ;
#1923=LINE ( 'NONE', #49635, #18443 ) ;
#1925=ORIENTED_EDGE ( 'NONE', *, *, #42229, .F. ) ;
#1932=DIRECTION ( 'NONE',  ( 0.9750030843324432039, -0.2182216942497586243, -0.04181241084878352388 ) ) ;
#1933=ORIENTED_EDGE ( 'NONE', *, *, #37546, .T. ) ;
#1934=CARTESIAN_POINT ( 'NONE',  ( 45.71458171117632219, 6.890963836120773678, -61.74677868268134517 ) ) ;
#1944=ORIENTED_EDGE ( 'NONE', *, *, #30435, .F. ) ;
#1951=CIRCLE ( 'NONE', #27081, 16.60961179679778610 ) ;
#1956=VERTEX_POINT ( 'NONE', #37504 ) ;
#1966=CARTESIAN_POINT ( 'NONE',  ( 9.976573729570910487, -53.79438198982419550, -34.67842804303189297 ) ) ;
#1968=AXIS2_PLACEMENT_3D ( 'NONE', #43740, #16464, #32166 ) ;
#1969=PLANE ( 'NONE',  #11684 ) ;
#1976=CARTESIAN_POINT ( 'NONE',  ( 38.67452568954050207, -36.11618894467930119, -81.65000000000000568 ) ) ;
#1977=DIRECTION ( 'NONE',  ( 0.000000000000000000, 0.000000000000000000, 1.000000000000000000 ) ) ;
#1979=CARTESIAN_POINT ( 'NONE',  ( 45.05458756453126767, 8.801970288391714803, -61.54777943354527281 ) ) ;
#1981=CARTESIAN_POINT ( 'NONE',  ( 19.21265657477716005, 18.23736444591407135, -34.79644660940672907 ) ) ;
#1982=CARTESIAN_POINT ( 'NONE',  ( 20.13393739769620083, -2.337132753317949785, -62.14999999999999858 ) ) ;
#1984=EDGE_LOOP ( 'NONE', ( #32187, #27398, #36832, #18906 ) ) ;
#1986=VERTEX_POINT ( 'NONE', #33563 ) ;
#1990=CYLINDRICAL_SURFACE ( 'NONE', #16811, 0.4999999999999980571 ) ;
#1992=ORIENTED_EDGE ( 'NONE', *, *, #50752, .F. ) ;
#2003=CONICAL_SURFACE ( 'NONE', #23749, 3.567506086244481622, 0.04995839572194331335 ) ;
#2016=EDGE_CURVE ( 'NONE', #11224, #26299, #45114, .T. ) ;
#2019=AXIS2_PLACEMENT_3D ( 'NONE', #13002, #23970, #47863 ) ;
#2028=ORIENTED_EDGE ( 'NONE', *, *, #12361, .F. ) ;
#2031=DIRECTION ( 'NONE',  ( 1.000000000000000000, 0.000000000000000000, 0.000000000000000000 ) ) ;
#2032=DIRECTION ( 'NONE',  ( 0.8090169943749472292, -0.5877852522924734702, 0.000000000000000000 ) ) ;
#2037=CARTESIAN_POINT ( 'NONE',  ( 19.40270147970599979, -49.11618894467930829, -34.64999999999999858 ) ) ;
#2041=CARTESIAN_POINT ( 'NONE',  ( 8.664097273252890474, -48.79579064807929711, -34.96018206680729890 ) ) ;
#2046=DIRECTION ( 'NONE',  ( 0.8660254037844351549, -0.5000000000000061062, 0.000000000000000000 ) ) ;
#2051=ORIENTED_EDGE ( 'NONE', *, *, #31232, .F. ) ;
#2052=CARTESIAN_POINT ( 'NONE',  ( -20.73632584900919795, -28.65688283608509934, -52.79758657238259900 ) ) ;
#2062=EDGE_LOOP ( 'NONE', ( #45987, #51744 ) ) ;
#2066=ORIENTED_EDGE ( 'NONE', *, *, #44781, .T. ) ;
#2067=LINE ( 'NONE', #9425, #28497 ) ;
#2074=ORIENTED_EDGE ( 'NONE', *, *, #40283, .T. ) ;
#2079=PLANE ( 'NONE',  #31097 ) ;
#2090=CARTESIAN_POINT ( 'NONE',  ( 42.09738834484929271, -37.61273901578999812, -79.83211318711599347 ) ) ;
#2103=CARTESIAN_POINT ( 'NONE',  ( 29.10811623682189975, -26.73044074004180004, -34.99013415954840411 ) ) ;
#2122=CARTESIAN_POINT ( 'NONE',  ( 23.13393739769620083, -2.337132753317950229, -84.65000000000000568 ) ) ;
#2137=CARTESIAN_POINT ( 'NONE',  ( 45.55117721137337128, -38.10517850036617205, -62.56376302709497139 ) ) ;
#2155=CARTESIAN_POINT ( 'NONE',  ( 41.51536462713278297, -39.71075051493620123, -78.67016534560366381 ) ) ;
#2161=ADVANCED_FACE ( 'NONE', ( #14430 ), #6573, .T. ) ;
#2186=ORIENTED_EDGE ( 'NONE', *, *, #29324, .F. ) ;
#2189=DIRECTION ( 'NONE',  ( 0.8660254037844387076, 0.4999999999999998890, 0.000000000000000000 ) ) ;
#2198=ORIENTED_EDGE ( 'NONE', *, *, #35446, .T. ) ;
#2208=DIRECTION ( 'NONE',  ( 1.000000000000000000, 0.000000000000000000, 0.000000000000000000 ) ) ;
#2210=AXIS2_PLACEMENT_3D ( 'NONE', #29549, #18022, #14093 ) ;
#2220=CARTESIAN_POINT ( 'NONE',  ( 3.633937397696210159, -22.83306730954970121, -34.64999999999999858 ) ) ;
#2241=CARTESIAN_POINT ( 'NONE',  ( 43.63810915241377586, 8.691766788974046420, -68.41189615741917862 ) ) ;
#2247=ORIENTED_EDGE ( 'NONE', *, *, #18614, .F. ) ;
#2249=( BOUNDED_CURVE ( )  B_SPLINE_CURVE ( 3, ( #25269, #28685, #37085, #12995 ),
 .UNSPECIFIED., .F., .T. ) 
 B_SPLINE_CURVE_WITH_KNOTS ( ( 4, 4 ),
 ( 1.570796326794895226, 2.356194490192482505 ),
 .UNSPECIFIED. ) 
 CURVE ( )  GEOMETRIC_REPRESENTATION_ITEM ( )  RATIONAL_B_SPLINE_CURVE ( ( 1.000000000000000000, 0.9492530216741734694, 0.9492530216741734694, 1.000000000000000000 ) ) 
 REPRESENTATION_ITEM ( '' )  );
#2254=ORIENTED_EDGE ( 'NONE', *, *, #29257, .T. ) ;
#2255=CARTESIAN_POINT ( 'NONE',  ( -0.4410626023037880206, -27.49517073325580085, -35.14999999999999858 ) ) ;
#2257=ORIENTED_EDGE ( 'NONE', *, *, #7986, .F. ) ;
#2261=AXIS2_PLACEMENT_3D ( 'NONE', #7012, #10682, #35290 ) ;
#2269=CARTESIAN_POINT ( 'NONE',  ( 47.10914403122639982, 8.080609220371670176, -53.83103343289329956 ) ) ;
#2275=CARTESIAN_POINT ( 'NONE',  ( 14.28038400710302724, 10.53025766472732450, -34.79644660940672907 ) ) ;
#2277=DIRECTION ( 'NONE',  ( 0.000000000000000000, -1.000000000000000000, 0.000000000000000000 ) ) ;
#2289=CARTESIAN_POINT ( 'NONE',  ( 0.3209249304026170480, -50.71887597443840434, -35.14999999999999858 ) ) ;
#2298=DIRECTION ( 'NONE',  ( 0.000000000000000000, 0.000000000000000000, -1.000000000000000000 ) ) ;
#2299=VERTEX_POINT ( 'NONE', #47448 ) ;
#2300=CARTESIAN_POINT ( 'NONE',  ( 8.644451877215889368, -48.75768716228870403, -35.10565360069929852 ) ) ;
#2306=FACE_OUTER_BOUND ( 'NONE', #27368, .T. ) ;
#2310=CARTESIAN_POINT ( 'NONE',  ( -13.76835980061299836, -41.17840569159340447, -47.00285061395300090 ) ) ;
#2332=PLANE ( 'NONE',  #17724 ) ;
#2342=CARTESIAN_POINT ( 'NONE',  ( -0.1635911377674279799, 19.81675348476660048, -35.29985221058469591 ) ) ;
#2344=CARTESIAN_POINT ( 'NONE',  ( 42.32416139106639008, -38.87540147440780913, -78.75518257947804557 ) ) ;
#2346=FACE_OUTER_BOUND ( 'NONE', #6063, .T. ) ;
#2348=VERTEX_POINT ( 'NONE', #48204 ) ;
#2359=DIRECTION ( 'NONE',  ( 0.000000000000000000, -1.000000000000000000, 0.000000000000000000 ) ) ;
#2372=ORIENTED_EDGE ( 'NONE', *, *, #12854, .F. ) ;
#2376=ADVANCED_FACE ( 'NONE', ( #40851 ), #12307, .T. ) ;
#2377=CARTESIAN_POINT ( 'NONE',  ( 22.60607335269574492, -20.31847096301905609, -47.64999999999999858 ) ) ;
#2387=CARTESIAN_POINT ( 'NONE',  ( 43.88839816904001623, -37.90263197162346387, -70.87765394619944459 ) ) ;
#2388=ORIENTED_EDGE ( 'NONE', *, *, #27241, .F. ) ;
#2402=CARTESIAN_POINT ( 'NONE',  ( 46.98749101202549383, -39.23094825485602399, -34.79644638567071269 ) ) ;
#2421=DIRECTION ( 'NONE',  ( 0.000000000000000000, 1.000000000000000000, 0.000000000000000000 ) ) ;
#2430=EDGE_LOOP ( 'NONE', ( #48923, #24938, #29146, #19387 ) ) ;
#2433=ORIENTED_EDGE ( 'NONE', *, *, #28309, .F. ) ;
#2445=CARTESIAN_POINT ( 'NONE',  ( 47.09446252081839646, 7.025840437962705742, -54.84737438438714463 ) ) ;
#2464=ORIENTED_EDGE ( 'NONE', *, *, #10308, .F. ) ;
#2465=DIRECTION ( 'NONE',  ( -0.5516667872527503125, 0.8340645993220362486, -1.942890293094025918E-16 ) ) ;
#2469=DIRECTION ( 'NONE',  ( 0.8529218806139627906, -0.5196445842661518988, -0.04993767728678798895 ) ) ;
#2470=AXIS2_PLACEMENT_3D ( 'NONE', #45539, #29780, #32673 ) ;
#2473=AXIS2_PLACEMENT_3D ( 'NONE', #9175, #28, #16252 ) ;
#2474=CARTESIAN_POINT ( 'NONE',  ( 8.633937397695980565, 17.54628985290149856, -34.64999999999999858 ) ) ;
#2475=AXIS2_PLACEMENT_3D ( 'NONE', #37544, #6618, #10030 ) ;
#2478=CONICAL_SURFACE ( 'NONE', #31749, 0.7350000000000010969, 0.06981317007977388966 ) ;
#2485=CIRCLE ( 'NONE', #25876, 3.000000000000003997 ) ;
#2495=DIRECTION ( 'NONE',  ( 0.000000000000000000, 0.000000000000000000, 1.000000000000000000 ) ) ;
#2496=CARTESIAN_POINT ( 'NONE',  ( 16.13393739769620083, -15.61618894467929941, -47.64999999999999858 ) ) ;
#2498=CARTESIAN_POINT ( 'NONE',  ( 46.06102096816690050, 8.864772444052823275, -56.66258995241773277 ) ) ;
#2502=ORIENTED_EDGE ( 'NONE', *, *, #43172, .T. ) ;
#2504=CARTESIAN_POINT ( 'NONE',  ( 26.13393739769619728, -28.89524513604070322, -39.64999999999999858 ) ) ;
#2520=VECTOR ( 'NONE', #19835, 1000.000000000000114 ) ;
#2531=CARTESIAN_POINT ( 'NONE',  ( 46.84271081672680026, 8.424848343090520331, -54.36135291155100191 ) ) ;
#2537=CARTESIAN_POINT ( 'NONE',  ( 44.36443571826935539, -39.98382968829412221, -64.89400308598267486 ) ) ;
#2561=CARTESIAN_POINT ( 'NONE',  ( 19.21265657477752598, -49.46974233527256359, -34.79644660940672907 ) ) ;
#2565=VERTEX_POINT ( 'NONE', #35828 ) ;
#2566=CARTESIAN_POINT ( 'NONE',  ( 18.44107633810049762, 5.527441888613518373, -34.79644660940672907 ) ) ;
#2588=EDGE_CURVE ( 'NONE', #12971, #36729, #32664, .T. ) ;
#2592=EDGE_CURVE ( 'NONE', #37038, #10379, #2670, .T. ) ;
#2595=CARTESIAN_POINT ( 'NONE',  ( 13.63393739769619906, -45.61618894467940066, -35.14999999999999858 ) ) ;
#2596=CIRCLE ( 'NONE', #45274, 2.999999999999999112 ) ;
#2600=ORIENTED_EDGE ( 'NONE', *, *, #46888, .F. ) ;
#2603=PLANE ( 'NONE',  #15551 ) ;
#2610=CARTESIAN_POINT ( 'NONE',  ( -0.2420090942845939952, 19.37547203512649929, -34.97694517729849650 ) ) ;
#2612=CARTESIAN_POINT ( 'NONE',  ( 45.89884848434977016, -40.22868796843931705, -56.88510789556015368 ) ) ;
#2620=CARTESIAN_POINT ( 'NONE',  ( 45.69008980065965631, 8.960831227535303256, -57.99265491320560528 ) ) ;
#2621=LINE ( 'NONE', #42719, #20185 ) ;
#2625=CARTESIAN_POINT ( 'NONE',  ( 28.63499203762230394, -26.55409882356909890, -34.64999999999999858 ) ) ;
#2647=VERTEX_POINT ( 'NONE', #48142 ) ;
#2648=CARTESIAN_POINT ( 'NONE',  ( 3.987490788289478783, -8.603434725040944642, -34.79644660940672907 ) ) ;
#2651=VERTEX_POINT ( 'NONE', #16166 ) ;
#2655=LINE ( 'NONE', #14440, #44553 ) ;
#2659=CARTESIAN_POINT ( 'NONE',  ( 45.04398199156845095, -38.04764848494028229, -65.09977662695574452 ) ) ;
#2670=CIRCLE ( 'NONE', #39480, 2.000000000000000000 ) ;
#2672=ORIENTED_EDGE ( 'NONE', *, *, #13327, .F. ) ;
#2676=CARTESIAN_POINT ( 'NONE',  ( 40.99639966443897521, -39.64985368671198529, -81.17215446963993486 ) ) ;
#2677=CARTESIAN_POINT ( 'NONE',  ( 20.39068152308554716, 10.74943050428834823, -34.64999999999999858 ) ) ;
#2684=DIRECTION ( 'NONE',  ( -0.8660254037844381525, 0.5000000000000007772, 0.000000000000000000 ) ) ;
#2714=CARTESIAN_POINT ( 'NONE',  ( 43.08803616482992993, 6.558594096496958237, -74.87949594534148900 ) ) ;
#2716=ORIENTED_EDGE ( 'NONE', *, *, #46821, .T. ) ;
#2723=DIRECTION ( 'NONE',  ( 0.000000000000000000, -1.000000000000000000, 0.000000000000000000 ) ) ;
#2729=DIRECTION ( 'NONE',  ( -0.6918010270571961495, 0.3994115091971370823, -0.6015661104845201335 ) ) ;
#2740=CARTESIAN_POINT ( 'NONE',  ( 14.17038268164670001, 1.343694785579800044, -34.95504743437649608 ) ) ;
#2759=CARTESIAN_POINT ( 'NONE',  ( 45.71596276813887272, 8.844597340974925004, -58.33858004979597922 ) ) ;
#2764=VERTEX_POINT ( 'NONE', #16958 ) ;
#2765=VECTOR ( 'NONE', #44428, 1000.000000000000000 ) ;
#2770=ORIENTED_EDGE ( 'NONE', *, *, #28864, .T. ) ;
#2775=CARTESIAN_POINT ( 'NONE',  ( 45.16555009513719199, -33.34057249083589625, -34.94897920698430482 ) ) ;
#2777=AXIS2_PLACEMENT_3D ( 'NONE', #23907, #15815, #31780 ) ;
#2780=CIRCLE ( 'NONE', #6974, 0.5000000000000004441 ) ;
#2789=CARTESIAN_POINT ( 'NONE',  ( 1.058369240368409958, -22.58802147093010149, -34.64999999999999858 ) ) ;
#2800=CARTESIAN_POINT ( 'NONE',  ( 45.34134074967911943, -40.05352858297872132, -60.15667676233234573 ) ) ;
#2814=TOROIDAL_SURFACE ( 'NONE', #6147, 16.60961179679779676, 0.5000000000000000000 ) ;
#2819=CARTESIAN_POINT ( 'NONE',  ( -0.007164427059776000244, -22.82436266295209748, -34.77269723891829756 ) ) ;
#2821=CARTESIAN_POINT ( 'NONE',  ( 14.53139780415610005, 1.019008445896690151, -34.65800258959599489 ) ) ;
#2830=ORIENTED_EDGE ( 'NONE', *, *, #29719, .F. ) ;
#2832=FACE_OUTER_BOUND ( 'NONE', #24242, .T. ) ;
#2833=DIRECTION ( 'NONE',  ( 0.000000000000000000, 0.000000000000000000, -1.000000000000000000 ) ) ;
#2835=ORIENTED_EDGE ( 'NONE', *, *, #25274, .F. ) ;
#2836=ORIENTED_EDGE ( 'NONE', *, *, #26536, .T. ) ;
#2851=EDGE_CURVE ( 'NONE', #46028, #38446, #39740, .T. ) ;
#2860=EDGE_LOOP ( 'NONE', ( #12695, #28886, #13030, #638 ) ) ;
#2869=CARTESIAN_POINT ( 'NONE',  ( -18.34876765167589951, 3.165124538224290074, -50.94389406753779781 ) ) ;
#2870=B_SPLINE_CURVE_WITH_KNOTS ( 'NONE', 3,
 ( #39553, #11003, #15187, #31148, #47173, #39295, #35618, #26699 ),
 .UNSPECIFIED., .F., .F.,
 ( 4, 2, 2, 4 ),
 ( 0.08070042245370699641, 0.09929974077558219314, 0.1184089355330240068, 0.1205773112035685712 ),
 .UNSPECIFIED. ) ;
#2904=ORIENTED_EDGE ( 'NONE', *, *, #44817, .T. ) ;
#2911=CARTESIAN_POINT ( 'NONE',  ( 23.13393739769620083, -28.89524513604070322, -84.65000000000000568 ) ) ;
#2918=ORIENTED_EDGE ( 'NONE', *, *, #47019, .F. ) ;
#2924=CARTESIAN_POINT ( 'NONE',  ( 0.1457839871805957643, 14.73018012514992137, -34.68167748489143776 ) ) ;
#2966=EDGE_CURVE ( 'NONE', #9803, #51621, #5334, .T. ) ;
#2970=CARTESIAN_POINT ( 'NONE',  ( 43.37366955983795691, 6.599305106106574392, -73.45127533249436169 ) ) ;
#2977=EDGE_CURVE ( 'NONE', #6854, #15707, #8480, .T. ) ;
#2983=VECTOR ( 'NONE', #44297, 1000.000000000000114 ) ;
#3003=CARTESIAN_POINT ( 'NONE',  ( -22.60072279458010058, -20.15755767129849829, -54.65015892017029842 ) ) ;
#3013=ORIENTED_EDGE ( 'NONE', *, *, #31196, .F. ) ;
#3019=CARTESIAN_POINT ( 'NONE',  ( 16.13393739769620083, -45.61618894467940066, -35.14999999999999858 ) ) ;
#3022=AXIS2_PLACEMENT_3D ( 'NONE', #41140, #50042, #10473 ) ;
#3024=ORIENTED_EDGE ( 'NONE', *, *, #16197, .T. ) ;
#3030=CARTESIAN_POINT ( 'NONE',  ( 22.13393739769619728, -54.15188668067469990, -54.64999999999999858 ) ) ;
#3033=ADVANCED_FACE ( 'NONE', ( #33075 ), #49103, .T. ) ;
#3040=CIRCLE ( 'NONE', #44899, 22.00000000000000000 ) ;
#3046=CARTESIAN_POINT ( 'NONE',  ( 1.057008924473209932, -22.58759019641090049, -34.64999999999999858 ) ) ;
#3049=DIRECTION ( 'NONE',  ( 0.000000000000000000, -1.000000000000000000, 0.000000000000000000 ) ) ;
#3052=AXIS2_PLACEMENT_3D ( 'NONE', #26799, #47261, #6385 ) ;
#3056=CARTESIAN_POINT ( 'NONE',  ( 44.80053834244425559, -40.01632457077029414, -62.78033700576844467 ) ) ;
#3064=ADVANCED_FACE ( 'NONE', ( #4800 ), #12937, .T. ) ;
#3078=CARTESIAN_POINT ( 'NONE',  ( 40.85150231246245056, 8.399356969744889767, -81.87147178968719174 ) ) ;
#3082=CARTESIAN_POINT ( 'NONE',  ( 0.1457839871805957643, 14.73018012514992137, -34.68167748489143776 ) ) ;
#3085=CARTESIAN_POINT ( 'NONE',  ( 28.63393739769619728, -22.83306730954970121, -34.64999999999999858 ) ) ;
#3086=ORIENTED_EDGE ( 'NONE', *, *, #7688, .F. ) ;
#3089=DIRECTION ( 'NONE',  ( 0.000000000000000000, 0.000000000000000000, 1.000000000000000000 ) ) ;
#3092=VECTOR ( 'NONE', #7022, 1000.000000000000000 ) ;
#3098=PLANE ( 'NONE',  #42125 ) ;
#3102=ADVANCED_FACE ( 'NONE', ( #8736 ), #32539, .T. ) ;
#3104=DIRECTION ( 'NONE',  ( 0.000000000000000000, 1.000000000000000000, 0.000000000000000000 ) ) ;
#3105=VERTEX_POINT ( 'NONE', #867 ) ;
#3107=CARTESIAN_POINT ( 'NONE',  ( 29.13393739769619728, -26.76363820448759867, -35.14999999999999858 ) ) ;
#3114=CARTESIAN_POINT ( 'NONE',  ( 8.919738259460300966, 18.05571844226340161, -34.65024031912469837 ) ) ;
#3122=CARTESIAN_POINT ( 'NONE',  ( 23.62400244246320113, 17.52418497763099836, -35.12503119152809461 ) ) ;
#3124=CARTESIAN_POINT ( 'NONE',  ( 8.830271178173081381, -49.11659379690700433, -34.68023162149790295 ) ) ;
#3137=ORIENTED_EDGE ( 'NONE', *, *, #30281, .T. ) ;
#3138=CARTESIAN_POINT ( 'NONE',  ( 46.99535652950729059, 8.020657431200683973, -55.88807232857796947 ) ) ;
#3144=EDGE_CURVE ( 'NONE', #14662, #21348, #29924, .T. ) ;
#3146=DIRECTION ( 'NONE',  ( 1.000000000000000000, 0.000000000000000000, 0.000000000000000000 ) ) ;
#3147=ORIENTED_EDGE ( 'NONE', *, *, #22468, .F. ) ;
#3155=CARTESIAN_POINT ( 'NONE',  ( 7.234750459571823278, -9.150551169462135093, -84.65000000000000568 ) ) ;
#3177=DIRECTION ( 'NONE',  ( 1.000000000000000000, 0.000000000000000000, 0.000000000000000000 ) ) ;
#3179=EDGE_CURVE ( 'NONE', #3226, #41446, #4843, .T. ) ;
#3181=DIRECTION ( 'NONE',  ( -0.05886216378138799110, 0.000000000000000000, -0.9982661196669817549 ) ) ;
#3193=CARTESIAN_POINT ( 'NONE',  ( 14.13393739769619906, -32.62399965035220362, -35.14999999999999858 ) ) ;
#3206=DIRECTION ( 'NONE',  ( 0.000000000000000000, 1.000000000000000000, 0.000000000000000000 ) ) ;
#3225=CARTESIAN_POINT ( 'NONE',  ( -0.007164427059776000244, -4.186223695871990280, -34.77269723891829756 ) ) ;
#3226=VERTEX_POINT ( 'NONE', #38326 ) ;
#3227=CARTESIAN_POINT ( 'NONE',  ( -11.80944000494479873, 2.826328597561450273, -45.03554556751399929 ) ) ;
#3228=CARTESIAN_POINT ( 'NONE',  ( 43.41473102517175420, 6.605039987487077546, -73.24597267587351723 ) ) ;
#3246=CARTESIAN_POINT ( 'NONE',  ( 38.67452568954060155, -36.11618894467930119, -81.65000000000000568 ) ) ;
#3260=EDGE_CURVE ( 'NONE', #50203, #24767, #5776, .T. ) ;
#3261=DIRECTION ( 'NONE',  ( 0.000000000000000000, -1.000000000000000000, 0.000000000000000000 ) ) ;
#3266=EDGE_CURVE ( 'NONE', #17159, #22505, #30542, .T. ) ;
#3279=ORIENTED_EDGE ( 'NONE', *, *, #2016, .T. ) ;
#3283=CARTESIAN_POINT ( 'NONE',  ( 16.13393739769620083, -15.61618894467929941, -44.64999999999999858 ) ) ;
#3285=DIRECTION ( 'NONE',  ( 0.000000000000000000, 0.000000000000000000, -1.000000000000000000 ) ) ;
#3290=LINE ( 'NONE', #6711, #35160 ) ;
#3291=ORIENTED_EDGE ( 'NONE', *, *, #44590, .T. ) ;
#3292=CARTESIAN_POINT ( 'NONE',  ( 44.13393739769620083, 1.883811055320659955, -54.27132075603810080 ) ) ;
#3301=CARTESIAN_POINT ( 'NONE',  ( 0.3209249304026170480, -15.61618894467929941, -35.14999999999999858 ) ) ;
#3307=DIRECTION ( 'NONE',  ( -0.1961161351381836004, -1.134894647394604573E-15, -0.9805806756909204447 ) ) ;
#3312=CARTESIAN_POINT ( 'NONE',  ( 45.06945685171515947, -40.03533966481339945, -61.47576887606990681 ) ) ;
#3314=( BOUNDED_CURVE ( )  B_SPLINE_CURVE ( 2, ( #6934, #22889, #6156 ),
 .UNSPECIFIED., .F., .F. ) 
 B_SPLINE_CURVE_WITH_KNOTS ( ( 3, 3 ),
 ( 0.09013418064815610642, 2.097305204714880134 ),
 .UNSPECIFIED. ) 
 CURVE ( )  GEOMETRIC_REPRESENTATION_ITEM ( )  RATIONAL_B_SPLINE_CURVE ( ( 1.000760730674140175, 1.008874108732590091, 1.001093714201509943 ) ) 
 REPRESENTATION_ITEM ( '' )  );
#3340=ORIENTED_EDGE ( 'NONE', *, *, #31431, .T. ) ;
#3341=DIRECTION ( 'NONE',  ( 0.000000000000000000, 0.000000000000000000, -1.000000000000000000 ) ) ;
#3342=CIRCLE ( 'NONE', #24244, 17.09468304687050022 ) ;
#3366=EDGE_CURVE ( 'NONE', #50035, #6096, #8024, .T. ) ;
#3370=EDGE_CURVE ( 'NONE', #24679, #4176, #35816, .T. ) ;
#3374=CARTESIAN_POINT ( 'NONE',  ( 16.13393739769620083, -15.61618894467929941, -34.64999999999999858 ) ) ;
#3386=AXIS2_PLACEMENT_3D ( 'NONE', #38353, #49190, #18172 ) ;
#3392=CARTESIAN_POINT ( 'NONE',  ( 44.37201056559310075, -37.88618800308559997, -68.45424654654109986 ) ) ;
#3399=CARTESIAN_POINT ( 'NONE',  ( 42.99808947197828957, 6.368226865670313153, -75.30230971069127577 ) ) ;
#3417=ORIENTED_EDGE ( 'NONE', *, *, #29651, .T. ) ;
#3424=CARTESIAN_POINT ( 'NONE',  ( 16.13393739769620083, -15.61618894467929941, -35.14999999999999858 ) ) ;
#3426=CARTESIAN_POINT ( 'NONE',  ( 44.94022070389027590, -33.11618894467929408, -54.43277924001892387 ) ) ;
#3452=CARTESIAN_POINT ( 'NONE',  ( 30.78462454764483169, -35.68771960809947785, -84.61927628510844102 ) ) ;
#3456=ORIENTED_EDGE ( 'NONE', *, *, #50652, .F. ) ;
#3468=CARTESIAN_POINT ( 'NONE',  ( -0.3684971866671489238, -45.31814476460159824, -35.08739145837887463 ) ) ;
#3479=DIRECTION ( 'NONE',  ( 0.000000000000000000, 0.000000000000000000, 1.000000000000000000 ) ) ;
#3483=DIRECTION ( 'NONE',  ( 0.000000000000000000, 1.000000000000000000, 0.000000000000000000 ) ) ;
#3489=DIRECTION ( 'NONE',  ( 0.000000000000000000, 0.000000000000000000, 1.000000000000000000 ) ) ;
#3490=ORIENTED_EDGE ( 'NONE', *, *, #21143, .T. ) ;
#3492=CARTESIAN_POINT ( 'NONE',  ( 43.38751250541962889, 6.601242059090285608, -73.38206190525755801 ) ) ;
#3496=CARTESIAN_POINT ( 'NONE',  ( 0.3209249304026170480, -26.47788675693900018, -34.64999999999999858 ) ) ;
#3510=CARTESIAN_POINT ( 'NONE',  ( 27.13393739769620083, 7.383811055320659733, -72.14999999999999147 ) ) ;
#3517=CYLINDRICAL_SURFACE ( 'NONE', #18958, 2.999999999999999112 ) ;
#3518=DIRECTION ( 'NONE',  ( 0.000000000000000000, 0.000000000000000000, -1.000000000000000000 ) ) ;
#3519=CARTESIAN_POINT ( 'NONE',  ( -0.03447620312153085176, -4.141051901845263394, -34.79644660940673617 ) ) ;
#3527=DIRECTION ( 'NONE',  ( -0.9304380493636941196, -0.3664492274467011090, 0.000000000000000000 ) ) ;
#3557=CARTESIAN_POINT ( 'NONE',  ( 44.68310481377952215, 1.934496889718864132, -44.40181776504896760 ) ) ;
#3576=CARTESIAN_POINT ( 'NONE',  ( 43.43392086188707424, -39.90592420333850043, -69.40102220065354288 ) ) ;
#3578=SURFACE_STYLE_USAGE ( .BOTH. , #47350 ) ;
#3591=CARTESIAN_POINT ( 'NONE',  ( 0.2007819157888829364, -20.71710295694509441, -34.66110989977897106 ) ) ;
#3597=ORIENTED_EDGE ( 'NONE', *, *, #6221, .F. ) ;
#3598=DIRECTION ( 'NONE',  ( 0.000000000000000000, 0.000000000000000000, 1.000000000000000000 ) ) ;
#3599=ORIENTED_EDGE ( 'NONE', *, *, #45140, .F. ) ;
#3611=CARTESIAN_POINT ( 'NONE',  ( -20.20258579638655050, -1.450742213106093859, -52.59143307560878355 ) ) ;
#3625=EDGE_CURVE ( 'NONE', #12367, #46682, #11287, .T. ) ;
#3629=( BOUNDED_CURVE ( )  B_SPLINE_CURVE ( 3, ( #15946, #27727, #51844, #31131 ),
 .UNSPECIFIED., .F., .T. ) 
 B_SPLINE_CURVE_WITH_KNOTS ( ( 4, 4 ),
 ( 4.675428907228452502, 4.913492185948230784 ),
 .UNSPECIFIED. ) 
 CURVE ( )  GEOMETRIC_REPRESENTATION_ITEM ( )  RATIONAL_B_SPLINE_CURVE ( ( 1.000000000000000000, 0.9952827299573674402, 0.9952827299573674402, 1.000000000000000000 ) ) 
 REPRESENTATION_ITEM ( '' )  );
#3633=EDGE_LOOP ( 'NONE', ( #9251, #51181, #8497, #30528 ) ) ;
#3639=CIRCLE ( 'NONE', #10337, 2.000000000000000000 ) ;
#3645=CARTESIAN_POINT ( 'NONE',  ( 45.28676693330019987, -37.97973142300439520, -63.87794661417289888 ) ) ;
#3646=FACE_OUTER_BOUND ( 'NONE', #21924, .T. ) ;
#3647=DIRECTION ( 'NONE',  ( 0.7071067811865475727, 0.000000000000000000, 0.7071067811865475727 ) ) ;
#3653=CARTESIAN_POINT ( 'NONE',  ( 46.06859774010791853, 7.964158654876348109, -60.46635192367470069 ) ) ;
#3656=CARTESIAN_POINT ( 'NONE',  ( 16.13393739769599833, 14.38381105532070059, -62.64999999999999858 ) ) ;
#3660=LINE ( 'NONE', #27995, #39032 ) ;
#3670=PLANE ( 'NONE',  #39408 ) ;
#3674=EDGE_LOOP ( 'NONE', ( #48511, #3456, #31767, #43641, #39332, #12826 ) ) ;
#3681=FACE_OUTER_BOUND ( 'NONE', #18794, .T. ) ;
#3683=AXIS2_PLACEMENT_3D ( 'NONE', #2595, #14641, #18569 ) ;
#3685=CARTESIAN_POINT ( 'NONE',  ( 16.13393739769620083, -15.61618894467929941, -81.65000000000000568 ) ) ;
#3693=ADVANCED_FACE ( 'NONE', ( #50131 ), #33866, .T. ) ;
#3698=VECTOR ( 'NONE', #48354, 1000.000000000000114 ) ;
#3729=DIRECTION ( 'NONE',  ( 0.000000000000000000, 0.7071067811865463515, -0.7071067811865487940 ) ) ;
#3732=EDGE_CURVE ( 'NONE', #27321, #49113, #20650, .T. ) ;
#3738=ORIENTED_EDGE ( 'NONE', *, *, #25277, .F. ) ;
#3745=CARTESIAN_POINT ( 'NONE',  ( 1.057008924472659928, -8.644787692947790703, -34.64999999999999858 ) ) ;
#3749=CARTESIAN_POINT ( 'NONE',  ( 43.72566957196067250, 6.648299627497703312, -71.69133740782910991 ) ) ;
#3765=ADVANCED_FACE ( 'NONE', ( #19237 ), #11391, .F. ) ;
#3776=ORIENTED_EDGE ( 'NONE', *, *, #40349, .T. ) ;
#3782=CARTESIAN_POINT ( 'NONE',  ( -18.32056709076247714, -20.94004174811257357, -50.69739520735551253 ) ) ;
#3791=CARTESIAN_POINT ( 'NONE',  ( 47.12245394960989842, 8.044248941898629823, -35.02700949942429531 ) ) ;
#3799=EDGE_CURVE ( 'NONE', #22659, #47961, #48145, .T. ) ;
#3800=ORIENTED_EDGE ( 'NONE', *, *, #6521, .F. ) ;
#3802=ORIENTED_EDGE ( 'NONE', *, *, #51070, .T. ) ;
#3803=EDGE_LOOP ( 'NONE', ( #43124, #165, #44393, #40521 ) ) ;
#3810=DIRECTION ( 'NONE',  ( 1.000000000000000000, 0.000000000000000000, 0.000000000000000000 ) ) ;
#3811=CARTESIAN_POINT ( 'NONE',  ( 45.27455033981039634, -33.67802718498660397, -34.68571053370059332 ) ) ;
#3814=ORIENTED_EDGE ( 'NONE', *, *, #36862, .T. ) ;
#3815=CARTESIAN_POINT ( 'NONE',  ( 44.30108064003440660, 1.883811055320657291, -51.43657703546407589 ) ) ;
#3823=ADVANCED_FACE ( 'NONE', ( #4034 ), #19994, .T. ) ;
#3825=ORIENTED_EDGE ( 'NONE', *, *, #39065, .T. ) ;
#3830=CARTESIAN_POINT ( 'NONE',  ( 42.26101777068934950, -39.79243905365653688, -75.07061934747760290 ) ) ;
#3832=DIRECTION ( 'NONE',  ( 0.000000000000000000, -1.000000000000000000, 0.000000000000000000 ) ) ;
#3833=AXIS2_PLACEMENT_3D ( 'NONE', #46056, #25837, #5191 ) ;
#3841=VERTEX_POINT ( 'NONE', #3003 ) ;
#3849=CARTESIAN_POINT ( 'NONE',  ( 41.61087022781433831, 8.489620259922302736, -78.20791600774551000 ) ) ;
#3859=CARTESIAN_POINT ( 'NONE',  ( 29.13393739769619728, -26.76363820448759867, -35.14999999999999858 ) ) ;
#3866=CARTESIAN_POINT ( 'NONE',  ( -22.10874326092599418, -7.786548904876307908, -54.22730359629444052 ) ) ;
#3883=CARTESIAN_POINT ( 'NONE',  ( 42.76911844754650360, -36.11618894467930119, -61.17703620997009750 ) ) ;
#3889=CARTESIAN_POINT ( 'NONE',  ( -0.02503409344753749696, -22.81475709047199985, -34.78823607925542660 ) ) ;
#3902=CARTESIAN_POINT ( 'NONE',  ( 43.46118252345650035, -37.78219224926380093, -73.01045585346660971 ) ) ;
#3903=CARTESIAN_POINT ( 'NONE',  ( 16.13393739769620083, -15.61618894467929941, -69.65000000000000568 ) ) ;
#3910=CARTESIAN_POINT ( 'NONE',  ( 43.53205667065411433, 7.709292839630085048, -73.05708749340493569 ) ) ;
#3920=CIRCLE ( 'NONE', #10617, 33.00000000000000000 ) ;
#3936=CARTESIAN_POINT ( 'NONE',  ( 23.61468320491630024, -48.77463972988229557, -35.01184033120630090 ) ) ;
#3945=DIRECTION ( 'NONE',  ( 1.000000000000000000, 0.000000000000000000, 0.000000000000000000 ) ) ;
#3946=CARTESIAN_POINT ( 'NONE',  ( 2.452285341914063110, -25.68011462166456127, -34.81767276520687915 ) ) ;
#3953=VECTOR ( 'NONE', #2046, 1000.000000000000000 ) ;
#3954=CARTESIAN_POINT ( 'NONE',  ( 11.87719327230648680, 10.74943050428830560, -34.64999999999999858 ) ) ;
#3957=EDGE_CURVE ( 'NONE', #336, #32835, #38063, .T. ) ;
#3975=CARTESIAN_POINT ( 'NONE',  ( 14.13393739769630031, 1.391621760993509982, -35.14999999999999858 ) ) ;
#3977=B_SPLINE_CURVE_WITH_KNOTS ( 'NONE', 3,
 ( #25139, #5255, #21209, #41925 ),
 .UNSPECIFIED., .F., .F.,
 ( 4, 4 ),
 ( 0.000000000000000000, 1.000000000000000000 ),
 .UNSPECIFIED. ) ;
#3980=ADVANCED_FACE ( 'NONE', ( #13462 ), #45021, .T. ) ;
#3989=CARTESIAN_POINT ( 'NONE',  ( 10.13393739769589885, 22.91950879131600161, -54.64999999999999858 ) ) ;
#3994=FACE_OUTER_BOUND ( 'NONE', #38869, .T. ) ;
#4000=CARTESIAN_POINT ( 'NONE',  ( 17.63393739769629676, 0.9255523191756780399, -34.64999999999999858 ) ) ;
#4024=APPLICATION_CONTEXT ( 'automotive_design' ) ;
#4028=CARTESIAN_POINT ( 'NONE',  ( -0.02503409344748377258, -4.155984009993316519, -34.78823607925539108 ) ) ;
#4029=DIRECTION ( 'NONE',  ( 1.000000000000000000, 0.000000000000000000, 0.000000000000000000 ) ) ;
#4034=FACE_OUTER_BOUND ( 'NONE', #42148, .T. ) ;
#4040=CARTESIAN_POINT ( 'NONE',  ( -6.866062602303790285, -15.61618894467929941, -84.65000000000000568 ) ) ;
#4048=ORIENTED_EDGE ( 'NONE', *, *, #4107, .F. ) ;
#4060=EDGE_LOOP ( 'NONE', ( #950, #1933, #44000, #39317 ) ) ;
#4061=CARTESIAN_POINT ( 'NONE',  ( 44.66749666976073740, 1.931639890059055675, -44.69767322463768267 ) ) ;
#4066=B_SPLINE_CURVE_WITH_KNOTS ( 'NONE', 3,
 ( #13968, #7906, #3468, #51421, #27041, #14992, #48, #11331, #16025, #23094, #47493, #11853, #38857, #12100 ),
 .UNSPECIFIED., .F., .F.,
 ( 4, 2, 2, 2, 2, 2, 4 ),
 ( 0.000000000000000000, 0.2500000000000620615, 0.3750000000001004197, 0.4375000000001131872, 0.4687500000001195155, 0.5000000000001258993, 1.000000000000000000 ),
 .UNSPECIFIED. ) ;
#4073=VERTEX_POINT ( 'NONE', #29921 ) ;
#4077=CARTESIAN_POINT ( 'NONE',  ( 42.94455545980090250, -39.86079545475082142, -71.76762032940678182 ) ) ;
#4079=AXIS2_PLACEMENT_3D ( 'NONE', #16959, #8831, #28469 ) ;
#4085=ORIENTED_EDGE ( 'NONE', *, *, #36354, .T. ) ;
#4092=CYLINDRICAL_SURFACE ( 'NONE', #31109, 0.5000000000000014433 ) ;
#4093=CARTESIAN_POINT ( 'NONE',  ( 41.55703060469905097, 8.483152042567137840, -78.46913939333057897 ) ) ;
#4107=EDGE_CURVE ( 'NONE', #46028, #38136, #30447, .T. ) ;
#4110=DIRECTION ( 'NONE',  ( 1.000000000000000000, 0.000000000000000000, 0.000000000000000000 ) ) ;
#4118=ORIENTED_EDGE ( 'NONE', *, *, #33456, .F. ) ;
#4119=FACE_OUTER_BOUND ( 'NONE', #30254, .T. ) ;
#4122=CIRCLE ( 'NONE', #745, 1.999999999999998224 ) ;
#4138=CARTESIAN_POINT ( 'NONE',  ( 0.1754120801744591396, 19.58041923384463345, -34.67138862792307918 ) ) ;
#4139=DIRECTION ( 'NONE',  ( 0.000000000000000000, 0.000000000000000000, 1.000000000000000000 ) ) ;
#4145=CARTESIAN_POINT ( 'NONE',  ( 16.13393739769620083, -15.61618894467929941, -35.14999999999999858 ) ) ;
#4151=EDGE_LOOP ( 'NONE', ( #44976, #16825, #37376, #26694 ) ) ;
#4153=CARTESIAN_POINT ( 'NONE',  ( 42.15399884802307895, 7.540547227200079305, -79.88060530502062306 ) ) ;
#4162=VERTEX_POINT ( 'NONE', #14220 ) ;
#4176=VERTEX_POINT ( 'NONE', #33607 ) ;
#4181=FACE_OUTER_BOUND ( 'NONE', #18744, .T. ) ;
#4184=CARTESIAN_POINT ( 'NONE',  ( 18.02855964079323670, -32.51455091268738329, -34.84133294386911217 ) ) ;
#4194=DIRECTION ( 'NONE',  ( 0.000000000000000000, 0.000000000000000000, 1.000000000000000000 ) ) ;
#4195=AXIS2_PLACEMENT_3D ( 'NONE', #17134, #1139, #33617 ) ;
#4203=B_SPLINE_CURVE_WITH_KNOTS ( 'NONE', 3,
 ( #8870, #9127, #41344, #20639, #1261, #17249, #28508, #48440, #32946, #16724 ),
 .UNSPECIFIED., .F., .F.,
 ( 4, 2, 2, 2, 4 ),
 ( -0.0004281134588448370026, 0.000000000000000000, 0.02012916873217849775, 0.03942875605114479903, 0.05028014561732389170 ),
 .UNSPECIFIED. ) ;
#4208=DIRECTION ( 'NONE',  ( 1.000000000000000000, 0.000000000000000000, 0.000000000000000000 ) ) ;
#4211=DIRECTION ( 'NONE',  ( -0.5877852522924744694, -0.8090169943749464521, 0.000000000000000000 ) ) ;
#4223=CARTESIAN_POINT ( 'NONE',  ( 9.894687805641289913, 22.37488585622680048, -34.64999999999999858 ) ) ;
#4232=CARTESIAN_POINT ( 'NONE',  ( 46.63604585716099393, 7.879209231990749629, -34.65000333419789769 ) ) ;
#4235=AXIS2_PLACEMENT_3D ( 'NONE', #15787, #23363, #12123 ) ;
#4243=CARTESIAN_POINT ( 'NONE',  ( 0.03729862092327890233, -45.78233701092020169, -34.73403371893299862 ) ) ;
#4249=CARTESIAN_POINT ( 'NONE',  ( 42.30695455116141801, 6.440213284654995540, -78.78491382788429576 ) ) ;
#4253=CARTESIAN_POINT ( 'NONE',  ( 41.95606716547078463, -37.61662454033810121, -80.53928227081438251 ) ) ;
#4261=LINE ( 'NONE', #26718, #4910 ) ;
#4276=CARTESIAN_POINT ( 'NONE',  ( 17.59555472085904171, 18.38379266497329212, -83.19301782015158153 ) ) ;
#4278=CARTESIAN_POINT ( 'NONE',  ( 18.13393739769620083, -41.61618894467930119, -35.14999999999999858 ) ) ;
#4280=CARTESIAN_POINT ( 'NONE',  ( 33.13393739769620083, 7.383811055320659733, -59.64999999999999147 ) ) ;
#4295=ORIENTED_EDGE ( 'NONE', *, *, #330, .F. ) ;
#4309=VERTEX_POINT ( 'NONE', #3975 ) ;
#4321=LINE ( 'NONE', #1432, #39291 ) ;
#4333=CARTESIAN_POINT ( 'NONE',  ( 44.00040578421071302, -39.95470630028139425, -66.65770786811647497 ) ) ;
#4336=EDGE_CURVE ( 'NONE', #43415, #18539, #8273, .T. ) ;
#4341=CARTESIAN_POINT ( 'NONE',  ( 14.63183004844949942, -32.15985502643049898, -34.65000333055159842 ) ) ;
#4349=CARTESIAN_POINT ( 'NONE',  ( 23.48034592329180015, 17.80194031521820008, -34.71551406240349280 ) ) ;
#4351=CARTESIAN_POINT ( 'NONE',  ( 42.26549200200313550, 8.560451897770759544, -75.04938479633833026 ) ) ;
#4352=CARTESIAN_POINT ( 'NONE',  ( 14.13393739769619906, -41.61618894467930119, -54.64999999999999858 ) ) ;
#4357=VERTEX_POINT ( 'NONE', #18916 ) ;
#4365=EDGE_LOOP ( 'NONE', ( #44840, #47760, #127, #9465, #41618, #39040, #11895 ) ) ;
#4366=ADVANCED_FACE ( 'NONE', ( #30957 ), #11852, .T. ) ;
#4372=DIRECTION ( 'NONE',  ( 0.6933752452815366007, -0.7071067811865471286, -0.1386750490563077864 ) ) ;
#4383=EDGE_CURVE ( 'NONE', #22924, #40090, #30698, .T. ) ;
#4384=CARTESIAN_POINT ( 'NONE',  ( 29.13393739769619728, 4.555383930574470774, -84.65000000000000568 ) ) ;
#4386=CARTESIAN_POINT ( 'NONE',  ( -0.01592648613901120544, -27.06133052499065172, -34.78031642072627250 ) ) ;
#4402=EDGE_CURVE ( 'NONE', #31635, #37056, #28349, .T. ) ;
#4426=ADVANCED_FACE ( 'NONE', ( #7141 ), #7473, .F. ) ;
#4431=ADVANCED_FACE ( 'NONE', ( #27040 ), #49339, .F. ) ;
#4441=DIRECTION ( 'NONE',  ( 0.000000000000000000, 0.000000000000000000, 1.000000000000000000 ) ) ;
#4442=DIRECTION ( 'NONE',  ( -1.000000000000000000, 0.000000000000000000, 0.000000000000000000 ) ) ;
#4446=LINE ( 'NONE', #40864, #45982 ) ;
#4450=AXIS2_PLACEMENT_3D ( 'NONE', #24682, #861, #33071 ) ;
#4469=EDGE_LOOP ( 'NONE', ( #21660, #15593, #7563, #28992 ) ) ;
#4479=ORIENTED_EDGE ( 'NONE', *, *, #36354, .F. ) ;
#4480=DIRECTION ( 'NONE',  ( -1.000000000000000000, 0.000000000000000000, 0.000000000000000000 ) ) ;
#4487=CARTESIAN_POINT ( 'NONE',  ( 14.63393739769620083, -23.61618894467940066, -35.14999999999999858 ) ) ;
#4502=CARTESIAN_POINT ( 'NONE',  ( 41.96574616844770844, 6.385856618463681578, -80.49088675293293704 ) ) ;
#4505=CARTESIAN_POINT ( 'NONE',  ( 45.32664390791340026, 2.629232284582370127, -34.65030768300919561 ) ) ;
#4506=CARTESIAN_POINT ( 'NONE',  ( 42.40338535657301833, -37.68800879611313093, -78.30275109164772118 ) ) ;
#4515=CARTESIAN_POINT ( 'NONE',  ( 18.11900864776900022, 1.362847559348050019, -35.02873218748179340 ) ) ;
#4519=EDGE_CURVE ( 'NONE', #38150, #34997, #2485, .T. ) ;
#4525=ORIENTED_EDGE ( 'NONE', *, *, #44169, .T. ) ;
#4533=CARTESIAN_POINT ( 'NONE',  ( -13.73674066540309902, -30.55263188852779876, -46.71145918530379504 ) ) ;
#4539=ADVANCED_FACE ( 'NONE', ( #48119 ), #16401, .T. ) ;
#4546=CARTESIAN_POINT ( 'NONE',  ( 28.28038400710291356, -22.62894316431776431, -34.79644660940672907 ) ) ;
#4552=EDGE_LOOP ( 'NONE', ( #47795, #4567, #42876, #32069 ) ) ;
#4559=CARTESIAN_POINT ( 'NONE',  ( 0.4371248283888460318, -8.845792823550640449, -35.02873218748179340 ) ) ;
#4562=FACE_OUTER_BOUND ( 'NONE', #8022, .T. ) ;
#4567=ORIENTED_EDGE ( 'NONE', *, *, #29640, .F. ) ;
#4578=ORIENTED_EDGE ( 'NONE', *, *, #29513, .T. ) ;
#4585=CARTESIAN_POINT ( 'NONE',  ( 43.69898371111283097, -39.92948724415479234, -68.11687742724626560 ) ) ;
#4589=DIRECTION ( 'NONE',  ( 0.000000000000000000, 0.000000000000000000, 1.000000000000000000 ) ) ;
#4603=CARTESIAN_POINT ( 'NONE',  ( 42.87835492171312524, 8.621997877449000924, -72.08792712645744416 ) ) ;
#4610=ORIENTED_EDGE ( 'NONE', *, *, #24701, .T. ) ;
#4613=ORIENTED_EDGE ( 'NONE', *, *, #36546, .T. ) ;
#4634=CARTESIAN_POINT ( 'NONE',  ( -0.1437508118502176246, -3.968240916618980041, -34.89146800830123851 ) ) ;
#4639=DIRECTION ( 'NONE',  ( 0.000000000000000000, 0.000000000000000000, -1.000000000000000000 ) ) ;
#4646=EDGE_CURVE ( 'NONE', #48924, #17157, #40980, .T. ) ;
#4654=CARTESIAN_POINT ( 'NONE',  ( 16.98877563629383403, -17.26294695554419434, -34.79644660940672907 ) ) ;
#4656=DIRECTION ( 'NONE',  ( 0.000000000000000000, -1.000000000000000000, 0.000000000000000000 ) ) ;
#4657=DIRECTION ( 'NONE',  ( 8.462868000000000073E-18, -1.066343000000000058E-17, 1.000000000000000000 ) ) ;
#4665=ORIENTED_EDGE ( 'NONE', *, *, #41164, .T. ) ;
#4678=EDGE_CURVE ( 'NONE', #46513, #35078, #33136, .T. ) ;
#4688=CARTESIAN_POINT ( 'NONE',  ( 0.7917425790954289999, -51.06248658143009322, -34.07803169642789953 ) ) ;
#4689=AXIS2_PLACEMENT_3D ( 'NONE', #50977, #18740, #18486 ) ;
#4692=CARTESIAN_POINT ( 'NONE',  ( 14.28038400710302724, 1.354373803797940035, -34.79644660940672907 ) ) ;
#4695=ORIENTED_EDGE ( 'NONE', *, *, #47943, .T. ) ;
#4698=ORIENTED_EDGE ( 'NONE', *, *, #4678, .F. ) ;
#4699=DIRECTION ( 'NONE',  ( 0.6339889056055382222, 0.000000000000000000, -0.7733421413379021336 ) ) ;
#4700=CARTESIAN_POINT ( 'NONE',  ( 29.11900864776890074, -26.73446727828369873, -35.02873218748179340 ) ) ;
#4711=DIRECTION ( 'NONE',  ( 0.000000000000000000, 0.000000000000000000, -1.000000000000000000 ) ) ;
#4713=AXIS2_PLACEMENT_3D ( 'NONE', #7079, #23029, #3146 ) ;
#4724=CARTESIAN_POINT ( 'NONE',  ( 38.67452568954060155, 6.328436186825679322, -81.65000000000000568 ) ) ;
#4755=ORIENTED_EDGE ( 'NONE', *, *, #16219, .T. ) ;
#4765=DIRECTION ( 'NONE',  ( 1.000000000000000000, 0.000000000000000000, 0.000000000000000000 ) ) ;
#4766=CARTESIAN_POINT ( 'NONE',  ( 42.31162289222356776, 6.440951911319115375, -78.76157231913752810 ) ) ;
#4771=EDGE_CURVE ( 'NONE', #45496, #21348, #31301, .T. ) ;
#4773=CARTESIAN_POINT ( 'NONE',  ( 43.25224801953689990, -37.81438149150337580, -74.05839184249462903 ) ) ;
#4784=EDGE_CURVE ( 'NONE', #21587, #12629, #43494, .T. ) ;
#4796=CARTESIAN_POINT ( 'NONE',  ( 13.13393739769600010, 18.38381105532060289, -83.01107220193038927 ) ) ;
#4800=FACE_OUTER_BOUND ( 'NONE', #5727, .T. ) ;
#4817=ORIENTED_EDGE ( 'NONE', *, *, #22288, .T. ) ;
#4823=DIRECTION ( 'NONE',  ( -0.6522074047277892639, -0.2731766849828938248, 0.7071067811865464625 ) ) ;
#4837=VERTEX_POINT ( 'NONE', #6954 ) ;
#4840=LINE ( 'NONE', #25254, #34555 ) ;
#4843=CIRCLE ( 'NONE', #36619, 2.999999999999994227 ) ;
#4844=CARTESIAN_POINT ( 'NONE',  ( 46.98749078828947034, 4.883811055320659733, -34.79644660940672907 ) ) ;
#4854=CARTESIAN_POINT ( 'NONE',  ( 41.52003636951408794, -39.71129688314757544, -78.64757901482110469 ) ) ;
#4863=CARTESIAN_POINT ( 'NONE',  ( 23.62413055734869971, -48.75525398023999912, -35.14999999999999858 ) ) ;
#4864=ORIENTED_EDGE ( 'NONE', *, *, #8510, .F. ) ;
#4872=CARTESIAN_POINT ( 'NONE',  ( 41.42126661153417189, 8.467416272844669578, -79.12460387921866811 ) ) ;
#4873=CARTESIAN_POINT ( 'NONE',  ( 28.63393739769619728, -8.399310579809030841, -34.64999999999999858 ) ) ;
#4874=FACE_OUTER_BOUND ( 'NONE', #39965, .T. ) ;
#4881=DIRECTION ( 'NONE',  ( 0.000000000000000000, -1.000000000000000000, 0.000000000000000000 ) ) ;
#4886=VERTEX_POINT ( 'NONE', #39437 ) ;
#4889=CARTESIAN_POINT ( 'NONE',  ( -7.203365501241526303, 15.66981567447505519, -41.43129459776488233 ) ) ;
#4890=CARTESIAN_POINT ( 'NONE',  ( 14.62183896472512323, 18.38379308823580516, -83.18933379704752440 ) ) ;
#4896=ORIENTED_EDGE ( 'NONE', *, *, #13025, .T. ) ;
#4907=CIRCLE ( 'NONE', #17481, 5.251829701412240148 ) ;
#4909=DIRECTION ( 'NONE',  ( 0.000000000000000000, 0.000000000000000000, -1.000000000000000000 ) ) ;
#4910=VECTOR ( 'NONE', #31415, 1000.000000000000114 ) ;
#4917=CARTESIAN_POINT ( 'NONE',  ( 0.2749857802900130266, 19.51618704702660168, -34.65028054350399600 ) ) ;
#4923=CARTESIAN_POINT ( 'NONE',  ( 0.4644698840366610071, -8.836735345369399752, -34.95504743437659556 ) ) ;
#4925=PLANE ( 'NONE',  #2470 ) ;
#4932=DIRECTION ( 'NONE',  ( -1.000000000000000000, 0.000000000000000000, 0.000000000000000000 ) ) ;
#4948=VECTOR ( 'NONE', #49581, 1000.000000000000000 ) ;
#4955=CARTESIAN_POINT ( 'NONE',  ( 3.987490788289483667, -22.62894316431776787, -34.79644660940672907 ) ) ;
#4957=EDGE_CURVE ( 'NONE', #36007, #36393, #12168, .T. ) ;
#4960=EDGE_CURVE ( 'NONE', #15778, #32833, #13382, .T. ) ;
#4976=CYLINDRICAL_SURFACE ( 'NONE', #11963, 2.999999999999999112 ) ;
#4978=CARTESIAN_POINT ( 'NONE',  ( 47.13393649688870113, -39.28050833195659663, -53.76790015415899404 ) ) ;
#4979=EDGE_CURVE ( 'NONE', #38690, #45896, #10062, .T. ) ;
#4991=FACE_OUTER_BOUND ( 'NONE', #43607, .T. ) ;
#4994=FACE_OUTER_BOUND ( 'NONE', #19302, .T. ) ;
#4997=EDGE_LOOP ( 'NONE', ( #29743, #2502 ) ) ;
#5035=ORIENTED_EDGE ( 'NONE', *, *, #9537, .F. ) ;
#5037=CARTESIAN_POINT ( 'NONE',  ( 42.03721945691450657, 6.397288423599181151, -80.13352371291058773 ) ) ;
#5045=CARTESIAN_POINT ( 'NONE',  ( 42.27252180811520788, -37.66705137823122129, -78.95707406319118604 ) ) ;
#5060=DIRECTION ( 'NONE',  ( 0.000000000000000000, 0.000000000000000000, -1.000000000000000000 ) ) ;
#5061=AXIS2_PLACEMENT_3D ( 'NONE', #46242, #45189, #42298 ) ;
#5065=AXIS2_PLACEMENT_3D ( 'NONE', #38936, #15342, #43128 ) ;
#5067=EDGE_CURVE ( 'NONE', #23939, #2764, #251, .T. ) ;
#5068=CARTESIAN_POINT ( 'NONE',  ( 22.19151943370611946, 22.78899166960877309, -34.82441657595546758 ) ) ;
#5071=VECTOR ( 'NONE', #25438, 1000.000000000000000 ) ;
#5075=CARTESIAN_POINT ( 'NONE',  ( -1.453061824024428850, -23.46064660281889047, -43.67210485538161890 ) ) ;
#5080=EDGE_CURVE ( 'NONE', #25882, #7747, #49095, .T. ) ;
#5084=DIRECTION ( 'NONE',  ( 0.000000000000000000, 0.7071067811865475727, 0.7071067811865475727 ) ) ;
#5090=VERTEX_POINT ( 'NONE', #59 ) ;
#5091=EDGE_LOOP ( 'NONE', ( #31573, #33406, #26990, #15134, #49184, #11411, #36586 ) ) ;
#5103=EDGE_CURVE ( 'NONE', #45283, #49938, #42559, .T. ) ;
#5118=CARTESIAN_POINT ( 'NONE',  ( 29.13393739769619728, 4.883811055320659733, -81.65000000000000568 ) ) ;
#5128=CARTESIAN_POINT ( 'NONE',  ( 14.37540540599747452, -41.85765695298066902, -34.70142521051218409 ) ) ;
#5139=VECTOR ( 'NONE', #50255, 1000.000000000000000 ) ;
#5147=CARTESIAN_POINT ( 'NONE',  ( 43.22233765097706737, 8.654584815917743867, -70.42371853659152237 ) ) ;
#5148=CARTESIAN_POINT ( 'NONE',  ( 44.66618967801522899, -33.16378185082322005, -44.72241104285924251 ) ) ;
#5150=CARTESIAN_POINT ( 'NONE',  ( 11.96660005458890019, -42.11618894467939356, -34.64999999999999858 ) ) ;
#5152=ORIENTED_EDGE ( 'NONE', *, *, #43152, .F. ) ;
#5164=VERTEX_POINT ( 'NONE', #24639 ) ;
#5169=EDGE_CURVE ( 'NONE', #40090, #611, #16285, .T. ) ;
#5182=AXIS2_PLACEMENT_3D ( 'NONE', #9588, #32618, #29223 ) ;
#5186=AXIS2_PLACEMENT_3D ( 'NONE', #4280, #48311, #40440 ) ;
#5191=DIRECTION ( 'NONE',  ( 0.7071067811865472397, -0.7071067811865479058, 0.000000000000000000 ) ) ;
#5198=CARTESIAN_POINT ( 'NONE',  ( 28.13393739769619728, -22.54439217495490055, -47.64999999999999858 ) ) ;
#5225=CARTESIAN_POINT ( 'NONE',  ( -22.69159524740030065, -13.72712742066280001, -54.49830448709099784 ) ) ;
#5231=CARTESIAN_POINT ( 'NONE',  ( 22.29130106582169901, -53.79438198982389707, -34.67842804303180060 ) ) ;
#5235=EDGE_LOOP ( 'NONE', ( #3490, #5546, #8752, #48826 ) ) ;
#5255=CARTESIAN_POINT ( 'NONE',  ( 14.13393739769630031, 1.380694156556678820, -35.10658870009210375 ) ) ;
#5256=CARTESIAN_POINT ( 'NONE',  ( 44.04591232117690680, -40.05666563364601984, -66.03710115006609271 ) ) ;
#5257=EDGE_CURVE ( 'NONE', #10013, #30043, #34998, .T. ) ;
#5261=ADVANCED_FACE ( 'NONE', ( #12357 ), #28321, .T. ) ;
#5265=DIRECTION ( 'NONE',  ( 0.000000000000000000, 0.000000000000000000, -1.000000000000000000 ) ) ;
#5285=CARTESIAN_POINT ( 'NONE',  ( -27.51648586239810257, -147.0143260265109859, -50.16206650068949813 ) ) ;
#5304=CARTESIAN_POINT ( 'NONE',  ( 42.63564515191668391, -37.72326100604439603, -77.14139479405923794 ) ) ;
#5305=ORIENTED_EDGE ( 'NONE', *, *, #38281, .F. ) ;
#5313=DIRECTION ( 'NONE',  ( 0.000000000000000000, 1.000000000000000000, 0.000000000000000000 ) ) ;
#5326=ADVANCED_FACE ( 'NONE', ( #22009 ), #49573, .T. ) ;
#5327=VECTOR ( 'NONE', #40021, 1000.000000000000000 ) ;
#5334=LINE ( 'NONE', #44378, #1806 ) ;
#5342=VERTEX_POINT ( 'NONE', #6310 ) ;
#5349=EDGE_LOOP ( 'NONE', ( #17131, #33679 ) ) ;
#5350=AXIS2_PLACEMENT_3D ( 'NONE', #20904, #25082, #45029 ) ;
#5351=DIRECTION ( 'NONE',  ( 0.000000000000000000, 0.000000000000000000, -1.000000000000000000 ) ) ;
#5358=CARTESIAN_POINT ( 'NONE',  ( 17.07096049057464526, 12.61358818065451182, -60.51477253168783221 ) ) ;
#5366=CARTESIAN_POINT ( 'NONE',  ( 18.13393739769639978, 10.38381105532070059, -54.64999999999999858 ) ) ;
#5368=DIRECTION ( 'NONE',  ( 0.000000000000000000, 0.000000000000000000, 1.000000000000000000 ) ) ;
#5369=EDGE_CURVE ( 'NONE', #34827, #31635, #5791, .T. ) ;
#5377=DIRECTION ( 'NONE',  ( 8.462868000000000073E-18, -1.066343000000000058E-17, 1.000000000000000000 ) ) ;
#5380=CARTESIAN_POINT ( 'NONE',  ( 28.28038400710291356, -22.62894316431776431, -34.79644660940672907 ) ) ;
#5391=ORIENTED_EDGE ( 'NONE', *, *, #627, .T. ) ;
#5395=ORIENTED_EDGE ( 'NONE', *, *, #7637, .F. ) ;
#5399=CARTESIAN_POINT ( 'NONE',  ( 20.63393739769599833, 10.38381105532070059, -35.14999999999999858 ) ) ;
#5400=CARTESIAN_POINT ( 'NONE',  ( 43.62374791249758488, 8.690508226694738880, -68.48145595108481132 ) ) ;
#5415=ORIENTED_EDGE ( 'NONE', *, *, #6221, .T. ) ;
#5417=CARTESIAN_POINT ( 'NONE',  ( -9.742541826421756923, 13.56590212943579488, -43.61116652808541971 ) ) ;
#5418=CARTESIAN_POINT ( 'NONE',  ( 16.13393739769620083, -15.61618894467929941, -35.14999999999999858 ) ) ;
#5437=CARTESIAN_POINT ( 'NONE',  ( 4.133937397696205274, -22.54439217495489700, -35.01561944896766931 ) ) ;
#5439=CARTESIAN_POINT ( 'NONE',  ( 46.50691046839970255, 8.847764697030390479, -54.64999999999999858 ) ) ;
#5445=CARTESIAN_POINT ( 'NONE',  ( 46.47536507427530239, -40.11920440292289669, -54.64999999999999858 ) ) ;
#5452=CARTESIAN_POINT ( 'NONE',  ( -18.28386310865111497, -15.61618894467930296, -82.14319696191608955 ) ) ;
#5454=DIRECTION ( 'NONE',  ( 0.000000000000000000, 0.000000000000000000, -1.000000000000000000 ) ) ;
#5456=DIRECTION ( 'NONE',  ( 0.3863301728269220581, -0.9223605572462000302, 0.000000000000000000 ) ) ;
#5458=EDGE_LOOP ( 'NONE', ( #35408, #39333, #4578, #45817 ) ) ;
#5460=ORIENTED_EDGE ( 'NONE', *, *, #30555, .T. ) ;
#5475=CARTESIAN_POINT ( 'NONE',  ( -6.866062602303790285, -15.61618894467929941, -84.65000000000000568 ) ) ;
#5479=CARTESIAN_POINT ( 'NONE',  ( -3.724451274984229787, -49.27919138543109767, -38.36253275904599747 ) ) ;
#5480=CARTESIAN_POINT ( 'NONE',  ( 16.13393739769620083, -15.61618894467929941, -35.14999999999999858 ) ) ;
#5489=ORIENTED_EDGE ( 'NONE', *, *, #765, .F. ) ;
#5491=LINE ( 'NONE', #37448, #37868 ) ;
#5494=AXIS2_PLACEMENT_3D ( 'NONE', #50990, #47839, #15092 ) ;
#5495=ADVANCED_FACE ( 'NONE', ( #22783 ), #38401, .T. ) ;
#5504=FACE_OUTER_BOUND ( 'NONE', #16358, .T. ) ;
#5509=CARTESIAN_POINT ( 'NONE',  ( 28.84982806847620296, -4.597856142697129833, -34.69901084462020435 ) ) ;
#5512=EDGE_CURVE ( 'NONE', #49694, #26020, #47443, .T. ) ;
#5516=CARTESIAN_POINT ( 'NONE',  ( 49.99435380674910334, -21.69248229676700390, -40.08896681911620163 ) ) ;
#5525=AXIS2_PLACEMENT_3D ( 'NONE', #48366, #4589, #40246 ) ;
#5529=DIRECTION ( 'NONE',  ( -0.2425356250363339128, 0.000000000000000000, -0.9701425001453316543 ) ) ;
#5540=LINE ( 'NONE', #20979, #6794 ) ;
#5542=CARTESIAN_POINT ( 'NONE',  ( 28.13393739769619728, -22.54439217495490055, -47.64999999999999858 ) ) ;
#5546=ORIENTED_EDGE ( 'NONE', *, *, #9537, .T. ) ;
#5554=ORIENTED_EDGE ( 'NONE', *, *, #8877, .F. ) ;
#5556=VECTOR ( 'NONE', #17360, 1000.000000000000114 ) ;
#5563=CARTESIAN_POINT ( 'NONE',  ( 45.33483351075369683, -38.08130543216955743, -63.64546632514639413 ) ) ;
#5570=AXIS2_PLACEMENT_3D ( 'NONE', #43637, #42609, #50721 ) ;
#5573=LINE ( 'NONE', #583, #48223 ) ;
#5575=ORIENTED_EDGE ( 'NONE', *, *, #10843, .T. ) ;
#5577=CONICAL_SURFACE ( 'NONE', #30656, 36.50000000000000711, 0.1651486774146265213 ) ;
#5581=EDGE_CURVE ( 'NONE', #6096, #5164, #44395, .T. ) ;
#5586=VECTOR ( 'NONE', #39667, 1000.000000000000000 ) ;
#5587=CARTESIAN_POINT ( 'NONE',  ( 22.13393739769600188, 22.91950879131610108, -35.09469305598949518 ) ) ;
#5600=DIRECTION ( 'NONE',  ( -1.000000000000000000, 0.000000000000000000, 0.000000000000000000 ) ) ;
#5606=AXIS2_PLACEMENT_3D ( 'NONE', #37524, #21785, #6085 ) ;
#5609=CARTESIAN_POINT ( 'NONE',  ( 15.19691430481735139, 12.61358818065448695, -60.51477253168943804 ) ) ;
#5618=CARTESIAN_POINT ( 'NONE',  ( 45.76382685223779845, 6.896243026199304182, -61.50055243549356732 ) ) ;
#5638=EDGE_CURVE ( 'NONE', #51719, #16095, #4261, .T. ) ;
#5655=VERTEX_POINT ( 'NONE', #51620 ) ;
#5663=CARTESIAN_POINT ( 'NONE',  ( 44.68656668712876723, 8.775795761644557658, -63.33238661288917370 ) ) ;
#5669=EDGE_LOOP ( 'NONE', ( #45036, #37948, #7848, #18221, #47425 ) ) ;
#5673=FACE_OUTER_BOUND ( 'NONE', #5091, .T. ) ;
#5687=CARTESIAN_POINT ( 'NONE',  ( -0.4410626023037970689, -22.87636857973879856, -35.14999999999999858 ) ) ;
#5691=CARTESIAN_POINT ( 'NONE',  ( 16.13393739769620083, -15.61618894467929941, -35.14999999999999858 ) ) ;
#5698=DIRECTION ( 'NONE',  ( -0.2201775509773258865, 0.9741807197710415922, 0.04993767387456497786 ) ) ;
#5705=VERTEX_POINT ( 'NONE', #3155 ) ;
#5707=ORIENTED_EDGE ( 'NONE', *, *, #19220, .F. ) ;
#5719=VERTEX_POINT ( 'NONE', #32696 ) ;
#5721=EDGE_CURVE ( 'NONE', #40328, #51550, #26223, .T. ) ;
#5726=LINE ( 'NONE', #21431, #14238 ) ;
#5727=EDGE_LOOP ( 'NONE', ( #41639, #51018, #5489, #36896 ) ) ;
#5728=CARTESIAN_POINT ( 'NONE',  ( -3.808086725916260296, -49.05426427394600353, -38.11425470904319468 ) ) ;
#5740=CIRCLE ( 'NONE', #44223, 3.000000000000003997 ) ;
#5758=CARTESIAN_POINT ( 'NONE',  ( 29.11900864776890074, -4.497910611074960485, -35.02873218748179340 ) ) ;
#5759=CARTESIAN_POINT ( 'NONE',  ( 17.64603583078074678, -49.61617097760094452, -83.18933379702824027 ) ) ;
#5762=CARTESIAN_POINT ( 'NONE',  ( 46.94493346192469119, -39.32255388986889955, -55.87925509191032347 ) ) ;
#5768=ORIENTED_EDGE ( 'NONE', *, *, #43490, .F. ) ;
#5776=LINE ( 'NONE', #10491, #49224 ) ;
#5791=LINE ( 'NONE', #42474, #14115 ) ;
#5794=ORIENTED_EDGE ( 'NONE', *, *, #27742, .F. ) ;
#5800=CARTESIAN_POINT ( 'NONE',  ( 0.1457841021255935343, -8.319710351909083812, -34.68167779225149161 ) ) ;
#5804=ORIENTED_EDGE ( 'NONE', *, *, #46017, .T. ) ;
#5805=FACE_OUTER_BOUND ( 'NONE', #42276, .T. ) ;
#5806=DIRECTION ( 'NONE',  ( -0.7071067811865511255, -0.7071067811865440200, 0.000000000000000000 ) ) ;
#5807=CARTESIAN_POINT ( 'NONE',  ( 23.13393739769620083, -2.337132753317950229, -39.64999999999999858 ) ) ;
#5811=CARTESIAN_POINT ( 'NONE',  ( 45.70030952488608733, -38.12153290717493093, -61.81813589282543120 ) ) ;
#5813=ORIENTED_EDGE ( 'NONE', *, *, #21013, .F. ) ;
#5817=VECTOR ( 'NONE', #14003, 1000.000000000000000 ) ;
#5834=ORIENTED_EDGE ( 'NONE', *, *, #40349, .F. ) ;
#5837=CARTESIAN_POINT ( 'NONE',  ( -11.80944000494499768, -34.05870648691990255, -45.03554556751409166 ) ) ;
#5843=DIRECTION ( 'NONE',  ( 0.000000000000000000, -1.000000000000000000, 0.000000000000000000 ) ) ;
#5851=ORIENTED_EDGE ( 'NONE', *, *, #42422, .F. ) ;
#5866=ORIENTED_EDGE ( 'NONE', *, *, #31602, .T. ) ;
#5867=CARTESIAN_POINT ( 'NONE',  ( 46.52998719834516805, 6.974158363553319973, -57.66974223607722649 ) ) ;
#5882=AXIS2_PLACEMENT_3D ( 'NONE', #5285, #48265, #16541 ) ;
#5885=AXIS2_PLACEMENT_3D ( 'NONE', #20518, #17389, #36512 ) ;
#5889=ORIENTED_EDGE ( 'NONE', *, *, #18096, .T. ) ;
#5894=CARTESIAN_POINT ( 'NONE',  ( 3.987490788289483667, -22.62894316431776787, -34.79644660940672907 ) ) ;
#5895=DIRECTION ( 'NONE',  ( -0.8660254037844390407, -0.4999999999999995004, -5.551115123125774074E-17 ) ) ;
#5899=EDGE_CURVE ( 'NONE', #6210, #27765, #13847, .T. ) ;
#5902=CIRCLE ( 'NONE', #35191, 3.000000000000003997 ) ;
#5906=EDGE_CURVE ( 'NONE', #11807, #12367, #5726, .T. ) ;
#5912=CARTESIAN_POINT ( 'NONE',  ( 45.05098064268191393, 8.801720613440462415, -61.56528120495866574 ) ) ;
#5925=CARTESIAN_POINT ( 'NONE',  ( 17.63393739769620083, -32.58675169315650066, -35.14999999999999858 ) ) ;
#5926=AXIS2_PLACEMENT_3D ( 'NONE', #17050, #33004, #29083 ) ;
#5927=ORIENTED_EDGE ( 'NONE', *, *, #45444, .F. ) ;
#5930=LINE ( 'NONE', #2255, #10981 ) ;
#5932=ADVANCED_FACE ( 'NONE', ( #2306 ), #34248, .T. ) ;
#5935=B_SPLINE_CURVE_WITH_KNOTS ( 'NONE', 3,
 ( #49435, #42340, #1723, #46019, #18480, #22397, #33417, #26585 ),
 .UNSPECIFIED., .F., .F.,
 ( 4, 2, 2, 4 ),
 ( 0.08616863070422620119, 0.1028498217474689974, 0.1208689123377440083, 0.1272047750358668849 ),
 .UNSPECIFIED. ) ;
#5953=CARTESIAN_POINT ( 'NONE',  ( 46.19857506040184347, -40.10460585432269909, -55.99493465955088567 ) ) ;
#5961=CYLINDRICAL_SURFACE ( 'NONE', #46865, 0.4999999999999997224 ) ;
#5963=ORIENTED_EDGE ( 'NONE', *, *, #36112, .F. ) ;
#5983=CYLINDRICAL_SURFACE ( 'NONE', #24291, 0.4999999999999982236 ) ;
#5986=CARTESIAN_POINT ( 'NONE',  ( -3.781020702776450193, -49.21259983685390438, -38.25262466549630602 ) ) ;
#5987=CARTESIAN_POINT ( 'NONE',  ( 28.13393739769619728, -8.687985714403851034, -47.64999999999999858 ) ) ;
#5998=ORIENTED_EDGE ( 'NONE', *, *, #39733, .T. ) ;
#6010=EDGE_CURVE ( 'NONE', #35235, #7036, #30326, .T. ) ;
#6013=ORIENTED_EDGE ( 'NONE', *, *, #48750, .T. ) ;
#6024=CARTESIAN_POINT ( 'NONE',  ( 46.36678673786003202, -40.25856219554008675, -54.59816767677268956 ) ) ;
#6027=ORIENTED_EDGE ( 'NONE', *, *, #12526, .T. ) ;
#6033=CARTESIAN_POINT ( 'NONE',  ( 46.38583315129304907, 9.012427395117848405, -54.56778683011410891 ) ) ;
#6034=DIRECTION ( 'NONE',  ( 0.000000000000000000, -1.000000000000000000, 0.000000000000000000 ) ) ;
#6059=CARTESIAN_POINT ( 'NONE',  ( 20.63393739769599833, 10.38381105532070059, -34.64999999999999858 ) ) ;
#6063=EDGE_LOOP ( 'NONE', ( #16722, #47120, #47886, #26331 ) ) ;
#6071=CARTESIAN_POINT ( 'NONE',  ( 45.74966035014026744, -38.12695882478442400, -61.57138523371202865 ) ) ;
#6072=ORIENTED_EDGE ( 'NONE', *, *, #48527, .T. ) ;
#6077=AXIS2_PLACEMENT_3D ( 'NONE', #6782, #46622, #10711 ) ;
#6079=CIRCLE ( 'NONE', #49598, 39.00000000000000711 ) ;
#6084=EDGE_CURVE ( 'NONE', #21662, #15955, #41434, .T. ) ;
#6085=DIRECTION ( 'NONE',  ( 0.7165155114351262622, 0.6975711590030506670, 0.000000000000000000 ) ) ;
#6096=VERTEX_POINT ( 'NONE', #37506 ) ;
#6104=CYLINDRICAL_SURFACE ( 'NONE', #24182, 2.999999999999994227 ) ;
#6105=ADVANCED_FACE ( 'NONE', ( #24650 ), #9223, .T. ) ;
#6128=CARTESIAN_POINT ( 'NONE',  ( 2.419685150592402856, -25.83699066625585417, -35.06583844469938072 ) ) ;
#6131=CARTESIAN_POINT ( 'NONE',  ( 45.86773870069588810, 6.907491052131607745, -60.98097754236641777 ) ) ;
#6143=EDGE_CURVE ( 'NONE', #51495, #11933, #14152, .T. ) ;
#6144=VECTOR ( 'NONE', #22449, 1000.000000000000227 ) ;
#6147=AXIS2_PLACEMENT_3D ( 'NONE', #5480, #9416, #37437 ) ;
#6151=ORIENTED_EDGE ( 'NONE', *, *, #37627, .T. ) ;
#6154=DIRECTION ( 'NONE',  ( 0.3535533905932738974, -0.6123724356957941373, 0.7071067811865477948 ) ) ;
#6156=CARTESIAN_POINT ( 'NONE',  ( 2.404741263826640107, -5.380232784273969671, -35.14999999999999858 ) ) ;
#6157=FACE_OUTER_BOUND ( 'NONE', #43264, .T. ) ;
#6175=CARTESIAN_POINT ( 'NONE',  ( 44.33333018168126216, 8.749049325578242886, -65.04467465255862635 ) ) ;
#6178=LINE ( 'NONE', #34454, #9231 ) ;
#6184=CARTESIAN_POINT ( 'NONE',  ( -22.74221626195645385, -18.63195909012526741, -54.69355302056131052 ) ) ;
#6185=CARTESIAN_POINT ( 'NONE',  ( -11.36606260230380094, -15.61618894467929941, -54.64999999999999858 ) ) ;
#6201=TOROIDAL_SURFACE ( 'NONE', #36286, 38.50000000000000000, 0.5000000000000000000 ) ;
#6208=CARTESIAN_POINT ( 'NONE',  ( 46.86113300846039920, 8.401293227643240158, -54.33266508569499820 ) ) ;
#6209=CARTESIAN_POINT ( 'NONE',  ( 8.643744238043749917, -48.75525398023999912, -35.14999999999999858 ) ) ;
#6210=VERTEX_POINT ( 'NONE', #2377 ) ;
#6211=LINE ( 'NONE', #47846, #13804 ) ;
#6212=AXIS2_PLACEMENT_3D ( 'NONE', #25483, #5600, #1917 ) ;
#6216=CYLINDRICAL_SURFACE ( 'NONE', #39764, 0.4999999999999967248 ) ;
#6221=EDGE_CURVE ( 'NONE', #30405, #20085, #18352, .T. ) ;
#6239=ORIENTED_EDGE ( 'NONE', *, *, #20506, .F. ) ;
#6245=ORIENTED_EDGE ( 'NONE', *, *, #24996, .F. ) ;
#6246=ORIENTED_EDGE ( 'NONE', *, *, #1104, .T. ) ;
#6247=CARTESIAN_POINT ( 'NONE',  ( -22.53151229193539962, -21.50213485567750027, -54.59180516875479583 ) ) ;
#6256=ORIENTED_EDGE ( 'NONE', *, *, #28990, .F. ) ;
#6265=EDGE_CURVE ( 'NONE', #35016, #11240, #31701, .T. ) ;
#6273=DIRECTION ( 'NONE',  ( 0.000000000000000000, 1.000000000000000000, 0.000000000000000000 ) ) ;
#6277=LINE ( 'NONE', #41651, #9180 ) ;
#6280=CARTESIAN_POINT ( 'NONE',  ( 0.3209249304026170480, -23.01378514180129997, -34.64999999999999858 ) ) ;
#6282=DIRECTION ( 'NONE',  ( -1.000000000000000000, 0.000000000000000000, 0.000000000000000000 ) ) ;
#6284=CARTESIAN_POINT ( 'NONE',  ( -18.22323072929020071, 2.939837993609400346, -50.61277379763759399 ) ) ;
#6286=CARTESIAN_POINT ( 'NONE',  ( 42.77811245501010262, -37.70056812138489732, -76.42740052126559647 ) ) ;
#6288=EDGE_CURVE ( 'NONE', #32498, #32056, #44263, .T. ) ;
#6309=CARTESIAN_POINT ( 'NONE',  ( 23.24148394091319858, 16.60930999848680401, -54.64999999999999858 ) ) ;
#6310=CARTESIAN_POINT ( 'NONE',  ( 14.13393739769640156, 6.292713355527309815, -54.64999999999999858 ) ) ;
#6312=ADVANCED_FACE ( 'NONE', ( #6575 ), #10512, .T. ) ;
#6315=ORIENTED_EDGE ( 'NONE', *, *, #17221, .T. ) ;
#6316=CIRCLE ( 'NONE', #13018, 0.5000000000000004441 ) ;
#6319=ORIENTED_EDGE ( 'NONE', *, *, #47508, .T. ) ;
#6320=DIRECTION ( 'NONE',  ( 0.000000000000000000, 0.000000000000000000, -1.000000000000000000 ) ) ;
#6326=CARTESIAN_POINT ( 'NONE',  ( -0.007164427059776000244, -27.04615419348650107, -34.77269723891829756 ) ) ;
#6330=CARTESIAN_POINT ( 'NONE',  ( 45.95646501821028806, -38.14902966602224410, -60.53732341105824588 ) ) ;
#6332=VERTEX_POINT ( 'NONE', #34595 ) ;
#6336=ADVANCED_FACE ( 'NONE', ( #18103 ), #41963, .T. ) ;
#6340=B_SPLINE_CURVE_WITH_KNOTS ( 'NONE', 3,
 ( #30871, #47155, #46898, #10988, #42958, #7056, #39027, #3122 ),
 .UNSPECIFIED., .F., .F.,
 ( 4, 2, 2, 4 ),
 ( -0.1329710036333066059, -0.1164701438935569905, -0.09932952752691590059, -0.09339196852977180163 ),
 .UNSPECIFIED. ) ;
#6342=CARTESIAN_POINT ( 'NONE',  ( 44.84924418339111440, -33.99486860111965569, -61.59306135713902108 ) ) ;
#6345=VERTEX_POINT ( 'NONE', #25690 ) ;
#6350=CARTESIAN_POINT ( 'NONE',  ( 42.04585206398351716, -39.76929823994083790, -76.11101280728998120 ) ) ;
#6354=CARTESIAN_POINT ( 'NONE',  ( 23.24148394091319858, 16.60930999848680401, -54.64999999999999858 ) ) ;
#6360=CARTESIAN_POINT ( 'NONE',  ( 16.13393739769620083, -15.61618894467929941, -54.64999999999999858 ) ) ;
#6368=CYLINDRICAL_SURFACE ( 'NONE', #51403, 0.4999999999999991118 ) ;
#6371=EDGE_CURVE ( 'NONE', #46602, #12186, #19974, .T. ) ;
#6376=EDGE_CURVE ( 'NONE', #41771, #11158, #46164, .T. ) ;
#6384=EDGE_CURVE ( 'NONE', #45182, #27942, #8268, .T. ) ;
#6385=DIRECTION ( 'NONE',  ( 0.000000000000000000, 0.7071067811865463515, -0.7071067811865487940 ) ) ;
#6390=CARTESIAN_POINT ( 'NONE',  ( 46.13676306618652490, 6.935121276559664594, -59.63581676699643452 ) ) ;
#6392=CARTESIAN_POINT ( 'NONE',  ( -11.00338044706756335, 12.40696740781548790, -44.69336853459499537 ) ) ;
#6395=CIRCLE ( 'NONE', #5570, 151.2593554377170051 ) ;
#6398=DIRECTION ( 'NONE',  ( 1.000000000000000000, 0.000000000000000000, 0.000000000000000000 ) ) ;
#6400=DIRECTION ( 'NONE',  ( 0.6522074047277899300, 0.2731766849828906607, 0.7071067811865471286 ) ) ;
#6403=EDGE_CURVE ( 'NONE', #45454, #611, #25639, .T. ) ;
#6417=DIRECTION ( 'NONE',  ( -0.3863301728269312174, 0.9223605572461961444, 0.000000000000000000 ) ) ;
#6423=DIRECTION ( 'NONE',  ( 0.000000000000000000, -0.7071067811865475727, 0.7071067811865475727 ) ) ;
#6436=CARTESIAN_POINT ( 'NONE',  ( 45.76614692253087924, 8.847677250480378675, -58.09469284861464189 ) ) ;
#6440=EDGE_CURVE ( 'NONE', #42352, #37266, #12462, .T. ) ;
#6447=CARTESIAN_POINT ( 'NONE',  ( -11.01912895885372379, -43.80691297044756283, -44.70832929457024107 ) ) ;
#6449=ORIENTED_EDGE ( 'NONE', *, *, #24701, .F. ) ;
#6450=VERTEX_POINT ( 'NONE', #23050 ) ;
#6451=DIRECTION ( 'NONE',  ( 0.8660254037844431485, 0.4999999999999921174, 0.000000000000000000 ) ) ;
#6460=CARTESIAN_POINT ( 'NONE',  ( 2.452285341914097305, -5.552263267694091731, -34.81767276520685073 ) ) ;
#6467=CARTESIAN_POINT ( 'NONE',  ( 46.72523890439229888, 8.574345336337970025, -54.52047978925480010 ) ) ;
#6472=CARTESIAN_POINT ( 'NONE',  ( 45.76880525768196861, -40.08018765987725374, -58.08188677919342524 ) ) ;
#6496=CARTESIAN_POINT ( 'NONE',  ( 16.13393739769620083, -15.61618894467929941, -84.65000000000000568 ) ) ;
#6499=ORIENTED_EDGE ( 'NONE', *, *, #37214, .T. ) ;
#6505=ORIENTED_EDGE ( 'NONE', *, *, #51156, .T. ) ;
#6517=PLANE ( 'NONE',  #17772 ) ;
#6521=EDGE_CURVE ( 'NONE', #45038, #50570, #24539, .T. ) ;
#6527=LINE ( 'NONE', #22489, #40211 ) ;
#6534=FACE_OUTER_BOUND ( 'NONE', #35123, .T. ) ;
#6536=CARTESIAN_POINT ( 'NONE',  ( -9.411761488291968902, 14.27370694945600071, -43.11785523033920242 ) ) ;
#6538=CARTESIAN_POINT ( 'NONE',  ( 45.56286034474006641, -39.21681118499099483, -62.73037012550634017 ) ) ;
#6542=ORIENTED_EDGE ( 'NONE', *, *, #37627, .F. ) ;
#6545=CARTESIAN_POINT ( 'NONE',  ( 46.82732515567090559, 9.047176644529985268, -52.37284531381663299 ) ) ;
#6550=CARTESIAN_POINT ( 'NONE',  ( 28.63604668330589931, -26.55449506982230190, -34.65000333679609668 ) ) ;
#6553=CARTESIAN_POINT ( 'NONE',  ( 15.19691430481782568, -43.84596607001308399, -60.51477253168710035 ) ) ;
#6563=EDGE_CURVE ( 'NONE', #40270, #5090, #32439, .T. ) ;
#6568=EDGE_CURVE ( 'NONE', #9565, #38690, #21180, .T. ) ;
#6571=VERTEX_POINT ( 'NONE', #40591 ) ;
#6573=CYLINDRICAL_SURFACE ( 'NONE', #23511, 0.4999999999999967248 ) ;
#6575=FACE_OUTER_BOUND ( 'NONE', #7737, .T. ) ;
#6578=ORIENTED_EDGE ( 'NONE', *, *, #30028, .T. ) ;
#6579=CYLINDRICAL_SURFACE ( 'NONE', #29960, 39.00000000000000711 ) ;
#6586=CARTESIAN_POINT ( 'NONE',  ( 44.68164263780834489, -38.00422853341399332, -66.91141490620562138 ) ) ;
#6587=ADVANCED_FACE ( 'NONE', ( #37187 ), #498, .T. ) ;
#6588=ORIENTED_EDGE ( 'NONE', *, *, #37815, .F. ) ;
#6597=VECTOR ( 'NONE', #49962, 999.9999999999998863 ) ;
#6598=ADVANCED_FACE ( 'NONE', ( #36921 ), #33236, .T. ) ;
#6605=CARTESIAN_POINT ( 'NONE',  ( 16.13393739769599833, 14.38381105532070059, -62.64999999999999858 ) ) ;
#6608=ORIENTED_EDGE ( 'NONE', *, *, #12294, .F. ) ;
#6613=CARTESIAN_POINT ( 'NONE',  ( 20.63393739769598767, 10.38381105532070414, -35.01561944896766931 ) ) ;
#6618=DIRECTION ( 'NONE',  ( 0.000000000000000000, 1.000000000000000000, 0.000000000000000000 ) ) ;
#6620=CYLINDRICAL_SURFACE ( 'NONE', #22946, 0.5000000000000006661 ) ;
#6621=EDGE_CURVE ( 'NONE', #4309, #5342, #23944, .T. ) ;
#6624=CARTESIAN_POINT ( 'NONE',  ( 18.13393739769639268, 10.38381105532070414, -35.01561944896763379 ) ) ;
#6632=VERTEX_POINT ( 'NONE', #4955 ) ;
#6633=ORIENTED_EDGE ( 'NONE', *, *, #12073, .F. ) ;
#6645=CARTESIAN_POINT ( 'NONE',  ( 46.79883821287099721, 6.999256669433407296, -56.32544524183283841 ) ) ;
#6650=CYLINDRICAL_SURFACE ( 'NONE', #25441, 0.4999999999999967248 ) ;
#6656=CARTESIAN_POINT ( 'NONE',  ( -0.007164378094141890356, 19.48649803870589992, -34.77269719633950018 ) ) ;
#6672=CONICAL_SURFACE ( 'NONE', #44290, 0.7350000000000010969, 0.06981317007977388966 ) ;
#6681=CARTESIAN_POINT ( 'NONE',  ( 10.03166977892449552, -53.91985561451862452, -34.73809820100212420 ) ) ;
#6682=FACE_OUTER_BOUND ( 'NONE', #11968, .T. ) ;
#6690=( BOUNDED_CURVE ( )  B_SPLINE_CURVE ( 3, ( #7353, #31682, #3426, #28017 ),
 .UNSPECIFIED., .F., .T. ) 
 B_SPLINE_CURVE_WITH_KNOTS ( ( 4, 4 ),
 ( 0.7853981633974506105, 1.570796326794898334 ),
 .UNSPECIFIED. ) 
 CURVE ( )  GEOMETRIC_REPRESENTATION_ITEM ( )  RATIONAL_B_SPLINE_CURVE ( ( 1.000000000000000000, 0.9492530216741912330, 0.9492530216741912330, 1.000000000000000000 ) ) 
 REPRESENTATION_ITEM ( '' )  );
#6711=CARTESIAN_POINT ( 'NONE',  ( -0.007164427059766999631, 19.48649803864789831, -34.77269723891829756 ) ) ;
#6715=CARTESIAN_POINT ( 'NONE',  ( 0.3209249304026170480, -46.25141913721060405, -34.64999999999999858 ) ) ;
#6735=CARTESIAN_POINT ( 'NONE',  ( 45.50949004153680733, -40.06418272001256042, -59.34096905993463622 ) ) ;
#6736=CARTESIAN_POINT ( 'NONE',  ( 16.13393739769620083, -15.61618894467929941, -81.65000000000000568 ) ) ;
#6749=AXIS2_PLACEMENT_3D ( 'NONE', #954, #16951, #41046 ) ;
#6758=DIRECTION ( 'NONE',  ( 0.000000000000000000, 0.000000000000000000, -1.000000000000000000 ) ) ;
#6759=EDGE_CURVE ( 'NONE', #19317, #51151, #23324, .T. ) ;
#6761=ORIENTED_EDGE ( 'NONE', *, *, #4784, .F. ) ;
#6764=VERTEX_POINT ( 'NONE', #44468 ) ;
#6766=CARTESIAN_POINT ( 'NONE',  ( 29.12893361417137328, -4.494242171482554227, -35.06842082984485387 ) ) ;
#6782=CARTESIAN_POINT ( 'NONE',  ( 14.13393739769649926, 18.32493655227499829, -34.64999999999999858 ) ) ;
#6791=AXIS2_PLACEMENT_3D ( 'NONE', #10995, #10217, #22244 ) ;
#6794=VECTOR ( 'NONE', #13155, 1000.000000000000000 ) ;
#6801=CARTESIAN_POINT ( 'NONE',  ( 8.942935310824880801, -49.33243882768289978, -34.64999999999999858 ) ) ;
#6802=DIRECTION ( 'NONE',  ( 0.1961161351381840445, 0.000000000000000000, 0.9805806756909201116 ) ) ;
#6803=FACE_OUTER_BOUND ( 'NONE', #33110, .T. ) ;
#6804=CARTESIAN_POINT ( 'NONE',  ( -21.98676283070069815, -6.896957895883470080, -53.98713251066509855 ) ) ;
#6806=CARTESIAN_POINT ( 'NONE',  ( -0.03447620312152738231, -22.81072779144790275, -34.79644660940672907 ) ) ;
#6807=DIRECTION ( 'NONE',  ( 0.000000000000000000, 0.000000000000000000, 1.000000000000000000 ) ) ;
#6810=ORIENTED_EDGE ( 'NONE', *, *, #42522, .F. ) ;
#6829=AXIS2_PLACEMENT_3D ( 'NONE', #26373, #42652, #2032 ) ;
#6843=CARTESIAN_POINT ( 'NONE',  ( 16.13393739769620083, -38.61618894467930119, -59.64999999999999147 ) ) ;
#6852=DIRECTION ( 'NONE',  ( 1.882763000000000063E-17, 1.367908000000000040E-17, -1.000000000000000000 ) ) ;
#6853=CARTESIAN_POINT ( 'NONE',  ( 46.52731067088307526, -38.20626701087121546, -57.68312601967695485 ) ) ;
#6854=VERTEX_POINT ( 'NONE', #38385 ) ;
#6856=CARTESIAN_POINT ( 'NONE',  ( -22.84939731388132245, -15.19272276721277493, -54.74980512766139640 ) ) ;
#6858=VECTOR ( 'NONE', #31378, 1000.000000000000114 ) ;
#6865=DIRECTION ( 'NONE',  ( 1.000000000000000000, 0.000000000000000000, 0.000000000000000000 ) ) ;
#6876=ORIENTED_EDGE ( 'NONE', *, *, #14, .T. ) ;
#6885=DIRECTION ( 'NONE',  ( 0.000000000000000000, 1.000000000000000000, 0.000000000000000000 ) ) ;
#6886=CARTESIAN_POINT ( 'NONE',  ( 13.10629489870503583, 18.33238584480843159, -34.89146800830128115 ) ) ;
#6889=EDGE_CURVE ( 'NONE', #51433, #12167, #42629, .T. ) ;
#6899=ORIENTED_EDGE ( 'NONE', *, *, #24996, .T. ) ;
#6902=ORIENTED_EDGE ( 'NONE', *, *, #28370, .T. ) ;
#6906=B_SPLINE_CURVE_WITH_KNOTS ( 'NONE', 3,
 ( #37916, #5439, #21394, #9874, #30292, #22163, #45265, #6467, #38175, #38428, #2531, #37397, #6208, #49468, #34482, #9621, #25577, #2269, #18243 ),
 .UNSPECIFIED., .F., .F.,
 ( 4, 3, 3, 3, 3, 3, 4 ),
 ( 1.000000950999999910E-06, 0.01506370868781899824, 0.03155346947011499620, 0.06469334631533249502, 0.07088861345938199388, 0.1184795979030530133, 0.1410854872666899851 ),
 .UNSPECIFIED. ) ;
#6911=CARTESIAN_POINT ( 'NONE',  ( 42.79442115924850754, 6.514747503090039693, -76.34753345981675920 ) ) ;
#6913=EDGE_LOOP ( 'NONE', ( #13468, #38932, #41012, #1916 ) ) ;
#6934=CARTESIAN_POINT ( 'NONE',  ( -1.839728563314010135, -2.929686987007059873, -54.64999999999999858 ) ) ;
#6937=CIRCLE ( 'NONE', #46261, 2.999999999999999112 ) ;
#6946=DIRECTION ( 'NONE',  ( 0.3863301728269249447, 0.9223605572461988089, -3.330669073875469621E-16 ) ) ;
#6954=CARTESIAN_POINT ( 'NONE',  ( 44.12711257345860361, 1.883811055320659955, -54.38706558040959749 ) ) ;
#6961=VECTOR ( 'NONE', #3181, 1000.000000000000114 ) ;
#6963=LINE ( 'NONE', #7217, #21844 ) ;
#6970=CARTESIAN_POINT ( 'NONE',  ( 45.22176751739600320, -33.50786583678460318, -34.76635026929679384 ) ) ;
#6973=CARTESIAN_POINT ( 'NONE',  ( 41.61626771661330082, 6.328436186825659782, -82.23834840541459812 ) ) ;
#6974=AXIS2_PLACEMENT_3D ( 'NONE', #11491, #44214, #23497 ) ;
#6992=CARTESIAN_POINT ( 'NONE',  ( 44.63094208885492975, -40.00404795335505526, -63.60229216252963624 ) ) ;
#6996=CARTESIAN_POINT ( 'NONE',  ( 0.9655226856871633734, -38.79346329613591138, -84.65000000000000568 ) ) ;
#6999=CARTESIAN_POINT ( 'NONE',  ( -15.32468133715470238, -15.61618894467930296, -84.65000000000000568 ) ) ;
#7010=CARTESIAN_POINT ( 'NONE',  ( 0.1457840918194806823, -20.72567761198500591, -34.68167776469320529 ) ) ;
#7011=CARTESIAN_POINT ( 'NONE',  ( 13.13393739769619906, -49.61618894467939356, -34.64999999999999858 ) ) ;
#7012=CARTESIAN_POINT ( 'NONE',  ( 38.67452568954060155, 4.883811055320659733, -81.65000000000000568 ) ) ;
#7013=CARTESIAN_POINT ( 'NONE',  ( 44.50508471174445191, -33.13860886180549414, -47.72927995595490813 ) ) ;
#7016=DIRECTION ( 'NONE',  ( 0.6339889056055360017, 0.000000000000000000, -0.7733421413379041320 ) ) ;
#7022=DIRECTION ( 'NONE',  ( 1.000000000000000000, 0.000000000000000000, 0.000000000000000000 ) ) ;
#7026=EDGE_CURVE ( 'NONE', #21662, #32183, #49337, .T. ) ;
#7027=VERTEX_POINT ( 'NONE', #43102 ) ;
#7035=DIRECTION ( 'NONE',  ( 0.000000000000000000, 0.000000000000000000, -1.000000000000000000 ) ) ;
#7036=VERTEX_POINT ( 'NONE', #50953 ) ;
#7038=CARTESIAN_POINT ( 'NONE',  ( 18.13393739769639978, 10.38381105532070059, -54.64999999999999858 ) ) ;
#7051=CARTESIAN_POINT ( 'NONE',  ( 47.02248099559329120, -39.42604202605379982, -54.03776557770559208 ) ) ;
#7056=CARTESIAN_POINT ( 'NONE',  ( 23.62216879347590037, 17.52774233096729617, -35.08633291502829366 ) ) ;
#7063=CARTESIAN_POINT ( 'NONE',  ( 0.1368909795571799926, 19.95311627097120066, -35.13391829916529474 ) ) ;
#7064=CARTESIAN_POINT ( 'NONE',  ( 47.13393739769619373, 7.029298498933709283, -54.64999999999999858 ) ) ;
#7067=DIRECTION ( 'NONE',  ( 0.000000000000000000, 1.000000000000000000, 0.000000000000000000 ) ) ;
#7072=CARTESIAN_POINT ( 'NONE',  ( 43.22292296461858285, 6.401212194726233484, -74.17814224749000118 ) ) ;
#7079=CARTESIAN_POINT ( 'NONE',  ( 16.13393739769620083, -45.61618894467940066, -62.64999999999999858 ) ) ;
#7098=EDGE_LOOP ( 'NONE', ( #36795, #43419, #32828, #33409 ) ) ;
#7108=CARTESIAN_POINT ( 'NONE',  ( 17.68664282411100075, -32.20606442350149479, -34.65032322548079691 ) ) ;
#7112=CARTESIAN_POINT ( 'NONE',  ( 46.71367998675990663, -38.22377110652077192, -56.75123991735566165 ) ) ;
#7117=FACE_OUTER_BOUND ( 'NONE', #16500, .T. ) ;
#7122=CARTESIAN_POINT ( 'NONE',  ( 0.08551642312347559893, 14.63024707446910000, -34.70586877331279396 ) ) ;
#7123=CARTESIAN_POINT ( 'NONE',  ( 9.976573729570530347, 22.56200410046550076, -34.67842804303189297 ) ) ;
#7141=FACE_OUTER_BOUND ( 'NONE', #18349, .T. ) ;
#7158=EDGE_CURVE ( 'NONE', #30658, #5655, #45103, .T. ) ;
#7161=ORIENTED_EDGE ( 'NONE', *, *, #28309, .T. ) ;
#7164=ORIENTED_EDGE ( 'NONE', *, *, #12526, .F. ) ;
#7165=CARTESIAN_POINT ( 'NONE',  ( 42.82578949616635100, 6.519398624929172215, -76.19070175595297201 ) ) ;
#7169=CARTESIAN_POINT ( 'NONE',  ( 16.13393739769620083, -38.61618894467930119, -59.64999999999999147 ) ) ;
#7182=VERTEX_POINT ( 'NONE', #351 ) ;
#7198=DIRECTION ( 'NONE',  ( 0.04100182651872441575, 0.05643417272666774454, -0.9975640502598241977 ) ) ;
#7208=CIRCLE ( 'NONE', #24745, 2.999999999999998224 ) ;
#7213=CIRCLE ( 'NONE', #29808, 0.4906046190927097483 ) ;
#7217=CARTESIAN_POINT ( 'NONE',  ( -0.2444979013989767025, -31.15369398163246473, 4.943674098299959851 ) ) ;
#7223=ADVANCED_FACE ( 'NONE', ( #12159 ), #8481, .T. ) ;
#7228=CYLINDRICAL_SURFACE ( 'NONE', #32629, 0.4999999999999982236 ) ;
#7247=CARTESIAN_POINT ( 'NONE',  ( 44.40914995519487007, -39.98739809836357040, -64.67686260219700500 ) ) ;
#7263=CARTESIAN_POINT ( 'NONE',  ( 0.2589946642435042579, -20.70800519868845413, -34.65038329361674130 ) ) ;
#7266=CARTESIAN_POINT ( 'NONE',  ( -0.007164427059776000244, -10.48291004383190028, -34.77269723891829756 ) ) ;
#7271=VERTEX_POINT ( 'NONE', #37291 ) ;
#7281=EDGE_CURVE ( 'NONE', #8293, #16490, #21030, .T. ) ;
#7292=FACE_OUTER_BOUND ( 'NONE', #30113, .T. ) ;
#7296=ADVANCED_FACE ( 'NONE', ( #17639 ), #6104, .T. ) ;
#7300=( BOUNDED_CURVE ( )  B_SPLINE_CURVE ( 3, ( #48154, #4386, #20612, #19599 ),
 .UNSPECIFIED., .F., .T. ) 
 B_SPLINE_CURVE_WITH_KNOTS ( ( 4, 4 ),
 ( 1.125870930210365994, 1.195525503939052436 ),
 .UNSPECIFIED. ) 
 CURVE ( )  GEOMETRIC_REPRESENTATION_ITEM ( )  RATIONAL_B_SPLINE_CURVE ( ( 1.000000000000000000, 0.9995957275622157079, 0.9995957275622157079, 1.000000000000000000 ) ) 
 REPRESENTATION_ITEM ( '' )  );
#7307=B_SPLINE_CURVE_WITH_KNOTS ( 'NONE', 3,
 ( #49839, #29889, #33828, #1360, #45908, #13680 ),
 .UNSPECIFIED., .F., .F.,
 ( 4, 2, 4 ),
 ( 0.01784182840660334182, 0.02050618711215480144, 0.03595209231937170069 ),
 .UNSPECIFIED. ) ;
#7308=CARTESIAN_POINT ( 'NONE',  ( 0.1457840807894888180, 19.59951024407514097, -34.68167773519660813 ) ) ;
#7311=CONICAL_SURFACE ( 'NONE', #48305, 19.50000000000000000, 0.2449786631268651149 ) ;
#7325=CARTESIAN_POINT ( 'NONE',  ( 47.10325001712173076, 6.750336882473666478, -54.73793454088935562 ) ) ;
#7332=FACE_OUTER_BOUND ( 'NONE', #47437, .T. ) ;
#7337=CYLINDRICAL_SURFACE ( 'NONE', #25325, 0.4999999999999982236 ) ;
#7345=CARTESIAN_POINT ( 'NONE',  ( 44.09915591415798275, -33.11626185954118284, -54.64999999999999858 ) ) ;
#7348=ORIENTED_EDGE ( 'NONE', *, *, #20746, .F. ) ;
#7349=CARTESIAN_POINT ( 'NONE',  ( 23.62216879347609932, -48.76012022032579551, -35.08633291502829366 ) ) ;
#7353=CARTESIAN_POINT ( 'NONE',  ( 46.25525774125583922, -33.99486860111965569, -54.56299356781535437 ) ) ;
#7355=PLANE ( 'NONE',  #9265 ) ;
#7357=DIRECTION ( 'NONE',  ( 0.000000000000000000, 0.000000000000000000, 1.000000000000000000 ) ) ;
#7362=AXIS2_PLACEMENT_3D ( 'NONE', #23404, #3261, #16079 ) ;
#7363=ORIENTED_EDGE ( 'NONE', *, *, #13127, .T. ) ;
#7376=ADVANCED_FACE ( 'NONE', ( #17377 ), #29416, .T. ) ;
#7379=CARTESIAN_POINT ( 'NONE',  ( 31.38963856960426568, -35.88105874546273100, -84.64183929351709423 ) ) ;
#7381=CARTESIAN_POINT ( 'NONE',  ( 22.37318698975080267, 22.37488585622680048, -34.64999999999999858 ) ) ;
#7382=CARTESIAN_POINT ( 'NONE',  ( -6.866062602303790285, -15.61618894467929941, 4.943674098299959851 ) ) ;
#7384=EDGE_LOOP ( 'NONE', ( #175, #37628, #45756, #11939, #182, #24992 ) ) ;
#7399=CARTESIAN_POINT ( 'NONE',  ( -22.60067283610179700, -11.07416626356550005, -54.64998264227110525 ) ) ;
#7400=DIRECTION ( 'NONE',  ( 0.000000000000000000, 1.000000000000000000, 0.000000000000000000 ) ) ;
#7408=ORIENTED_EDGE ( 'NONE', *, *, #12361, .T. ) ;
#7415=CARTESIAN_POINT ( 'NONE',  ( 0.8044204053651899944, -8.725579796100580765, -34.68801049095939959 ) ) ;
#7416=CARTESIAN_POINT ( 'NONE',  ( 0.03808610503982447909, -4.264599916538029944, -34.73334895013598356 ) ) ;
#7419=CARTESIAN_POINT ( 'NONE',  ( 42.69833145473944569, 6.500458167497354722, -76.82796414980892052 ) ) ;
#7423=DIRECTION ( 'NONE',  ( -6.580805000000000321E-18, -4.248364000000000300E-18, 1.000000000000000000 ) ) ;
#7429=CARTESIAN_POINT ( 'NONE',  ( -1.143840380081599717, -17.22304274993012285, -35.76111111111112706 ) ) ;
#7430=VECTOR ( 'NONE', #27644, 1000.000000000000000 ) ;
#7436=DIRECTION ( 'NONE',  ( 0.000000000000000000, 0.000000000000000000, -1.000000000000000000 ) ) ;
#7454=CYLINDRICAL_SURFACE ( 'NONE', #21435, 2.999999999999999112 ) ;
#7466=CARTESIAN_POINT ( 'NONE',  ( 45.73288634929132002, 8.845650597630955403, -58.25629762057298677 ) ) ;
#7467=VECTOR ( 'NONE', #21244, 1000.000000000000000 ) ;
#7469=ORIENTED_EDGE ( 'NONE', *, *, #40241, .F. ) ;
#7470=EDGE_CURVE ( 'NONE', #8281, #23002, #7591, .T. ) ;
#7473=CONICAL_SURFACE ( 'NONE', #42635, 0.7349999999999987654, 0.06981317007977388966 ) ;
#7476=FACE_OUTER_BOUND ( 'NONE', #48592, .T. ) ;
#7484=ORIENTED_EDGE ( 'NONE', *, *, #14510, .T. ) ;
#7493=CARTESIAN_POINT ( 'NONE',  ( -0.1295185695942999982, 0.6472670226113349523, -59.64999999999999147 ) ) ;
#7494=LINE ( 'NONE', #18762, #41478 ) ;
#7495=CIRCLE ( 'NONE', #30933, 34.47562460986249988 ) ;
#7500=ADVANCED_FACE ( 'NONE', ( #44772 ), #2478, .F. ) ;
#7503=CARTESIAN_POINT ( 'NONE',  ( 45.27541171706066336, -40.04939379810706157, -60.47585066460795389 ) ) ;
#7507=PRESENTATION_STYLE_ASSIGNMENT (( #3578 ) ) ;
#7510=DIRECTION ( 'NONE',  ( -0.06889765579810419593, -0.01091231665325485128, -0.9975640502598241977 ) ) ;
#7518=DIRECTION ( 'NONE',  ( 0.000000000000000000, 0.000000000000000000, -1.000000000000000000 ) ) ;
#7525=DIRECTION ( 'NONE',  ( 0.000000000000000000, 0.000000000000000000, -1.000000000000000000 ) ) ;
#7528=VERTEX_POINT ( 'NONE', #17760 ) ;
#7529=CARTESIAN_POINT ( 'NONE',  ( 0.08375394646315241498, 19.63944928676770019, -34.70982966457259522 ) ) ;
#7530=ORIENTED_EDGE ( 'NONE', *, *, #2016, .F. ) ;
#7535=CARTESIAN_POINT ( 'NONE',  ( 16.13393739769620083, -15.61618894467929941, -44.64999999999999858 ) ) ;
#7543=CARTESIAN_POINT ( 'NONE',  ( -20.42916145723442867, -2.043494675895988877, -52.78588572598070527 ) ) ;
#7548=DIRECTION ( 'NONE',  ( 0.2201775510703259942, -0.9741807197500960136, 0.04993767387313000072 ) ) ;
#7554=EDGE_CURVE ( 'NONE', #26020, #50974, #8876, .T. ) ;
#7562=DIRECTION ( 'NONE',  ( 0.000000000000000000, 0.000000000000000000, -1.000000000000000000 ) ) ;
#7563=ORIENTED_EDGE ( 'NONE', *, *, #34363, .T. ) ;
#7571=DIRECTION ( 'NONE',  ( -0.3863301728269232238, -0.9223605572461994750, 0.000000000000000000 ) ) ;
#7583=VERTEX_POINT ( 'NONE', #1523 ) ;
#7585=ORIENTED_EDGE ( 'NONE', *, *, #44852, .T. ) ;
#7586=CARTESIAN_POINT ( 'NONE',  ( 47.11598513326693904, 6.751028634652659122, -54.67405396673499496 ) ) ;
#7591=LINE ( 'NONE', #31916, #14195 ) ;
#7598=ORIENTED_EDGE ( 'NONE', *, *, #48823, .F. ) ;
#7610=CARTESIAN_POINT ( 'NONE',  ( 23.62400244246340009, -48.75656286698960429, -35.12503119152809461 ) ) ;
#7614=( BOUNDED_CURVE ( )  B_SPLINE_CURVE ( 3, ( #3519, #4028, #7712, #16073 ),
 .UNSPECIFIED., .F., .T. ) 
 B_SPLINE_CURVE_WITH_KNOTS ( ( 4, 4 ),
 ( 5.087659803240767609, 5.157314376969199365 ),
 .UNSPECIFIED. ) 
 CURVE ( )  GEOMETRIC_REPRESENTATION_ITEM ( )  RATIONAL_B_SPLINE_CURVE ( ( 1.000000000000000000, 0.9995957275622187055, 0.9995957275622187055, 1.000000000000000000 ) ) 
 REPRESENTATION_ITEM ( '' )  );
#7629=CARTESIAN_POINT ( 'NONE',  ( 13.00414154252451659, -49.37472093637801862, -34.70142521051216988 ) ) ;
#7633=CARTESIAN_POINT ( 'NONE',  ( 10.03166977892496625, 22.68747772516197259, -34.73809820100316870 ) ) ;
#7637=EDGE_CURVE ( 'NONE', #5655, #36176, #50262, .T. ) ;
#7644=CARTESIAN_POINT ( 'NONE',  ( 20.38275687770202538, 4.296863009278949264, -59.64999999999999147 ) ) ;
#7653=AXIS2_PLACEMENT_3D ( 'NONE', #37433, #34520, #38467 ) ;
#7657=CARTESIAN_POINT ( 'NONE',  ( 0.3209249304026170480, -15.61618894467929941, -35.14999999999999858 ) ) ;
#7666=CARTESIAN_POINT ( 'NONE',  ( 16.13393739769620083, -1.759782484128323166, -35.01561944896766221 ) ) ;
#7670=ORIENTED_EDGE ( 'NONE', *, *, #19714, .T. ) ;
#7673=CARTESIAN_POINT ( 'NONE',  ( -0.007164427059776000244, -45.70803162167019451, -34.77269723891829756 ) ) ;
#7674=ORIENTED_EDGE ( 'NONE', *, *, #20221, .T. ) ;
#7680=CARTESIAN_POINT ( 'NONE',  ( 43.34489039530834020, 6.595245306295674403, -73.59517026744862278 ) ) ;
#7688=EDGE_CURVE ( 'NONE', #49694, #9565, #47412, .T. ) ;
#7691=CARTESIAN_POINT ( 'NONE',  ( 16.13393739769639623, 7.383811055320659733, -59.64999999999999147 ) ) ;
#7700=CARTESIAN_POINT ( 'NONE',  ( 16.13393739769620083, -15.61618894467929941, -54.64999999999999858 ) ) ;
#7712=CARTESIAN_POINT ( 'NONE',  ( -0.01592648613897638260, -4.171047364367892030, -34.78031642072625829 ) ) ;
#7713=CARTESIAN_POINT ( 'NONE',  ( 18.15116866486563652, 18.38379944632345797, -83.15271738017148095 ) ) ;
#7725=CARTESIAN_POINT ( 'NONE',  ( 46.98749101202549383, 7.998570365497442936, -34.79644638567071269 ) ) ;
#7737=EDGE_LOOP ( 'NONE', ( #9125, #31180, #17663, #49723, #46222 ) ) ;
#7740=CARTESIAN_POINT ( 'NONE',  ( -11.54263325867530199, -34.48402086119780563, -44.80353970119273299 ) ) ;
#7746=CARTESIAN_POINT ( 'NONE',  ( 45.15010597285510130, -33.29644663991430065, -35.08262351468650309 ) ) ;
#7747=VERTEX_POINT ( 'NONE', #46339 ) ;
#7750=DIRECTION ( 'NONE',  ( 0.8660254037844387076, 0.4999999999999998890, 2.775557561562889194E-17 ) ) ;
#7762=CARTESIAN_POINT ( 'NONE',  ( 11.63245656708829756, -51.88627667935560339, -69.46507341766636046 ) ) ;
#7765=CARTESIAN_POINT ( 'NONE',  ( 42.62445565279771387, -39.82941498042225703, -73.31524913290161294 ) ) ;
#7781=CARTESIAN_POINT ( 'NONE',  ( 41.83358903174870846, 8.514088802998820427, -77.13456888834446090 ) ) ;
#7782=CARTESIAN_POINT ( 'NONE',  ( 16.13393739769620083, -45.61618894467940066, -35.14999999999999858 ) ) ;
#7783=CARTESIAN_POINT ( 'NONE',  ( 30.96406434931616403, 4.463581150976708933, -84.62099912964093562 ) ) ;
#7786=CARTESIAN_POINT ( 'NONE',  ( 0.1155610841158959956, 19.94237700917059897, -35.14999985728680088 ) ) ;
#7787=EDGE_LOOP ( 'NONE', ( #45604, #28330 ) ) ;
#7789=CARTESIAN_POINT ( 'NONE',  ( -1.224559824875987468, -24.96582652780387690, -84.65000000000000568 ) ) ;
#7790=CARTESIAN_POINT ( 'NONE',  ( 29.13393466042959901, -4.484470077231426544, -35.10904485683914800 ) ) ;
#7794=AXIS2_PLACEMENT_3D ( 'NONE', #28805, #12847, #19473 ) ;
#7795=ORIENTED_EDGE ( 'NONE', *, *, #16365, .T. ) ;
#7799=EDGE_CURVE ( 'NONE', #14157, #20336, #50750, .T. ) ;
#7805=CARTESIAN_POINT ( 'NONE',  ( 46.63393739769619373, -39.11086919362080039, -34.64999999999999858 ) ) ;
#7818=CARTESIAN_POINT ( 'NONE',  ( -0.03447620312152738231, -22.81072779144790275, -34.79644660940672907 ) ) ;
#7828=AXIS2_PLACEMENT_3D ( 'NONE', #16817, #35703, #43824 ) ;
#7831=CARTESIAN_POINT ( 'NONE',  ( -6.866062602303809825, -22.61618894467929763, -59.64999999999999147 ) ) ;
#7838=EDGE_LOOP ( 'NONE', ( #440, #14884, #5152, #24851, #5415 ) ) ;
#7839=CARTESIAN_POINT ( 'NONE',  ( 42.60159069889220262, 7.610747875504726423, -77.64264605067509706 ) ) ;
#7840=CARTESIAN_POINT ( 'NONE',  ( 4.133937397696209715, -22.54439217495480108, -47.64999999999999858 ) ) ;
#7847=CIRCLE ( 'NONE', #40459, 1.999999999999998224 ) ;
#7848=ORIENTED_EDGE ( 'NONE', *, *, #28958, .T. ) ;
#7854=CARTESIAN_POINT ( 'NONE',  ( 11.63393739769619906, -41.61618894467930119, -34.64999999999999858 ) ) ;
#7872=CARTESIAN_POINT ( 'NONE',  ( 0.3209249304026220440, -50.71887597443840434, -34.64999999999999858 ) ) ;
#7874=ADVANCED_FACE ( 'NONE', ( #24178 ), #20262, .T. ) ;
#7877=CARTESIAN_POINT ( 'NONE',  ( 46.06102281558538891, -38.15968466400891401, -60.01451776560848117 ) ) ;
#7895=DIRECTION ( 'NONE',  ( 0.5835456732599411112, 0.8120803206700689669, 0.000000000000000000 ) ) ;
#7905=CARTESIAN_POINT ( 'NONE',  ( 0.1457841021255935343, -4.451138319363987073, -34.68167779225149161 ) ) ;
#7906=CARTESIAN_POINT ( 'NONE',  ( -0.3963262347861145618, -45.30092459685357653, -35.11109881085425144 ) ) ;
#7911=( BOUNDED_CURVE ( )  B_SPLINE_CURVE ( 3, ( #4546, #45164, #41489, #9278 ),
 .UNSPECIFIED., .F., .T. ) 
 B_SPLINE_CURVE_WITH_KNOTS ( ( 4, 4 ),
 ( 0.7853981633974360665, 1.570796326794899000 ),
 .UNSPECIFIED. ) 
 CURVE ( )  GEOMETRIC_REPRESENTATION_ITEM ( )  RATIONAL_B_SPLINE_CURVE ( ( 1.000000000000000000, 0.9492530216741892346, 0.9492530216741892346, 1.000000000000000000 ) ) 
 REPRESENTATION_ITEM ( '' )  );
#7917=DIRECTION ( 'NONE',  ( 8.462868000000000073E-18, -1.066343000000000058E-17, 1.000000000000000000 ) ) ;
#7920=ORIENTED_EDGE ( 'NONE', *, *, #30685, .T. ) ;
#7931=CARTESIAN_POINT ( 'NONE',  ( 44.38457061139609294, 6.734955052058427150, -68.39683385616302758 ) ) ;
#7933=EDGE_CURVE ( 'NONE', #9877, #5342, #43808, .T. ) ;
#7951=B_SPLINE_CURVE_WITH_KNOTS ( 'NONE', 3,
 ( #24134, #8452, #32510, #4505, #11615, #20475, #27580, #36466, #28085, #78, #12127, #24659, #44090, #12377 ),
 .UNSPECIFIED., .F., .F.,
 ( 4, 2, 2, 2, 2, 2, 4 ),
 ( -0.2176222735790200036, -0.2170920924270339780, -0.1934197942039800056, -0.1709809187548010090, -0.1448153107580100185, -0.1239068615272080065, -0.1078515919262239969 ),
 .UNSPECIFIED. ) ;
#7957=ADVANCED_FACE ( 'NONE', ( #28904 ), #40451, .T. ) ;
#7965=LINE ( 'NONE', #36247, #51571 ) ;
#7966=ADVANCED_FACE ( 'NONE', ( #8748 ), #46370, .T. ) ;
#7969=EDGE_CURVE ( 'NONE', #32053, #51550, #26980, .T. ) ;
#7971=CARTESIAN_POINT ( 'NONE',  ( 47.13393739769619373, 8.048130187719140238, -35.08812023096459853 ) ) ;
#7974=CARTESIAN_POINT ( 'NONE',  ( 22.13834065091210235, -54.14192202099170004, -35.04035092416999220 ) ) ;
#7979=VERTEX_POINT ( 'NONE', #32300 ) ;
#7986=EDGE_CURVE ( 'NONE', #46545, #677, #8228, .T. ) ;
#7991=CARTESIAN_POINT ( 'NONE',  ( 15.53930990683061353, -38.18416678424433286, 4.943674098299959851 ) ) ;
#7994=CARTESIAN_POINT ( 'NONE',  ( 44.67095740009779803, 1.932267065267109896, -44.63214371738488495 ) ) ;
#8000=CARTESIAN_POINT ( 'NONE',  ( 0.9261640637186691061, -22.54594764139109841, -34.65800258959599489 ) ) ;
#8010=CARTESIAN_POINT ( 'NONE',  ( 43.33491147696511092, -39.89712550726049756, -69.87957685626012960 ) ) ;
#8022=EDGE_LOOP ( 'NONE', ( #27028, #49122, #2074, #50350 ) ) ;
#8024=LINE ( 'NONE', #12471, #25733 ) ;
#8030=CARTESIAN_POINT ( 'NONE',  ( 42.48761169368059853, 8.583421331073370908, -73.97586456252511766 ) ) ;
#8050=CARTESIAN_POINT ( 'NONE',  ( -22.40773940430613109, -9.428819728254625332, -54.48440151228250983 ) ) ;
#8057=( BOUNDED_CURVE ( )  B_SPLINE_CURVE ( 2, ( #3030, #14823, #27127 ),
 .UNSPECIFIED., .F., .T. ) 
 B_SPLINE_CURVE_WITH_KNOTS ( ( 3, 3 ),
 ( 1.923142637343010053, 4.853851569643779840 ),
 .UNSPECIFIED. ) 
 CURVE ( )  GEOMETRIC_REPRESENTATION_ITEM ( )  RATIONAL_B_SPLINE_CURVE ( ( 1.003436844930060134, 1.004455541115540029, 1.000597593688330011 ) ) 
 REPRESENTATION_ITEM ( '' )  );
#8063=CIRCLE ( 'NONE', #13892, 5.461610137242769447 ) ;
#8071=LINE ( 'NONE', #24016, #37981 ) ;
#8095=CARTESIAN_POINT ( 'NONE',  ( 41.63907510861591987, 6.190619291336893149, -82.10713965745907217 ) ) ;
#8105=ORIENTED_EDGE ( 'NONE', *, *, #4960, .F. ) ;
#8114=ORIENTED_EDGE ( 'NONE', *, *, #49145, .F. ) ;
#8126=CARTESIAN_POINT ( 'NONE',  ( 10.13393739769589885, 22.91950879131600161, -35.09469305598949518 ) ) ;
#8127=AXIS2_PLACEMENT_3D ( 'NONE', #28885, #24937, #29408 ) ;
#8129=CARTESIAN_POINT ( 'NONE',  ( 2.434269054290299827, -25.76645817901039948, -34.90839531524130024 ) ) ;
#8132=CARTESIAN_POINT ( 'NONE',  ( 16.13393739769620083, -15.61618894467929941, -54.64999999999999858 ) ) ;
#8133=ORIENTED_EDGE ( 'NONE', *, *, #6143, .F. ) ;
#8147=FACE_OUTER_BOUND ( 'NONE', #29085, .T. ) ;
#8152=ADVANCED_FACE ( 'NONE', ( #1398 ), #21816, .T. ) ;
#8155=ADVANCED_FACE ( 'NONE', ( #9276 ), #6368, .T. ) ;
#8160=EDGE_CURVE ( 'NONE', #51641, #18232, #25224, .T. ) ;
#8172=CARTESIAN_POINT ( 'NONE',  ( 2.543036500622910090, -25.25580902796040306, -34.65032322548090349 ) ) ;
#8174=AXIS2_PLACEMENT_3D ( 'NONE', #49697, #49953, #21621 ) ;
#8185=CARTESIAN_POINT ( 'NONE',  ( 0.3209249304026170480, -15.61618894467929941, -35.14999999999999858 ) ) ;
#8188=CARTESIAN_POINT ( 'NONE',  ( 42.51832970315865623, 6.473372013560068083, -77.72799465092199966 ) ) ;
#8225=CARTESIAN_POINT ( 'NONE',  ( 23.32430482491550094, 18.10127401595489971, -34.64999999999999858 ) ) ;
#8228=LINE ( 'NONE', #51290, #30432 ) ;
#8229=CARTESIAN_POINT ( 'NONE',  ( 22.13393739769619728, -54.15188668067469990, -35.14999999999999858 ) ) ;
#8235=VERTEX_POINT ( 'NONE', #27235 ) ;
#8245=CARTESIAN_POINT ( 'NONE',  ( -11.39236625349550103, 2.585530954890270294, -54.64999999999999858 ) ) ;
#8246=ORIENTED_EDGE ( 'NONE', *, *, #28302, .F. ) ;
#8247=ORIENTED_EDGE ( 'NONE', *, *, #45330, .T. ) ;
#8251=EDGE_CURVE ( 'NONE', #24679, #19168, #22782, .T. ) ;
#8256=DIRECTION ( 'NONE',  ( -0.7071067811865510144, -0.7071067811865440200, 0.000000000000000000 ) ) ;
#8260=CARTESIAN_POINT ( 'NONE',  ( 16.13393739769620083, -15.61618894467929941, -643.2998782751060389 ) ) ;
#8264=CARTESIAN_POINT ( 'NONE',  ( 42.84502392579520347, -39.85101499308053263, -72.24970805093310844 ) ) ;
#8268=CIRCLE ( 'NONE', #38429, 38.50000000000001421 ) ;
#8273=CIRCLE ( 'NONE', #15842, 3.000000000000004885 ) ;
#8281=VERTEX_POINT ( 'NONE', #26458 ) ;
#8286=CARTESIAN_POINT ( 'NONE',  ( 41.14166300954741473, 8.434767834753492011, -80.47192884955046566 ) ) ;
#8288=CARTESIAN_POINT ( 'NONE',  ( 29.69570898453723728, 4.415807149541521426, -84.61328641085442825 ) ) ;
#8293=VERTEX_POINT ( 'NONE', #10502 ) ;
#8294=ORIENTED_EDGE ( 'NONE', *, *, #48028, .T. ) ;
#8307=ORIENTED_EDGE ( 'NONE', *, *, #28773, .F. ) ;
#8319=CARTESIAN_POINT ( 'NONE',  ( -22.62717218277616738, -11.30032500101179238, -54.65011942300672132 ) ) ;
#8320=LINE ( 'NONE', #972, #29325 ) ;
#8355=VECTOR ( 'NONE', #16731, 1000.000000000000114 ) ;
#8376=DIRECTION ( 'NONE',  ( 0.5516667872527449834, 0.8340645993220396903, 2.775557561562889194E-17 ) ) ;
#8377=FACE_OUTER_BOUND ( 'NONE', #35207, .T. ) ;
#8388=ORIENTED_EDGE ( 'NONE', *, *, #51070, .F. ) ;
#8389=VECTOR ( 'NONE', #28470, 1000.000000000000000 ) ;
#8393=CARTESIAN_POINT ( 'NONE',  ( 11.73137203405248385, 10.53025766472752522, -34.79644660940672907 ) ) ;
#8397=FACE_OUTER_BOUND ( 'NONE', #16278, .T. ) ;
#8405=CARTESIAN_POINT ( 'NONE',  ( 42.40177580631258536, -39.88217762379048281, -74.07840177966397732 ) ) ;
#8406=B_SPLINE_CURVE_WITH_KNOTS ( 'NONE', 3,
 ( #14212, #11322, #43037, #6354 ),
 .UNSPECIFIED., .F., .F.,
 ( 4, 4 ),
 ( 0.4931821396943200098, 20.02578215755499969 ),
 .UNSPECIFIED. ) ;
#8408=ADVANCED_FACE ( 'NONE', ( #49156 ), #13253, .T. ) ;
#8434=TOROIDAL_SURFACE ( 'NONE', #37717, 38.50000000000000000, 0.5000000000000000000 ) ;
#8435=VECTOR ( 'NONE', #22218, 1000.000000000000000 ) ;
#8438=ORIENTED_EDGE ( 'NONE', *, *, #13849, .T. ) ;
#8442=ORIENTED_EDGE ( 'NONE', *, *, #26884, .T. ) ;
#8443=DIRECTION ( 'NONE',  ( 0.6933752452815367118, 0.7071067811865475727, -0.1386750490563054827 ) ) ;
#8444=CARTESIAN_POINT ( 'NONE',  ( 22.13393739769589885, 22.91950879131610108, -54.64999999999999858 ) ) ;
#8448=CARTESIAN_POINT ( 'NONE',  ( 42.32923956695206869, 6.443803624954492548, -78.67348905400854164 ) ) ;
#8452=CARTESIAN_POINT ( 'NONE',  ( 45.34361468062490275, 2.694758396794109778, -34.64999999999999858 ) ) ;
#8460=CARTESIAN_POINT ( 'NONE',  ( 47.13393739769619373, 4.883811055320659733, -35.14999999999999858 ) ) ;
#8478=CARTESIAN_POINT ( 'NONE',  ( 26.13393739769619728, -2.337132753317950229, -62.14999999999999858 ) ) ;
#8480=LINE ( 'NONE', #9267, #27760 ) ;
#8481=CYLINDRICAL_SURFACE ( 'NONE', #10842, 0.4999999999999984457 ) ;
#8490=CARTESIAN_POINT ( 'NONE',  ( -0.05431535188140382969, -10.47559300615912115, -34.81369804311114535 ) ) ;
#8497=ORIENTED_EDGE ( 'NONE', *, *, #4957, .T. ) ;
#8498=ORIENTED_EDGE ( 'NONE', *, *, #33825, .T. ) ;
#8502=CARTESIAN_POINT ( 'NONE',  ( 0.4253373362159595383, -8.849698965567686315, -35.06583844469757594 ) ) ;
#8510=EDGE_CURVE ( 'NONE', #21889, #32046, #15566, .T. ) ;
#8526=VERTEX_POINT ( 'NONE', #10861 ) ;
#8535=CARTESIAN_POINT ( 'NONE',  ( 42.93611710919282842, -39.85996260035505401, -71.80852276252326760 ) ) ;
#8543=CARTESIAN_POINT ( 'NONE',  ( 18.13393739769630031, 1.380694156556650176, -35.10658870009205401 ) ) ;
#8545=VERTEX_POINT ( 'NONE', #16069 ) ;
#8553=CARTESIAN_POINT ( 'NONE',  ( 42.84219048620263948, 8.618426686109231127, -72.26305710318311526 ) ) ;
#8554=CARTESIAN_POINT ( 'NONE',  ( 44.97636411188102556, -33.23110557053604452, -38.73002865210571599 ) ) ;
#8556=CARTESIAN_POINT ( 'NONE',  ( 29.52393724633215299, 4.446165992738185579, -84.61793436501787369 ) ) ;
#8570=FACE_OUTER_BOUND ( 'NONE', #41552, .T. ) ;
#8574=DIRECTION ( 'NONE',  ( -0.3863301728269271096, 0.9223605572461979207, 0.000000000000000000 ) ) ;
#8587=CARTESIAN_POINT ( 'NONE',  ( 21.79705635832086585, -42.73068571072664668, -84.65000000000000568 ) ) ;
#8619=EDGE_LOOP ( 'NONE', ( #15428, #28658, #9968, #10737 ) ) ;
#8627=ORIENTED_EDGE ( 'NONE', *, *, #3260, .T. ) ;
#8635=CARTESIAN_POINT ( 'NONE',  ( 10.06369629474122185, 22.76024865223496363, -34.79644414665609986 ) ) ;
#8645=CIRCLE ( 'NONE', #2777, 6.999999999999999112 ) ;
#8653=CARTESIAN_POINT ( 'NONE',  ( 28.63499203762230394, -4.678279065789539892, -34.64999999999999858 ) ) ;
#8654=CARTESIAN_POINT ( 'NONE',  ( 13.13393739769619906, -49.61618894467939356, -83.01107220193038927 ) ) ;
#8655=AXIS2_PLACEMENT_3D ( 'NONE', #7493, #24207, #8256 ) ;
#8657=DIRECTION ( 'NONE',  ( 0.8660254037844380415, -0.5000000000000012212, -2.498001805406606160E-16 ) ) ;
#8658=LINE ( 'NONE', #48759, #2983 ) ;
#8667=DIRECTION ( 'NONE',  ( 0.000000000000000000, -1.000000000000000000, 0.000000000000000000 ) ) ;
#8676=ORIENTED_EDGE ( 'NONE', *, *, #4784, .T. ) ;
#8677=DIRECTION ( 'NONE',  ( 0.5516667872527207805, -0.8340645993220556775, 0.000000000000000000 ) ) ;
#8679=AXIS2_PLACEMENT_3D ( 'NONE', #29541, #9893, #21664 ) ;
#8688=AXIS2_PLACEMENT_3D ( 'NONE', #48416, #454, #36344 ) ;
#8690=CIRCLE ( 'NONE', #35466, 34.47562460986249278 ) ;
#8691=FACE_OUTER_BOUND ( 'NONE', #39688, .T. ) ;
#8697=ORIENTED_EDGE ( 'NONE', *, *, #3799, .F. ) ;
#8704=CARTESIAN_POINT ( 'NONE',  ( 41.81045037156589217, 6.360722813067012815, -81.26737402878971750 ) ) ;
#8709=CARTESIAN_POINT ( 'NONE',  ( 41.63696876380908662, -37.56364127202510872, -82.13484301340810134 ) ) ;
#8732=CARTESIAN_POINT ( 'NONE',  ( 29.13393739769619728, 4.555383930574479656, -84.63196841427449613 ) ) ;
#8734=DIRECTION ( 'NONE',  ( -0.6522074047277892639, -0.2731766849828938248, 0.7071067811865464625 ) ) ;
#8736=FACE_OUTER_BOUND ( 'NONE', #37629, .T. ) ;
#8737=DIRECTION ( 'NONE',  ( 0.3535533905932736198, -0.6123724356957950254, 0.7071067811865472397 ) ) ;
#8738=CARTESIAN_POINT ( 'NONE',  ( -3.839728563314090071, -24.83858928721370063, -54.64999999999999858 ) ) ;
#8740=CARTESIAN_POINT ( 'NONE',  ( -0.2544260390843469111, -20.43873413140054041, -34.98772936183320326 ) ) ;
#8747=ORIENTED_EDGE ( 'NONE', *, *, #47880, .T. ) ;
#8748=FACE_OUTER_BOUND ( 'NONE', #35864, .T. ) ;
#8750=FACE_OUTER_BOUND ( 'NONE', #19333, .T. ) ;
#8752=ORIENTED_EDGE ( 'NONE', *, *, #39577, .F. ) ;
#8765=DIRECTION ( 'NONE',  ( 0.000000000000000000, 0.000000000000000000, -1.000000000000000000 ) ) ;
#8790=CARTESIAN_POINT ( 'NONE',  ( 43.55496689572915159, -39.91667278102725192, -68.81525705887698052 ) ) ;
#8792=CARTESIAN_POINT ( 'NONE',  ( -0.03447620312153643757, -27.09132598751343579, -34.79644660940672907 ) ) ;
#8809=CARTESIAN_POINT ( 'NONE',  ( 40.97558342559717914, 8.414888246701108798, -81.27204827182337965 ) ) ;
#8814=ORIENTED_EDGE ( 'NONE', *, *, #46767, .T. ) ;
#8818=ORIENTED_EDGE ( 'NONE', *, *, #47790, .F. ) ;
#8826=EDGE_LOOP ( 'NONE', ( #42454, #51208, #21685, #19193, #8889, #39635, #27809 ) ) ;
#8827=CARTESIAN_POINT ( 'NONE',  ( -0.007164427059776000244, 14.47565373231149977, -34.77269723891829756 ) ) ;
#8828=CARTESIAN_POINT ( 'NONE',  ( -16.19549477698355844, 6.204146130383243474, -49.15060503604010478 ) ) ;
#8829=DIRECTION ( 'NONE',  ( -0.2846079131720410937, -0.9586440088791334801, 0.000000000000000000 ) ) ;
#8831=DIRECTION ( 'NONE',  ( -1.000000000000000000, 0.000000000000000000, 0.000000000000000000 ) ) ;
#8832=EDGE_CURVE ( 'NONE', #41771, #33944, #9303, .T. ) ;
#8833=CARTESIAN_POINT ( 'NONE',  ( 18.63393739769599833, 14.38381105532070059, -35.14999999999999858 ) ) ;
#8840=CARTESIAN_POINT ( 'NONE',  ( 19.13393739769600188, 18.38381105532069881, -35.14999999999999858 ) ) ;
#8852=AXIS2_PLACEMENT_3D ( 'NONE', #20627, #465, #32406 ) ;
#8856=DIRECTION ( 'NONE',  ( -1.000000000000000000, 0.000000000000000000, 0.000000000000000000 ) ) ;
#8860=VECTOR ( 'NONE', #31060, 1000.000000000000000 ) ;
#8870=CARTESIAN_POINT ( 'NONE',  ( 2.558369240368460140, -6.046280207075140467, -34.64999999999999858 ) ) ;
#8876=LINE ( 'NONE', #41100, #8355 ) ;
#8877=EDGE_CURVE ( 'NONE', #51503, #46428, #15419, .T. ) ;
#8882=ORIENTED_EDGE ( 'NONE', *, *, #32512, .T. ) ;
#8889=ORIENTED_EDGE ( 'NONE', *, *, #42779, .F. ) ;
#8902=CYLINDRICAL_SURFACE ( 'NONE', #14303, 2.999999999999999112 ) ;
#8915=CARTESIAN_POINT ( 'NONE',  ( 30.13393739769619728, 7.383811055320659733, -72.14999999999999147 ) ) ;
#8922=CARTESIAN_POINT ( 'NONE',  ( 28.63710131890649890, -4.677486598597970335, -34.65001001049759566 ) ) ;
#8923=CONICAL_SURFACE ( 'NONE', #33995, 3.567506086244480734, 0.04995839572194331335 ) ;
#8928=CARTESIAN_POINT ( 'NONE',  ( 42.87338644773151941, -39.93353782726089918, -71.78159119793272680 ) ) ;
#8933=EDGE_CURVE ( 'NONE', #39703, #8293, #24127, .T. ) ;
#8962=ORIENTED_EDGE ( 'NONE', *, *, #28302, .T. ) ;
#8965=DIRECTION ( 'NONE',  ( -0.3502816565540492477, 0.000000000000000000, 0.9366444154970182678 ) ) ;
#8967=ORIENTED_EDGE ( 'NONE', *, *, #16744, .F. ) ;
#8969=CARTESIAN_POINT ( 'NONE',  ( 41.61626771661330082, 6.328436186825659782, -82.23834840541459812 ) ) ;
#8975=ORIENTED_EDGE ( 'NONE', *, *, #35399, .F. ) ;
#8988=DIRECTION ( 'NONE',  ( 0.000000000000000000, 0.000000000000000000, -1.000000000000000000 ) ) ;
#8997=FACE_OUTER_BOUND ( 'NONE', #29641, .T. ) ;
#8999=LINE ( 'NONE', #8478, #45731 ) ;
#9012=DIRECTION ( 'NONE',  ( 0.000000000000000000, 0.000000000000000000, -1.000000000000000000 ) ) ;
#9017=EDGE_LOOP ( 'NONE', ( #43634, #32873, #3013, #29969 ) ) ;
#9028=VERTEX_POINT ( 'NONE', #19808 ) ;
#9031=DIRECTION ( 'NONE',  ( 0.000000000000000000, 0.000000000000000000, 1.000000000000000000 ) ) ;
#9033=EDGE_LOOP ( 'NONE', ( #21957, #17215, #29376, #29010 ) ) ;
#9036=DIRECTION ( 'NONE',  ( 0.000000000000000000, 1.000000000000000000, 0.000000000000000000 ) ) ;
#9038=EDGE_CURVE ( 'NONE', #21587, #11026, #47602, .T. ) ;
#9040=DIRECTION ( 'NONE',  ( 0.000000000000000000, -0.7071067811865466846, -0.7071067811865483499 ) ) ;
#9042=LINE ( 'NONE', #21072, #40488 ) ;
#9057=CARTESIAN_POINT ( 'NONE',  ( 14.63288374505870060, -32.15889263939740772, -34.64999999999999858 ) ) ;
#9059=LINE ( 'NONE', #28436, #17259 ) ;
#9063=VERTEX_POINT ( 'NONE', #19033 ) ;
#9069=CARTESIAN_POINT ( 'NONE',  ( 44.97106839982397730, 8.796052713493059727, -61.95337525835541470 ) ) ;
#9070=CARTESIAN_POINT ( 'NONE',  ( -0.02503409344754733978, -8.417620798886582989, -34.78823607925543371 ) ) ;
#9075=ORIENTED_EDGE ( 'NONE', *, *, #14122, .T. ) ;
#9087=CARTESIAN_POINT ( 'NONE',  ( -13.33284876601550728, 9.986826335083126338, -46.69325378129649096 ) ) ;
#9093=DIRECTION ( 'NONE',  ( -1.000000000000000000, 0.000000000000000000, 0.000000000000000000 ) ) ;
#9094=CARTESIAN_POINT ( 'NONE',  ( 23.24148394091340109, -47.84168788784550230, -54.64999999999999858 ) ) ;
#9112=CARTESIAN_POINT ( 'NONE',  ( 23.14289354968460088, -48.86424211905639936, -35.14566343974149731 ) ) ;
#9121=EDGE_CURVE ( 'NONE', #50203, #32053, #43417, .T. ) ;
#9125=ORIENTED_EDGE ( 'NONE', *, *, #36824, .F. ) ;
#9127=CARTESIAN_POINT ( 'NONE',  ( 2.558062577109650348, -6.044886501696560721, -34.64999999999999858 ) ) ;
#9141=VECTOR ( 'NONE', #4765, 1000.000000000000000 ) ;
#9146=AXIS2_PLACEMENT_3D ( 'NONE', #2122, #45897, #17844 ) ;
#9147=ORIENTED_EDGE ( 'NONE', *, *, #23519, .F. ) ;
#9150=AXIS2_PLACEMENT_3D ( 'NONE', #42790, #6885, #11074 ) ;
#9152=DIRECTION ( 'NONE',  ( 0.000000000000000000, -1.000000000000000000, 0.000000000000000000 ) ) ;
#9156=CARTESIAN_POINT ( 'NONE',  ( 18.11511214869360131, -32.59175772023380091, -35.01387690002269437 ) ) ;
#9163=EDGE_CURVE ( 'NONE', #16231, #8281, #48781, .T. ) ;
#9175=CARTESIAN_POINT ( 'NONE',  ( 16.13393739769599833, 14.38381105532070059, -34.64999999999999858 ) ) ;
#9180=VECTOR ( 'NONE', #25900, 999.9999999999998863 ) ;
#9181=CIRCLE ( 'NONE', #25871, 33.97624844042369574 ) ;
#9182=CARTESIAN_POINT ( 'NONE',  ( 14.67232007451260323, -49.61617055433323742, -83.19301782014780144 ) ) ;
#9186=B_SPLINE_CURVE_WITH_KNOTS ( 'NONE', 3,
 ( #39794, #214, #24814, #23782, #4923, #47666, #15951, #24549 ),
 .UNSPECIFIED., .F., .F.,
 ( 4, 2, 2, 4 ),
 ( -0.1350635247378738635, -0.1243669311571979907, -0.1075965482621700081, -0.1052074838067399987 ),
 .UNSPECIFIED. ) ;
#9188=CARTESIAN_POINT ( 'NONE',  ( 29.57851616124868599, -35.65923776031012693, -84.61510634421995292 ) ) ;
#9212=CARTESIAN_POINT ( 'NONE',  ( 2.458146360389370511, -25.65221394861527671, -34.79644291222910368 ) ) ;
#9223=CYLINDRICAL_SURFACE ( 'NONE', #25002, 2.999999999999994227 ) ;
#9225=CARTESIAN_POINT ( 'NONE',  ( 26.13393739769619728, -28.89524513604070322, -62.14999999999999858 ) ) ;
#9226=CIRCLE ( 'NONE', #33467, 0.4934525379923264121 ) ;
#9228=AXIS2_PLACEMENT_3D ( 'NONE', #3883, #11753, #15159 ) ;
#9231=VECTOR ( 'NONE', #18732, 1000.000000000000000 ) ;
#9234=AXIS2_PLACEMENT_3D ( 'NONE', #40277, #15916, #31870 ) ;
#9248=CARTESIAN_POINT ( 'NONE',  ( 44.13393739769620083, 1.883811055320659955, -54.35294145922169662 ) ) ;
#9249=CARTESIAN_POINT ( 'NONE',  ( 33.38393739769599478, 10.53025766472752522, -34.79644660940672907 ) ) ;
#9251=ORIENTED_EDGE ( 'NONE', *, *, #8160, .F. ) ;
#9258=AXIS2_PLACEMENT_3D ( 'NONE', #47001, #50910, #11086 ) ;
#9265=AXIS2_PLACEMENT_3D ( 'NONE', #23564, #19655, #39078 ) ;
#9267=CARTESIAN_POINT ( 'NONE',  ( 11.96660005458869946, 10.88381105532060111, -34.64999999999999858 ) ) ;
#9269=DIRECTION ( 'NONE',  ( 0.000000000000000000, 0.000000000000000000, -1.000000000000000000 ) ) ;
#9276=FACE_OUTER_BOUND ( 'NONE', #41761, .T. ) ;
#9278=CARTESIAN_POINT ( 'NONE',  ( 28.63393739769619728, -22.83306730954970121, -34.64999999999999858 ) ) ;
#9279=EDGE_CURVE ( 'NONE', #39608, #18727, #6211, .T. ) ;
#9283=ORIENTED_EDGE ( 'NONE', *, *, #34824, .F. ) ;
#9284=EDGE_CURVE ( 'NONE', #24387, #38190, #42239, .T. ) ;
#9295=ORIENTED_EDGE ( 'NONE', *, *, #12683, .F. ) ;
#9300=CARTESIAN_POINT ( 'NONE',  ( 0.1457840918194806823, -20.72567761198500591, -34.68167776469320529 ) ) ;
#9303=( BOUNDED_CURVE ( )  B_SPLINE_CURVE ( 3, ( #38583, #2677, #11317, #18650 ),
 .UNSPECIFIED., .F., .T. ) 
 B_SPLINE_CURVE_WITH_KNOTS ( ( 4, 4 ),
 ( 1.570796326794898556, 2.356194490192396351 ),
 .UNSPECIFIED. ) 
 CURVE ( )  GEOMETRIC_REPRESENTATION_ITEM ( )  RATIONAL_B_SPLINE_CURVE ( ( 1.000000000000000000, 0.9492530216741847937, 0.9492530216741847937, 1.000000000000000000 ) ) 
 REPRESENTATION_ITEM ( '' )  );
#9304=ORIENTED_EDGE ( 'NONE', *, *, #48224, .F. ) ;
#9308=DIRECTION ( 'NONE',  ( 0.8204012560548784583, -0.5717882292104110586, 0.000000000000000000 ) ) ;
#9334=ORIENTED_EDGE ( 'NONE', *, *, #6288, .T. ) ;
#9339=CARTESIAN_POINT ( 'NONE',  ( 43.82411958768233262, 8.707906524021627348, -67.51045570699398013 ) ) ;
#9357=FACE_OUTER_BOUND ( 'NONE', #50941, .T. ) ;
#9360=ORIENTED_EDGE ( 'NONE', *, *, #16617, .T. ) ;
#9364=CARTESIAN_POINT ( 'NONE',  ( 14.15276264669880035, -32.59175772023380091, -35.01387690002269437 ) ) ;
#9368=CARTESIAN_POINT ( 'NONE',  ( 8.653191590475879380, 17.54226184052370030, -35.01184033120630090 ) ) ;
#9375=AXIS2_PLACEMENT_3D ( 'NONE', #26780, #42795, #51170 ) ;
#9380=ORIENTED_EDGE ( 'NONE', *, *, #2851, .F. ) ;
#9390=CARTESIAN_POINT ( 'NONE',  ( 23.49471107943040238, -48.44626589137899941, -41.74835364838589413 ) ) ;
#9401=DIRECTION ( 'NONE',  ( -0.6918010270571991471, -0.3994115091971301434, -0.6015661104845211327 ) ) ;
#9404=EDGE_LOOP ( 'NONE', ( #7598, #15528, #2198, #45694, #28518 ) ) ;
#9413=CIRCLE ( 'NONE', #37005, 17.09468304687054996 ) ;
#9415=CARTESIAN_POINT ( 'NONE',  ( -19.05153563686570095, -33.04232519026420078, -51.54856132249189216 ) ) ;
#9416=DIRECTION ( 'NONE',  ( 0.000000000000000000, 0.000000000000000000, 1.000000000000000000 ) ) ;
#9425=CARTESIAN_POINT ( 'NONE',  ( 4.133937397696209715, -22.54439217495480108, -47.64999999999999858 ) ) ;
#9437=CARTESIAN_POINT ( 'NONE',  ( 34.00893739769620083, -11.50256827670329862, -35.14999999999999858 ) ) ;
#9442=AXIS2_PLACEMENT_3D ( 'NONE', #8185, #48530, #8965 ) ;
#9448=CARTESIAN_POINT ( 'NONE',  ( 45.09311312900799606, -39.18053832272051551, -65.04754641029070683 ) ) ;
#9451=ORIENTED_EDGE ( 'NONE', *, *, #11914, .F. ) ;
#9465=ORIENTED_EDGE ( 'NONE', *, *, #45307, .T. ) ;
#9475=DIRECTION ( 'NONE',  ( -0.4999999999999998890, 0.8660254037844387076, 0.000000000000000000 ) ) ;
#9477=DIRECTION ( 'NONE',  ( 0.000000000000000000, 0.000000000000000000, -1.000000000000000000 ) ) ;
#9492=CARTESIAN_POINT ( 'NONE',  ( 14.13393739769619906, -41.61618894467930119, -35.14999999999999858 ) ) ;
#9493=CARTESIAN_POINT ( 'NONE',  ( 11.66815189201670400, -41.66761415519156486, -34.89146800830130246 ) ) ;
#9496=CARTESIAN_POINT ( 'NONE',  ( 41.65893704031727651, -37.56744562278856137, -82.02500123744080440 ) ) ;
#9497=ADVANCED_FACE ( 'NONE', ( #653 ), #12128, .F. ) ;
#9506=EDGE_CURVE ( 'NONE', #11807, #31098, #19149, .T. ) ;
#9515=AXIS2_PLACEMENT_3D ( 'NONE', #46333, #22706, #42128 ) ;
#9516=ORIENTED_EDGE ( 'NONE', *, *, #48224, .T. ) ;
#9520=CARTESIAN_POINT ( 'NONE',  ( -11.59939519670759189, -33.93743706034221219, -49.87766020311142512 ) ) ;
#9537=EDGE_CURVE ( 'NONE', #24151, #2565, #22631, .T. ) ;
#9539=ORIENTED_EDGE ( 'NONE', *, *, #4678, .T. ) ;
#9541=CARTESIAN_POINT ( 'NONE',  ( 15.10238578887267735, 12.66681598883027426, -61.51477253168943804 ) ) ;
#9548=DIRECTION ( 'NONE',  ( 0.4743737082415241391, -0.8803235683140518963, 0.000000000000000000 ) ) ;
#9550=CARTESIAN_POINT ( 'NONE',  ( 46.35743359015805254, 6.957031320103493677, -58.53251102570533959 ) ) ;
#9553=CARTESIAN_POINT ( 'NONE',  ( -0.9510857394171997603, -26.69247394909374904, -59.64999999999999147 ) ) ;
#9565=VERTEX_POINT ( 'NONE', #34157 ) ;
#9566=DIRECTION ( 'NONE',  ( 0.000000000000000000, 0.000000000000000000, 1.000000000000000000 ) ) ;
#9584=VERTEX_POINT ( 'NONE', #49411 ) ;
#9585=CARTESIAN_POINT ( 'NONE',  ( 16.13393739769620083, -15.61618894467929941, -54.64999999999999858 ) ) ;
#9588=CARTESIAN_POINT ( 'NONE',  ( 44.13393739769620083, -36.11618894467930119, -34.64999999999999858 ) ) ;
#9589=CARTESIAN_POINT ( 'NONE',  ( 43.52531948755864732, 8.681712052945677272, -68.95854737653661459 ) ) ;
#9593=EDGE_CURVE ( 'NONE', #38190, #18993, #42573, .T. ) ;
#9597=ORIENTED_EDGE ( 'NONE', *, *, #14901, .T. ) ;
#9601=( BOUNDED_CURVE ( )  B_SPLINE_CURVE ( 2, ( #23961, #7762, #15876 ),
 .UNSPECIFIED., .F., .T. ) 
 B_SPLINE_CURVE_WITH_KNOTS ( ( 3, 3 ),
 ( 0.2168422315592359872, 3.147551163859270140 ),
 .UNSPECIFIED. ) 
 CURVE ( )  GEOMETRIC_REPRESENTATION_ITEM ( )  RATIONAL_B_SPLINE_CURVE ( ( 1.000597593688249853, 1.004455541114980033, 1.003436844929630034 ) ) 
 REPRESENTATION_ITEM ( '' )  );
#9607=VECTOR ( 'NONE', #29255, 1000.000000000000000 ) ;
#9621=CARTESIAN_POINT ( 'NONE',  ( 47.05485148372110160, 8.151374499743630153, -53.95852907688490063 ) ) ;
#9623=EDGE_LOOP ( 'NONE', ( #43719, #40520, #50872, #5998, #28266, #51770 ) ) ;
#9648=EDGE_CURVE ( 'NONE', #18491, #3105, #26315, .T. ) ;
#9659=ORIENTED_EDGE ( 'NONE', *, *, #37388, .F. ) ;
#9660=CARTESIAN_POINT ( 'NONE',  ( -22.69159524740030065, -18.52108238997520218, -54.49830448709099784 ) ) ;
#9664=CARTESIAN_POINT ( 'NONE',  ( 22.27218754053139804, -53.83794553065759914, -34.69483829921989582 ) ) ;
#9691=CARTESIAN_POINT ( 'NONE',  ( 17.84637960111742672, -49.61616104255114834, -83.17357193461836573 ) ) ;
#9693=CARTESIAN_POINT ( 'NONE',  ( 20.13393739769620083, -2.337132753317949785, -84.65000000000000568 ) ) ;
#9695=DIRECTION ( 'NONE',  ( 1.000000000000000000, 0.000000000000000000, 0.000000000000000000 ) ) ;
#9696=CARTESIAN_POINT ( 'NONE',  ( 47.16590163426349847, -39.34201989322590975, -54.77441423021601707 ) ) ;
#9699=ORIENTED_EDGE ( 'NONE', *, *, #35323, .T. ) ;
#9730=CARTESIAN_POINT ( 'NONE',  ( 30.13393739769619728, -38.61618894467930119, -84.65000000000000568 ) ) ;
#9735=CARTESIAN_POINT ( 'NONE',  ( 14.13393739769599833, 14.38381105532070059, -35.14999999999999858 ) ) ;
#9737=CARTESIAN_POINT ( 'NONE',  ( 0.3209249304026170480, -15.61618894467929941, -35.14999999999999858 ) ) ;
#9742=CARTESIAN_POINT ( 'NONE',  ( 43.59785196581361078, -37.86270477977220850, -72.33041599445031977 ) ) ;
#9750=CIRCLE ( 'NONE', #11410, 16.60961179679779676 ) ;
#9758=EDGE_CURVE ( 'NONE', #4073, #46602, #21968, .T. ) ;
#9765=CARTESIAN_POINT ( 'NONE',  ( 46.81384049422970151, -39.17204965157010577, -34.68207991959079806 ) ) ;
#9797=ORIENTED_EDGE ( 'NONE', *, *, #17749, .T. ) ;
#9802=CARTESIAN_POINT ( 'NONE',  ( 6.784299814571713050, 1.742308277892916646, -84.65000000000000568 ) ) ;
#9803=VERTEX_POINT ( 'NONE', #10858 ) ;
#9805=CARTESIAN_POINT ( 'NONE',  ( 45.44635879492527408, 6.861525894367711764, -63.08783649271359906 ) ) ;
#9824=ORIENTED_EDGE ( 'NONE', *, *, #45017, .F. ) ;
#9825=DIRECTION ( 'NONE',  ( 0.8204012560548797905, 0.5717882292104092823, 0.000000000000000000 ) ) ;
#9827=CARTESIAN_POINT ( 'NONE',  ( 16.81199894099719927, -16.95676073769629610, -35.14999999999999858 ) ) ;
#9832=CARTESIAN_POINT ( 'NONE',  ( 10.04852440032967209, -53.95817006707463293, -34.76477869314685876 ) ) ;
#9835=CARTESIAN_POINT ( 'NONE',  ( 38.67452568954060155, 4.883811055320659733, -81.65000000000000568 ) ) ;
#9837=VERTEX_POINT ( 'NONE', #6996 ) ;
#9845=CARTESIAN_POINT ( 'NONE',  ( 44.31510748265038302, 8.747601604831885425, -65.13307718246910838 ) ) ;
#9851=CARTESIAN_POINT ( 'NONE',  ( -22.76297446149728998, -18.32468108091643089, -54.70357014338004831 ) ) ;
#9852=CARTESIAN_POINT ( 'NONE',  ( 17.63393739769639978, 10.88381105532070059, -34.64999999999999858 ) ) ;
#9857=DIRECTION ( 'NONE',  ( 1.000000000000000000, 0.000000000000000000, 0.000000000000000000 ) ) ;
#9858=ADVANCED_FACE ( 'NONE', ( #17744 ), #6216, .T. ) ;
#9874=CARTESIAN_POINT ( 'NONE',  ( 46.56831964672900170, 8.771274579019829432, -54.63028235546250500 ) ) ;
#9876=EDGE_CURVE ( 'NONE', #5705, #27765, #40617, .T. ) ;
#9877=VERTEX_POINT ( 'NONE', #29776 ) ;
#9880=CARTESIAN_POINT ( 'NONE',  ( 46.21668119980922285, -40.10555969717534452, -55.90708416986943519 ) ) ;
#9886=PLANE ( 'NONE',  #48198 ) ;
#9893=DIRECTION ( 'NONE',  ( 0.000000000000000000, 0.000000000000000000, 1.000000000000000000 ) ) ;
#9900=CARTESIAN_POINT ( 'NONE',  ( 0.6045892726184849408, -22.44175889786657763, -34.79644291222908237 ) ) ;
#9902=DIRECTION ( 'NONE',  ( 1.000000000000000000, 0.000000000000000000, 0.000000000000000000 ) ) ;
#9905=ORIENTED_EDGE ( 'NONE', *, *, #15093, .T. ) ;
#9911=CARTESIAN_POINT ( 'NONE',  ( -22.58910033241870252, -11.83175606744140040, -54.40873678327959340 ) ) ;
#9935=VECTOR ( 'NONE', #39593, 1000.000000000000000 ) ;
#9945=LINE ( 'NONE', #26683, #23078 ) ;
#9946=CARTESIAN_POINT ( 'NONE',  ( -21.13107420191839836, -3.984212544564229574, -53.16029643437919816 ) ) ;
#9947=FACE_OUTER_BOUND ( 'NONE', #32377, .T. ) ;
#9948=CARTESIAN_POINT ( 'NONE',  ( 45.20206541413084267, -40.17273866886250744, -60.31333638933742947 ) ) ;
#9956=CARTESIAN_POINT ( 'NONE',  ( 43.35873532115121520, 8.736805108720993474, -69.47954381186947614 ) ) ;
#9957=CARTESIAN_POINT ( 'NONE',  ( 16.13393739769620083, -29.89477637979525682, -34.64999999999999858 ) ) ;
#9968=ORIENTED_EDGE ( 'NONE', *, *, #18404, .T. ) ;
#9971=FACE_OUTER_BOUND ( 'NONE', #1381, .T. ) ;
#9990=PLANE ( 'NONE',  #18365 ) ;
#9995=CARTESIAN_POINT ( 'NONE',  ( 45.40002876707641377, -38.08857925617063245, -63.31948497716211222 ) ) ;
#10004=ADVANCED_FACE ( 'NONE', ( #43917 ), #23454, .T. ) ;
#10013=VERTEX_POINT ( 'NONE', #11958 ) ;
#10017=CARTESIAN_POINT ( 'NONE',  ( 41.94197894960735340, -39.75821015298250671, -76.61187673551151534 ) ) ;
#10030=DIRECTION ( 'NONE',  ( 1.000000000000000000, 0.000000000000000000, 0.000000000000000000 ) ) ;
#10033=AXIS2_PLACEMENT_3D ( 'NONE', #26083, #45769, #10383 ) ;
#10038=ORIENTED_EDGE ( 'NONE', *, *, #21315, .F. ) ;
#10042=AXIS2_PLACEMENT_3D ( 'NONE', #30202, #34909, #42273 ) ;
#10045=ORIENTED_EDGE ( 'NONE', *, *, #40971, .F. ) ;
#10055=( BOUNDED_SURFACE ( )  B_SPLINE_SURFACE ( 2, 3, ( 
 ( #24092, #1054, #40114, #32215, #36421, #36170, #40624, #28040, #48239, #33002, #8405, #20689, #8928, #24873, #49026, #40367, #528, #5256, #37218, #17307, #21472, #29341, #9948, #13635, #46129, #2612, #14398, #49284, #6024, #17809, #37733, #25912, #18583, #29594, #45343, #18068, #13381 ),
 ( #46391, #26176, #26433, #38251, #1831, #30109, #2344, #30366, #34297, #21984, #10478, #33783, #14139, #49792, #41926, #10216, #13884, #17561, #9448, #42451, #6538, #50313, #45598, #37994, #34036, #22501, #5762, #9696, #38513, #25396, #37472, #29844, #25656, #41398, #42187, #21726, #50046 ),
 ( #5516, #1570, #45864, #49543, #22243, #2090, #41659, #33530, #6286, #18318, #15440, #3902, #27472, #19616, #39543, #3392, #11513, #47163, #46908, #3645, #26959, #19359, #11774, #46650, #14656, #35074, #35607, #23783, #50566, #18837, #43473, #31391, #26687, #51080, #35340, #14914, #39284 ) ),
 .UNSPECIFIED., .F., .F., .T. ) 
 B_SPLINE_SURFACE_WITH_KNOTS ( ( 3, 3 ),
 ( 4, 3, 3, 3, 3, 3, 3, 3, 3, 3, 3, 3, 4 ),
 ( -0.3950274212275620145, 0.3825042522605620054 ),
 ( 1.319931596140740071, 1.327157646422050030, 1.335327538272319980, 1.343527953381050022, 1.351756755142390132, 1.360011799518540121, 1.368290935607660019, 1.376592006214460095, 1.384912848423149878, 1.392992571260399881, 1.393221429621980034, 1.393251294075019908, 1.399915485122189995 ),
 .UNSPECIFIED. ) 
 GEOMETRIC_REPRESENTATION_ITEM ( )  RATIONAL_B_SPLINE_SURFACE ( (
 ( 1.002404754520709984, 1.002404754520709984, 1.002404754520709984, 1.002404754520709984, 1.002404754520709984, 1.002404754520709984, 1.002404754520709984, 1.002404754520709984, 1.002404754520709984, 1.002404754520709984, 1.002404754520709984, 1.002404754520709984, 1.002404754520709984, 1.002404754520709984, 1.002404754520709984, 1.002404754520709984, 1.002404754520709984, 1.002404754520709984, 1.002404754520709984, 1.002404754520709984, 1.002404754520709984, 1.002404754520709984, 1.002404754520709984, 1.002404754520709984, 1.002404754520709984, 1.002404754520709984, 1.002404754520709984, 1.002404754520709984, 1.002404754520709984, 1.002404754520709984, 1.002404754520709984, 1.002404754520709984, 1.002404754520709984, 1.002404754520709984, 1.002404754520709984, 1.002404754520709984, 1.002404754520709984),
 ( 0.9265498347468470453, 0.9265498347725940054, 0.9265498347720859673, 0.9265498347720839689, 0.9265498347720839689, 0.9265498347721010663, 0.9265498347721010663, 0.9265498347721010663, 0.9265498347720839689, 0.9265498347720839689, 0.9265498347720839689, 0.9265498347720809713, 0.9265498347720809713, 0.9265498347720809713, 0.9265498347720950711, 0.9265498347720950711, 0.9265498347720950711, 0.9265498347720919625, 0.9265498347720919625, 0.9265498347720919625, 0.9265498347720960703, 0.9265498347720960703, 0.9265498347720960703, 0.9265498347720879657, 0.9265498347720879657, 0.9265498347720879657, 0.9265498347720839689, 0.9265498347720839689, 0.9265498347720839689, 0.9265498347720779737, 0.9265498347720779737, 0.9265498347720779737, 0.9265498347721010663, 0.9265498347721010663, 0.9265498347721010663, 0.9265498347721010663, 0.9265498347721010663),
 ( 1.000000000000000000, 1.000000000000000000, 1.000000000000000000, 1.000000000000000000, 1.000000000000000000, 1.000000000000000000, 1.000000000000000000, 1.000000000000000000, 1.000000000000000000, 1.000000000000000000, 1.000000000000000000, 1.000000000000000000, 1.000000000000000000, 1.000000000000000000, 1.000000000000000000, 1.000000000000000000, 1.000000000000000000, 1.000000000000000000, 1.000000000000000000, 1.000000000000000000, 1.000000000000000000, 1.000000000000000000, 1.000000000000000000, 1.000000000000000000, 1.000000000000000000, 1.000000000000000000, 1.000000000000000000, 1.000000000000000000, 1.000000000000000000, 1.000000000000000000, 1.000000000000000000, 1.000000000000000000, 1.000000000000000000, 1.000000000000000000, 1.000000000000000000, 1.000000000000000000, 1.000000000000000000) ) ) 
 REPRESENTATION_ITEM ( '' )  SURFACE ( )  );
#10059=CARTESIAN_POINT ( 'NONE',  ( 46.86172237601420676, 7.004961998947965895, -56.01103048085943215 ) ) ;
#10060=ORIENTED_EDGE ( 'NONE', *, *, #21267, .T. ) ;
#10062=B_SPLINE_CURVE_WITH_KNOTS ( 'NONE', 3,
 ( #51235, #51736, #23924, #31541, #15831, #7974, #47560, #8229 ),
 .UNSPECIFIED., .F., .F.,
 ( 4, 2, 2, 4 ),
 ( 0.04513248637320322471, 0.05146834907058789321, 0.06948743966080110634, 0.08616863070398819713 ),
 .UNSPECIFIED. ) ;
#10080=EDGE_LOOP ( 'NONE', ( #19365, #43772, #41429, #45702, #26209 ) ) ;
#10093=MANIFOLD_SOLID_BREP ( 'Stock-MAS-691-1', #14266 ) ;
#10103=PLANE ( 'NONE',  #37676 ) ;
#10106=CARTESIAN_POINT ( 'NONE',  ( 43.43658709381130478, 8.673818529245354014, -69.38805309085101669 ) ) ;
#10112=EDGE_CURVE ( 'NONE', #20864, #7979, #47106, .T. ) ;
#10113=ORIENTED_EDGE ( 'NONE', *, *, #38895, .F. ) ;
#10116=PLANE ( 'NONE',  #41602 ) ;
#10117=CARTESIAN_POINT ( 'NONE',  ( 0.3209249304026170480, -50.71887597443840434, -35.14999999999999858 ) ) ;
#10118=EDGE_CURVE ( 'NONE', #51599, #40270, #2249, .T. ) ;
#10121=VECTOR ( 'NONE', #36978, 1000.000000000000114 ) ;
#10122=ADVANCED_FACE ( 'NONE', ( #923 ), #40493, .T. ) ;
#10123=ORIENTED_EDGE ( 'NONE', *, *, #36824, .T. ) ;
#10151=LINE ( 'NONE', #5198, #19767 ) ;
#10175=EDGE_LOOP ( 'NONE', ( #1772, #4817 ) ) ;
#10176=ORIENTED_EDGE ( 'NONE', *, *, #47921, .T. ) ;
#10178=CARTESIAN_POINT ( 'NONE',  ( -22.39805312675529692, -21.43557466898330333, -54.24260450001559519 ) ) ;
#10179=DIRECTION ( 'NONE',  ( 0.4999999999999995004, -0.8660254037844390407, 0.000000000000000000 ) ) ;
#10192=DIRECTION ( 'NONE',  ( 1.000000000000000000, 0.000000000000000000, 0.000000000000000000 ) ) ;
#10211=DIRECTION ( 'NONE',  ( 0.000000000000000000, 0.7071067811865475727, 0.7071067811865475727 ) ) ;
#10214=CARTESIAN_POINT ( 'NONE',  ( -0.004241732451505779607, 19.56172084038890091, -34.76917063876959446 ) ) ;
#10216=CARTESIAN_POINT ( 'NONE',  ( 44.39799025600027704, -39.11365857096617304, -68.49055761514939888 ) ) ;
#10217=DIRECTION ( 'NONE',  ( -1.000000000000000000, 0.000000000000000000, 0.000000000000000000 ) ) ;
#10218=FACE_OUTER_BOUND ( 'NONE', #24511, .T. ) ;
#10220=ADVANCED_FACE ( 'NONE', ( #14015 ), #5577, .T. ) ;
#10225=ORIENTED_EDGE ( 'NONE', *, *, #39034, .F. ) ;
#10226=CARTESIAN_POINT ( 'NONE',  ( 47.22924368751841229, 8.040797879301941009, -54.71938430924458885 ) ) ;
#10227=LINE ( 'NONE', #30374, #932 ) ;
#10231=CARTESIAN_POINT ( 'NONE',  ( 29.06532888865369912, -26.71461010031690009, -34.89721277419639733 ) ) ;
#10235=ORIENTED_EDGE ( 'NONE', *, *, #10454, .F. ) ;
#10251=DIRECTION ( 'NONE',  ( 0.8340645993220362486, 0.5516667872527503125, 0.000000000000000000 ) ) ;
#10263=CARTESIAN_POINT ( 'NONE',  ( 45.71767653649329333, -38.12345008805129254, -61.73130295846522841 ) ) ;
#10281=CARTESIAN_POINT ( 'NONE',  ( 42.18259662932334919, -39.78407723318860434, -75.44989511367202795 ) ) ;
#10289=CARTESIAN_POINT ( 'NONE',  ( 17.63393739769620083, -32.15793020853440254, -34.64999999999999858 ) ) ;
#10301=B_SPLINE_CURVE_WITH_KNOTS ( 'NONE', 3,
 ( #29756, #48941, #29511, #1230, #37641, #9364, #13044, #44996 ),
 .UNSPECIFIED., .F., .F.,
 ( 4, 2, 2, 4 ),
 ( 0.05028014561794270920, 0.06097673919875580550, 0.07774712209399009533, 0.08013618654945309228 ),
 .UNSPECIFIED. ) ;
#10308=EDGE_CURVE ( 'NONE', #46894, #30043, #18199, .T. ) ;
#10320=ORIENTED_EDGE ( 'NONE', *, *, #40036, .F. ) ;
#10322=CARTESIAN_POINT ( 'NONE',  ( 45.84154099693467543, 6.904674428428495325, -61.11197212361961562 ) ) ;
#10323=CARTESIAN_POINT ( 'NONE',  ( -14.38189736085656278, 8.722225734311907175, -47.59448514485664816 ) ) ;
#10337=AXIS2_PLACEMENT_3D ( 'NONE', #48016, #16040, #32499 ) ;
#10343=ADVANCED_FACE ( 'NONE', ( #22636 ), #21593, .T. ) ;
#10353=DIRECTION ( 'NONE',  ( 1.000000000000000000, 0.000000000000000000, 0.000000000000000000 ) ) ;
#10354=CARTESIAN_POINT ( 'NONE',  ( 44.89329732587840027, 2.479591951453110177, -35.14498018237689791 ) ) ;
#10358=ORIENTED_EDGE ( 'NONE', *, *, #47034, .F. ) ;
#10364=DIRECTION ( 'NONE',  ( 0.000000000000000000, 1.000000000000000000, 0.000000000000000000 ) ) ;
#10373=EDGE_LOOP ( 'NONE', ( #759, #11531, #29434, #29577, #47910, #31877, #14689 ) ) ;
#10377=VECTOR ( 'NONE', #40047, 1000.000000000000000 ) ;
#10379=VERTEX_POINT ( 'NONE', #37592 ) ;
#10383=DIRECTION ( 'NONE',  ( 0.000000000000000000, -1.000000000000000000, 0.000000000000000000 ) ) ;
#10384=ORIENTED_EDGE ( 'NONE', *, *, #46563, .T. ) ;
#10402=ADVANCED_FACE ( 'NONE', ( #6157 ), #22114, .T. ) ;
#10405=CARTESIAN_POINT ( 'NONE',  ( 44.56408710588276278, -39.99924422512690825, -63.92564782215845298 ) ) ;
#10406=EDGE_CURVE ( 'NONE', #6632, #43432, #20281, .T. ) ;
#10407=LINE ( 'NONE', #17998, #11724 ) ;
#10430=CARTESIAN_POINT ( 'NONE',  ( 8.731180243531696306, -48.92556967366426335, -34.79644561402096770 ) ) ;
#10432=EDGE_CURVE ( 'NONE', #24006, #14961, #29822, .T. ) ;
#10436=DIRECTION ( 'NONE',  ( 0.000000000000000000, 0.000000000000000000, -1.000000000000000000 ) ) ;
#10437=DIRECTION ( 'NONE',  ( 0.000000000000000000, 1.000000000000000000, 0.000000000000000000 ) ) ;
#10438=EDGE_LOOP ( 'NONE', ( #24391, #19135 ) ) ;
#10440=CARTESIAN_POINT ( 'NONE',  ( -20.85360007628929679, -28.79220445502869907, -53.09923876720240088 ) ) ;
#10452=CARTESIAN_POINT ( 'NONE',  ( 29.11900864776890074, -26.73446727828369873, -35.02873218748179340 ) ) ;
#10453=CARTESIAN_POINT ( 'NONE',  ( 4.133937397696209715, -22.54439217495480108, -47.64999999999999858 ) ) ;
#10454=EDGE_CURVE ( 'NONE', #47128, #8235, #7614, .T. ) ;
#10458=B_SPLINE_CURVE_WITH_KNOTS ( 'NONE', 3,
 ( #1739, #11160, #46815, #46555, #50984, #3811, #19526, #6970, #10645, #38689, #2775, #19008, #7746, #22669 ),
 .UNSPECIFIED., .F., .F.,
 ( 4, 2, 2, 2, 2, 2, 4 ),
 ( -0.1848816165265140254, -0.1844538286700970198, -0.1648065685561440064, -0.1461169962912039766, -0.1247799312927769938, -0.1076800599504059985, -0.09475412375652510211 ),
 .UNSPECIFIED. ) ;
#10466=VECTOR ( 'NONE', #11296, 1000.000000000000000 ) ;
#10471=CARTESIAN_POINT ( 'NONE',  ( 20.63393739769599833, 10.38381105532070059, -54.64999999999999858 ) ) ;
#10472=CARTESIAN_POINT ( 'NONE',  ( 29.02733844998730106, -4.531842835453759655, -34.83948955561429983 ) ) ;
#10473=DIRECTION ( 'NONE',  ( 1.000000000000000000, 0.000000000000000000, 0.000000000000000000 ) ) ;
#10476=CARTESIAN_POINT ( 'NONE',  ( -9.348116653862801329, 14.36157061842440008, -43.27560221459960133 ) ) ;
#10478=CARTESIAN_POINT ( 'NONE',  ( 43.23834971915461978, -38.99408868500810854, -74.22024637953136050 ) ) ;
#10479=AXIS2_PLACEMENT_3D ( 'NONE', #45794, #37924, #30299 ) ;
#10485=ORIENTED_EDGE ( 'NONE', *, *, #47406, .T. ) ;
#10486=CARTESIAN_POINT ( 'NONE',  ( 45.21445506089588662, 8.926488757556171549, -60.31552598061868764 ) ) ;
#10491=CARTESIAN_POINT ( 'NONE',  ( -3.366062602303800055, -15.61618894467929941, -44.64999999999999858 ) ) ;
#10502=CARTESIAN_POINT ( 'NONE',  ( 14.13393739769619906, -32.62399965035220362, -35.14999999999999858 ) ) ;
#10505=ORIENTED_EDGE ( 'NONE', *, *, #31267, .T. ) ;
#10508=CIRCLE ( 'NONE', #3022, 2.999999999999999112 ) ;
#10512=PLANE ( 'NONE',  #30856 ) ;
#10525=CARTESIAN_POINT ( 'NONE',  ( 45.05447910683652424, -38.04890345680490782, -65.04729142848933066 ) ) ;
#10527=CARTESIAN_POINT ( 'NONE',  ( 0.1155611319282749960, -51.17475502668380472, -35.14999999933320396 ) ) ;
#10535=CARTESIAN_POINT ( 'NONE',  ( 16.97276188636949712, 12.56821928479469896, -59.64999999999999147 ) ) ;
#10536=CIRCLE ( 'NONE', #40632, 0.4934432872204244647 ) ;
#10539=ORIENTED_EDGE ( 'NONE', *, *, #34824, .T. ) ;
#10544=CARTESIAN_POINT ( 'NONE',  ( 41.57151345658783015, -39.71737154464926789, -78.39838314987487422 ) ) ;
#10573=DIRECTION ( 'NONE',  ( -1.000000000000000000, 0.000000000000000000, 0.000000000000000000 ) ) ;
#10583=CARTESIAN_POINT ( 'NONE',  ( 45.75929793348244345, 6.895754709389400716, -61.52319716619024348 ) ) ;
#10594=FACE_OUTER_BOUND ( 'NONE', #46496, .T. ) ;
#10610=CARTESIAN_POINT ( 'NONE',  ( 12.95491128060830022, 18.65448050664010182, -82.14319696191608955 ) ) ;
#10616=CARTESIAN_POINT ( 'NONE',  ( 9.895190454276159286, -53.60841447722820163, -34.64999999999999858 ) ) ;
#10617=AXIS2_PLACEMENT_3D ( 'NONE', #15494, #23578, #22815 ) ;
#10629=CARTESIAN_POINT ( 'NONE',  ( 45.75938509646260854, 8.847270729488906582, -58.12753028167146141 ) ) ;
#10634=TOROIDAL_SURFACE ( 'NONE', #580, 16.60961179679779676, 0.5000000000000000000 ) ;
#10636=DIRECTION ( 'NONE',  ( 0.01091231665325478536, -0.06889765579810422369, -0.9975640502598241977 ) ) ;
#10641=ORIENTED_EDGE ( 'NONE', *, *, #25470, .F. ) ;
#10645=CARTESIAN_POINT ( 'NONE',  ( 45.20352061843870217, -33.45237892079950370, -34.80811307016849554 ) ) ;
#10650=B_SPLINE_CURVE_WITH_KNOTS ( 'NONE', 3,
 ( #9900, #25857, #50517, #14608, #23219, #30575, #46856, #34238 ),
 .UNSPECIFIED., .F., .F.,
 ( 4, 2, 2, 4 ),
 ( 0.05028014561811239985, 0.06097673919894460587, 0.07774712209420850395, 0.08013618654967340216 ),
 .UNSPECIFIED. ) ;
#10657=CARTESIAN_POINT ( 'NONE',  ( 11.63393739769602320, 10.38381105532059934, -35.01561944896759826 ) ) ;
#10659=EDGE_CURVE ( 'NONE', #15707, #11818, #34135, .T. ) ;
#10663=EDGE_CURVE ( 'NONE', #27942, #49694, #11498, .T. ) ;
#10665=CARTESIAN_POINT ( 'NONE',  ( 44.85304072945612575, -40.02002747739808797, -62.52602019059866478 ) ) ;
#10667=( BOUNDED_CURVE ( )  B_SPLINE_CURVE ( 3, ( #20068, #36309, #9070, #16663 ),
 .UNSPECIFIED., .F., .T. ) 
 B_SPLINE_CURVE_WITH_KNOTS ( ( 4, 4 ),
 ( 0.3056162491274368453, 0.3752708228560562298 ),
 .UNSPECIFIED. ) 
 CURVE ( )  GEOMETRIC_REPRESENTATION_ITEM ( )  RATIONAL_B_SPLINE_CURVE ( ( 1.000000000000000000, 0.9995957275622165961, 0.9995957275622165961, 1.000000000000000000 ) ) 
 REPRESENTATION_ITEM ( '' )  );
#10682=DIRECTION ( 'NONE',  ( -1.000000000000000000, 0.000000000000000000, 0.000000000000000000 ) ) ;
#10683=CARTESIAN_POINT ( 'NONE',  ( 14.63288374505910028, 0.9265147500385738644, -34.64999999999999858 ) ) ;
#10686=CARTESIAN_POINT ( 'NONE',  ( 16.13393739769620083, -1.759782484128330049, -35.14999999999999858 ) ) ;
#10687=DIRECTION ( 'NONE',  ( 0.000000000000000000, -1.000000000000000000, 0.000000000000000000 ) ) ;
#10688=ORIENTED_EDGE ( 'NONE', *, *, #16903, .T. ) ;
#10692=CARTESIAN_POINT ( 'NONE',  ( 16.13393739769620083, -15.61618894467929941, -35.02873218748179340 ) ) ;
#10693=DIRECTION ( 'NONE',  ( -0.3863301728269175062, -0.9223605572462019175, 3.330669073875470114E-16 ) ) ;
#10695=ORIENTED_EDGE ( 'NONE', *, *, #33201, .T. ) ;
#10709=ORIENTED_EDGE ( 'NONE', *, *, #22346, .F. ) ;
#10711=DIRECTION ( 'NONE',  ( 0.000000000000000000, 0.000000000000000000, 1.000000000000000000 ) ) ;
#10718=CIRCLE ( 'NONE', #31593, 34.41780050634729804 ) ;
#10720=FACE_OUTER_BOUND ( 'NONE', #33360, .T. ) ;
#10721=ORIENTED_EDGE ( 'NONE', *, *, #14122, .F. ) ;
#10737=ORIENTED_EDGE ( 'NONE', *, *, #5067, .F. ) ;
#10740=CARTESIAN_POINT ( 'NONE',  ( 40.80250930014859279, 8.415445928904281558, -82.01417162886387757 ) ) ;
#10748=LINE ( 'NONE', #50837, #13121 ) ;
#10749=EDGE_LOOP ( 'NONE', ( #30352, #35044, #17065, #23477 ) ) ;
#10759=CARTESIAN_POINT ( 'NONE',  ( 19.40270147970599979, -49.11618894467930829, -34.64999999999999858 ) ) ;
#10761=AXIS2_PLACEMENT_3D ( 'NONE', #28729, #44730, #1486 ) ;
#10764=CYLINDRICAL_SURFACE ( 'NONE', #19268, 0.4999999999999967248 ) ;
#10765=ORIENTED_EDGE ( 'NONE', *, *, #11492, .T. ) ;
#10770=CARTESIAN_POINT ( 'NONE',  ( 3.892469389394924484, -8.548574094810398094, -34.70142521051216278 ) ) ;
#10775=CARTESIAN_POINT ( 'NONE',  ( 16.13393739769620083, -15.61618894467929941, -54.64999999999999858 ) ) ;
#10779=EDGE_CURVE ( 'NONE', #51599, #6854, #49207, .T. ) ;
#10782=CARTESIAN_POINT ( 'NONE',  ( 43.33111814803011441, -37.82550818684872240, -73.66403162998959431 ) ) ;
#10787=EDGE_CURVE ( 'NONE', #16095, #6632, #548, .T. ) ;
#10792=CARTESIAN_POINT ( 'NONE',  ( 14.14886614762350092, -32.59522544870679894, -35.02873218748179340 ) ) ;
#10801=CARTESIAN_POINT ( 'NONE',  ( 41.55168008675715896, -39.71505707655544626, -78.49431477701308779 ) ) ;
#10819=CARTESIAN_POINT ( 'NONE',  ( 18.08251218718420716, 10.43523626583289321, -34.89146800830123851 ) ) ;
#10826=ORIENTED_EDGE ( 'NONE', *, *, #1873, .F. ) ;
#10829=ORIENTED_EDGE ( 'NONE', *, *, #38391, .F. ) ;
#10832=CARTESIAN_POINT ( 'NONE',  ( 0.6614253361915152229, -8.772027323367371565, -34.75586992539665943 ) ) ;
#10837=DIRECTION ( 'NONE',  ( 0.000000000000000000, 0.000000000000000000, -1.000000000000000000 ) ) ;
#10839=CARTESIAN_POINT ( 'NONE',  ( 44.10370407306162832, 6.698676713549935435, -69.80110960494087635 ) ) ;
#10842=AXIS2_PLACEMENT_3D ( 'NONE', #28631, #24166, #8737 ) ;
#10843=EDGE_CURVE ( 'NONE', #36140, #15955, #44479, .T. ) ;
#10854=CARTESIAN_POINT ( 'NONE',  ( 27.13393739769620083, 7.383811055320659733, -59.64999999999999147 ) ) ;
#10858=CARTESIAN_POINT ( 'NONE',  ( 12.86517331568619937, 17.88381105532060289, -34.64999999999999858 ) ) ;
#10861=CARTESIAN_POINT ( 'NONE',  ( 31.79224979287389985, 4.883811055320679273, -84.65000000000000568 ) ) ;
#10864=TOROIDAL_SURFACE ( 'NONE', #39288, 31.45861873485090143, 3.000000000000000000 ) ;
#10894=CARTESIAN_POINT ( 'NONE',  ( 29.13393739769619728, 1.883811055320659955, -53.85091742636659973 ) ) ;
#10911=CIRCLE ( 'NONE', #15090, 2.999999999999998668 ) ;
#10912=CARTESIAN_POINT ( 'NONE',  ( 38.67452568954060155, 6.328436186825659782, -84.65000000000000568 ) ) ;
#10923=CARTESIAN_POINT ( 'NONE',  ( 44.44775996439803123, -39.99043000850869589, -64.48947138781548460 ) ) ;
#10942=CARTESIAN_POINT ( 'NONE',  ( 40.83956339042367745, 8.397827017939304639, -81.92924210665236728 ) ) ;
#10949=ORIENTED_EDGE ( 'NONE', *, *, #2592, .F. ) ;
#10952=EDGE_LOOP ( 'NONE', ( #25387, #45096, #2433, #6246 ) ) ;
#10954=DIRECTION ( 'NONE',  ( -1.000000000000000000, 0.000000000000000000, 0.000000000000000000 ) ) ;
#10959=ADVANCED_FACE ( 'NONE', ( #46306 ), #10634, .T. ) ;
#10969=ORIENTED_EDGE ( 'NONE', *, *, #31014, .T. ) ;
#10979=( BOUNDED_CURVE ( )  B_SPLINE_CURVE ( 2, ( #11855, #36439, #43809 ),
 .UNSPECIFIED., .F., .T. ) 
 B_SPLINE_CURVE_WITH_KNOTS ( ( 3, 3 ),
 ( -1.071465066616890116, -0.1016765296687800468 ),
 .UNSPECIFIED. ) 
 CURVE ( )  GEOMETRIC_REPRESENTATION_ITEM ( )  RATIONAL_B_SPLINE_CURVE ( ( 1.000064779730289954, 1.000064447938610046, 1.000011648212760118 ) ) 
 REPRESENTATION_ITEM ( '' )  );
#10981=VECTOR ( 'NONE', #6451, 1000.000000000000114 ) ;
#10983=CARTESIAN_POINT ( 'NONE',  ( 46.67455644844360307, -39.87048571057250257, -54.56212092059809748 ) ) ;
#10984=AXIS2_PLACEMENT_3D ( 'NONE', #19059, #10693, #19832 ) ;
#10988=CARTESIAN_POINT ( 'NONE',  ( 23.60377752213929980, 17.56341275872070185, -34.96018206680729890 ) ) ;
#10992=CARTESIAN_POINT ( 'NONE',  ( -15.89903062800279976, 7.092556714909539650, -48.83602070084049984 ) ) ;
#10995=CARTESIAN_POINT ( 'NONE',  ( 33.38393739769599478, 10.88381105532080007, -35.14999999999999858 ) ) ;
#11000=CARTESIAN_POINT ( 'NONE',  ( 39.73155014768870785, 8.662390057901488305, -85.55364038000607252 ) ) ;
#11003=CARTESIAN_POINT ( 'NONE',  ( 47.13393739769619373, -39.28050807707769820, -35.08812023096449906 ) ) ;
#11010=ORIENTED_EDGE ( 'NONE', *, *, #43328, .T. ) ;
#11021=ORIENTED_EDGE ( 'NONE', *, *, #12703, .T. ) ;
#11026=VERTEX_POINT ( 'NONE', #49402 ) ;
#11035=CARTESIAN_POINT ( 'NONE',  ( 0.3209249304026170480, -20.69829881652800196, -34.64999999999999858 ) ) ;
#11051=B_SPLINE_CURVE_WITH_KNOTS ( 'NONE', 3,
 ( #44956, #9057, #4341, #25006, #24751, #20308, #21091, #36048, #41021, #20829 ),
 .UNSPECIFIED., .F., .F.,
 ( 4, 2, 2, 2, 4 ),
 ( -0.0004281134594814769946, 0.000000000000000000, 0.02012916873241540200, 0.03942875605163800173, 0.05028014561794270920 ),
 .UNSPECIFIED. ) ;
#11074=DIRECTION ( 'NONE',  ( 0.000000000000000000, 0.000000000000000000, 1.000000000000000000 ) ) ;
#11086=DIRECTION ( 'NONE',  ( 0.000000000000000000, 0.7071067811865463515, -0.7071067811865487940 ) ) ;
#11099=VECTOR ( 'NONE', #43515, 999.9999999999998863 ) ;
#11101=CARTESIAN_POINT ( 'NONE',  ( 44.41528266476777986, 6.738903454959987549, -68.24327111710597649 ) ) ;
#11105=DIRECTION ( 'NONE',  ( -0.8090169943749478954, -0.5877852522924724710, 0.000000000000000000 ) ) ;
#11111=CARTESIAN_POINT ( 'NONE',  ( -1.143840380081567076, -15.61618894467929941, -35.76111111111109864 ) ) ;
#11141=DIRECTION ( 'NONE',  ( 0.7071067811865475727, 0.7071067811865475727, 0.000000000000000000 ) ) ;
#11143=CARTESIAN_POINT ( 'NONE',  ( 46.39995713829783597, 8.883003650160496534, -55.01640863334984033 ) ) ;
#11153=CARTESIAN_POINT ( 'NONE',  ( 47.13393739769619373, 8.048130187719129580, -35.14999999999999858 ) ) ;
#11155=CARTESIAN_POINT ( 'NONE',  ( -17.31035082052260776, -35.95763326800162929, -50.10886653532376300 ) ) ;
#11156=VERTEX_POINT ( 'NONE', #34613 ) ;
#11158=VERTEX_POINT ( 'NONE', #19153 ) ;
#11159=DIRECTION ( 'NONE',  ( -1.000000000000000000, 0.000000000000000000, 0.000000000000000000 ) ) ;
#11160=CARTESIAN_POINT ( 'NONE',  ( 45.34362094574520086, -33.92716053989970248, -34.64999999999999858 ) ) ;
#11163=CARTESIAN_POINT ( 'NONE',  ( 44.69938546025573345, 1.937554778470574446, -44.09236103973196919 ) ) ;
#11170=CARTESIAN_POINT ( 'NONE',  ( 18.13393739769620083, -49.55731444163359356, -34.64999999999999858 ) ) ;
#11174=DIRECTION ( 'NONE',  ( -0.3502816565540492477, 0.000000000000000000, 0.9366444154970182678 ) ) ;
#11179=CIRCLE ( 'NONE', #8655, 5.251829701412229490 ) ;
#11182=CARTESIAN_POINT ( 'NONE',  ( 45.07384444018408942, -40.03565744828185302, -61.45441968810736455 ) ) ;
#11185=DIRECTION ( 'NONE',  ( -0.7071067811865492381, 0.000000000000000000, 0.7071067811865457964 ) ) ;
#11202=DIRECTION ( 'NONE',  ( 0.000000000000000000, 0.000000000000000000, 1.000000000000000000 ) ) ;
#11208=ORIENTED_EDGE ( 'NONE', *, *, #47734, .T. ) ;
#11224=VERTEX_POINT ( 'NONE', #18094 ) ;
#11228=PLANE ( 'NONE',  #6077 ) ;
#11239=CARTESIAN_POINT ( 'NONE',  ( 46.85975247610159755, -39.63543722116869361, -54.33484572181019701 ) ) ;
#11240=VERTEX_POINT ( 'NONE', #9693 ) ;
#11243=DIRECTION ( 'NONE',  ( 0.000000000000000000, 0.000000000000000000, -1.000000000000000000 ) ) ;
#11255=ORIENTED_EDGE ( 'NONE', *, *, #44437, .F. ) ;
#11258=CARTESIAN_POINT ( 'NONE',  ( 45.05343097613845771, 6.588082144191076850, -65.00781254588196134 ) ) ;
#11270=ORIENTED_EDGE ( 'NONE', *, *, #26536, .F. ) ;
#11287=( BOUNDED_CURVE ( )  B_SPLINE_CURVE ( 3, ( #22069, #10819, #6624, #42013 ),
 .UNSPECIFIED., .F., .T. ) 
 B_SPLINE_CURVE_WITH_KNOTS ( ( 4, 4 ),
 ( 5.497787143782005614, 6.283185307179586232 ),
 .UNSPECIFIED. ) 
 CURVE ( )  GEOMETRIC_REPRESENTATION_ITEM ( )  RATIONAL_B_SPLINE_CURVE ( ( 1.000000000000000000, 0.9492530216741742466, 0.9492530216741742466, 1.000000000000000000 ) ) 
 REPRESENTATION_ITEM ( '' )  );
#11296=DIRECTION ( 'NONE',  ( 0.000000000000000000, -1.000000000000000000, 0.000000000000000000 ) ) ;
#11297=CARTESIAN_POINT ( 'NONE',  ( 46.74119668981005304, -38.22629118898348111, -56.61365389520171476 ) ) ;
#11317=CARTESIAN_POINT ( 'NONE',  ( 20.47328261930381643, 10.62527906362196717, -34.70142521051216988 ) ) ;
#11322=CARTESIAN_POINT ( 'NONE',  ( 23.49471107959579896, 17.21388800241559736, -41.74835363994539961 ) ) ;
#11330=DIRECTION ( 'NONE',  ( 0.000000000000000000, -1.000000000000000000, 0.000000000000000000 ) ) ;
#11331=CARTESIAN_POINT ( 'NONE',  ( -0.2240635586800976686, -45.43677584701738681, -34.96139953375227805 ) ) ;
#11336=LINE ( 'NONE', #39626, #33587 ) ;
#11343=ORIENTED_EDGE ( 'NONE', *, *, #37973, .T. ) ;
#11347=DIRECTION ( 'NONE',  ( 0.000000000000000000, 0.000000000000000000, 1.000000000000000000 ) ) ;
#11353=CARTESIAN_POINT ( 'NONE',  ( 44.20159454932027643, 6.711260822063675135, -69.31168125965361071 ) ) ;
#11360=( LENGTH_UNIT ( ) NAMED_UNIT ( * ) SI_UNIT ( .MILLI., .METRE. ) );
#11361=ADVANCED_FACE ( 'NONE', ( #6803 ), #14911, .T. ) ;
#11363=B_SPLINE_CURVE_WITH_KNOTS ( 'NONE', 3,
 ( #27281, #43290, #7379, #23328, #39353, #3452, #28293, #782, #13132, #20433, #29082, #40882, #45078, #36679, #12333, #9188, #25140, #20955 ),
 .UNSPECIFIED., .F., .F.,
 ( 4, 2, 2, 2, 2, 2, 2, 2, 4 ),
 ( 0.000000000000000000, 0.2499999999999950595, 0.3749999999999915623, 0.4374999999999900080, 0.4687499999999898970, 0.4999999999999897859, 0.6249999999999922284, 0.7499999999999945599, 1.000000000000000000 ),
 .UNSPECIFIED. ) ;
#11368=CARTESIAN_POINT ( 'NONE',  ( 17.98749078828947745, -41.76263555408611694, -34.79644660940672907 ) ) ;
#11370=EDGE_CURVE ( 'NONE', #48656, #32778, #29205, .T. ) ;
#11372=DIRECTION ( 'NONE',  ( 0.5516667872527503125, -0.8340645993220362486, 0.000000000000000000 ) ) ;
#11374=ADVANCED_FACE ( 'NONE', ( #32408 ), #36111, .T. ) ;
#11378=ORIENTED_EDGE ( 'NONE', *, *, #20506, .T. ) ;
#11384=LINE ( 'NONE', #44365, #49098 ) ;
#11385=DIRECTION ( 'NONE',  ( -0.9876883405951387696, -0.1564344650402249015, 0.000000000000000000 ) ) ;
#11391=CYLINDRICAL_SURFACE ( 'NONE', #14048, 2.000000000000000000 ) ;
#11404=CARTESIAN_POINT ( 'NONE',  ( 45.86779753676328397, 8.854011588677400013, -57.59996879060989272 ) ) ;
#11408=ORIENTED_EDGE ( 'NONE', *, *, #38654, .T. ) ;
#11410=AXIS2_PLACEMENT_3D ( 'NONE', #51499, #3285, #19000 ) ;
#11411=ORIENTED_EDGE ( 'NONE', *, *, #13957, .T. ) ;
#11429=AXIS2_PLACEMENT_3D ( 'NONE', #35092, #39557, #51093 ) ;
#11434=CARTESIAN_POINT ( 'NONE',  ( 0.7461747575532640120, -22.48794087071790315, -34.70985242058460329 ) ) ;
#11445=CARTESIAN_POINT ( 'NONE',  ( 45.82950911773824032, -40.08398659257233732, -57.78639530639727440 ) ) ;
#11451=AXIS2_PLACEMENT_3D ( 'NONE', #50179, #30499, #14788 ) ;
#11454=ORIENTED_EDGE ( 'NONE', *, *, #33456, .T. ) ;
#11462=DIRECTION ( 'NONE',  ( 0.3535533905932784493, 0.6123724356957970238, 0.7071067811865430208 ) ) ;
#11464=FACE_OUTER_BOUND ( 'NONE', #19895, .T. ) ;
#11465=ADVANCED_FACE ( 'NONE', ( #46784 ), #26838, .T. ) ;
#11466=CARTESIAN_POINT ( 'NONE',  ( 29.24327964038718619, 4.516725609936003139, -84.62771067598525576 ) ) ;
#11470=EDGE_CURVE ( 'NONE', #50723, #11026, #45132, .T. ) ;
#11480=DIRECTION ( 'NONE',  ( 0.4743737082415266926, 0.8803235683140505641, 0.000000000000000000 ) ) ;
#11481=CARTESIAN_POINT ( 'NONE',  ( 21.68571409299283559, 1.614639264107643246, -34.79644660940672907 ) ) ;
#11487=EDGE_LOOP ( 'NONE', ( #45954, #49086, #16890, #39999, #13486 ) ) ;
#11491=CARTESIAN_POINT ( 'NONE',  ( 46.63393739769619373, 4.883811055320659733, -35.14999999999999858 ) ) ;
#11492=EDGE_CURVE ( 'NONE', #218, #50974, #22806, .T. ) ;
#11498=LINE ( 'NONE', #51325, #16483 ) ;
#11511=DIRECTION ( 'NONE',  ( -0.1961161351381840723, -2.837236618486510447E-16, -0.9805806756909202226 ) ) ;
#11513=CARTESIAN_POINT ( 'NONE',  ( 44.59825589618289854, -37.91486344825149502, -67.32301989359220329 ) ) ;
#11519=CARTESIAN_POINT ( 'NONE',  ( 46.53888375069291783, 7.993794312659110446, -58.14357038517931642 ) ) ;
#11522=DIRECTION ( 'NONE',  ( 0.000000000000000000, 0.000000000000000000, 1.000000000000000000 ) ) ;
#11527=DIRECTION ( 'NONE',  ( 0.000000000000000000, -1.000000000000000000, 0.000000000000000000 ) ) ;
#11528=EDGE_CURVE ( 'NONE', #45454, #22924, #22896, .T. ) ;
#11529=ORIENTED_EDGE ( 'NONE', *, *, #49237, .T. ) ;
#11531=ORIENTED_EDGE ( 'NONE', *, *, #47912, .F. ) ;
#11551=AXIS2_PLACEMENT_3D ( 'NONE', #15939, #27721, #47656 ) ;
#11564=CARTESIAN_POINT ( 'NONE',  ( 2.404741263826640107, -5.380232784273969671, -35.14999999999999858 ) ) ;
#11576=CARTESIAN_POINT ( 'NONE',  ( 22.35126475695520298, 22.42506970168830094, -34.65028073423250277 ) ) ;
#11581=VECTOR ( 'NONE', #10, 999.9999999999998863 ) ;
#11594=( BOUNDED_CURVE ( )  B_SPLINE_CURVE ( 3, ( #40151, #48022, #27063, #3227 ),
 .UNSPECIFIED., .F., .T. ) 
 B_SPLINE_CURVE_WITH_KNOTS ( ( 4, 4 ),
 ( 2.117032425727450207, 2.581755039733875101 ),
 .UNSPECIFIED. ) 
 CURVE ( )  GEOMETRIC_REPRESENTATION_ITEM ( )  RATIONAL_B_SPLINE_CURVE ( ( 1.000000000000000000, 0.9820835707424604433, 0.9820835707424604433, 1.000000000000000000 ) ) 
 REPRESENTATION_ITEM ( '' )  );
#11607=LINE ( 'NONE', #8444, #23508 ) ;
#11609=VERTEX_POINT ( 'NONE', #13764 ) ;
#11611=CARTESIAN_POINT ( 'NONE',  ( 43.70384182385213023, 6.645243339508008162, -71.80047792273670382 ) ) ;
#11615=CARTESIAN_POINT ( 'NONE',  ( 45.30944071664330153, 2.566574815035449930, -34.65725502031740035 ) ) ;
#11618=( NAMED_UNIT ( * ) PLANE_ANGLE_UNIT ( ) SI_UNIT ( $, .RADIAN. ) );
#11632=CARTESIAN_POINT ( 'NONE',  ( 4.082512187184039298, -8.658295355271496518, -34.89146800830128115 ) ) ;
#11645=CARTESIAN_POINT ( 'NONE',  ( 0.3198710486850440127, 15.01731126982059905, -34.64999999999999858 ) ) ;
#11647=CARTESIAN_POINT ( 'NONE',  ( -0.2088566477600920512, -20.53519877086888812, -34.94807878368268206 ) ) ;
#11667=VERTEX_POINT ( 'NONE', #30246 ) ;
#11673=ORIENTED_EDGE ( 'NONE', *, *, #39102, .F. ) ;
#11674=DIRECTION ( 'NONE',  ( 0.000000000000000000, 0.000000000000000000, -1.000000000000000000 ) ) ;
#11684=AXIS2_PLACEMENT_3D ( 'NONE', #26052, #26316, #18978 ) ;
#11692=ORIENTED_EDGE ( 'NONE', *, *, #47921, .F. ) ;
#11695=AXIS2_PLACEMENT_3D ( 'NONE', #22130, #18474, #34707 ) ;
#11697=CARTESIAN_POINT ( 'NONE',  ( 42.31941830961962836, -39.79865067521480881, -74.78800917364183931 ) ) ;
#11703=CARTESIAN_POINT ( 'NONE',  ( 33.13393739769620083, -38.61618894467930119, -59.64999999999999147 ) ) ;
#11707=ORIENTED_EDGE ( 'NONE', *, *, #4519, .F. ) ;
#11710=DIRECTION ( 'NONE',  ( 0.000000000000000000, 0.000000000000000000, -1.000000000000000000 ) ) ;
#11716=CARTESIAN_POINT ( 'NONE',  ( 41.73102901179257174, 8.502924699651416063, -77.62876425794036095 ) ) ;
#11717=DIRECTION ( 'NONE',  ( 0.000000000000000000, 0.000000000000000000, -1.000000000000000000 ) ) ;
#11719=CARTESIAN_POINT ( 'NONE',  ( 16.13393739769620083, -15.61618894467929941, -35.14999999999999858 ) ) ;
#11722=CARTESIAN_POINT ( 'NONE',  ( 0.07409199189653030426, 19.67928630151580194, -34.73152237081639981 ) ) ;
#11723=ORIENTED_EDGE ( 'NONE', *, *, #9284, .F. ) ;
#11724=VECTOR ( 'NONE', #17490, 1000.000000000000114 ) ;
#11725=ORIENTED_EDGE ( 'NONE', *, *, #17544, .F. ) ;
#11744=( BOUNDED_CURVE ( )  B_SPLINE_CURVE ( 2, ( #51755, #12185, #11937 ),
 .UNSPECIFIED., .F., .T. ) 
 B_SPLINE_CURVE_WITH_KNOTS ( ( 3, 3 ),
 ( 0.09013418061657679781, 2.097305204681399804 ),
 .UNSPECIFIED. ) 
 CURVE ( )  GEOMETRIC_REPRESENTATION_ITEM ( )  RATIONAL_B_SPLINE_CURVE ( ( 1.000760730681520050, 1.008874108821600002, 1.001093714212740071 ) ) 
 REPRESENTATION_ITEM ( '' )  );
#11746=B_SPLINE_CURVE_WITH_KNOTS ( 'NONE', 3,
 ( #48399, #33431, #49451, #12497, #44987, #28467, #24516, #28722, #24780, #4890, #19746, #19989, #48307, #48055, #12402, #28366, #40184, #24162, #44117, #24422, #23397, #4276, #7713, #39420, #44372 ),
 .UNSPECIFIED., .F., .F.,
 ( 4, 2, 2, 1, 1, 2, 2, 2, 2, 1, 1, 1, 2, 2, 4 ),
 ( 0.000000000000000000, 0.1250000000000000555, 0.1875000000000000833, 0.2187499999999996669, 0.2343749999999998890, 0.2421875000000003886, 0.2500000000000008882, 0.4999999999999942824, 0.6249999999999908962, 0.6874999999999883427, 0.7187499999999870104, 0.7343749999999861222, 0.7421874999999865663, 0.7499999999999870104, 1.000000000000000000 ),
 .UNSPECIFIED. ) ;
#11753=DIRECTION ( 'NONE',  ( 0.1961161351381840723, -2.713878504639270283E-16, 0.9805806756909202226 ) ) ;
#11755=CARTESIAN_POINT ( 'NONE',  ( 8.830271178172500512, 17.88421590754769852, -34.68023162149810190 ) ) ;
#11770=CIRCLE ( 'NONE', #32638, 7.000000000000000000 ) ;
#11774=CARTESIAN_POINT ( 'NONE',  ( 45.97697684862929890, -38.03835002546479416, -60.42395416268509933 ) ) ;
#11779=ORIENTED_EDGE ( 'NONE', *, *, #30909, .T. ) ;
#11780=CARTESIAN_POINT ( 'NONE',  ( 41.46338495793718693, 7.445976544050517454, -83.29850773724480462 ) ) ;
#11783=DIRECTION ( 'NONE',  ( -1.000000000000000000, 0.000000000000000000, 0.000000000000000000 ) ) ;
#11807=VERTEX_POINT ( 'NONE', #34379 ) ;
#11816=CARTESIAN_POINT ( 'NONE',  ( 46.08014022084859818, -38.16162640463598166, -59.91892963968066255 ) ) ;
#11818=VERTEX_POINT ( 'NONE', #50391 ) ;
#11821=ADVANCED_FACE ( 'NONE', ( #34636 ), #38599, .T. ) ;
#11822=CARTESIAN_POINT ( 'NONE',  ( 12.86517331568640010, -49.11618894467930829, -34.64999999999999858 ) ) ;
#11852=CYLINDRICAL_SURFACE ( 'NONE', #51829, 0.4999999999999967248 ) ;
#11853=CARTESIAN_POINT ( 'NONE',  ( -0.1032157185578773950, -45.55972716908853926, -34.85600551168373329 ) ) ;
#11855=CARTESIAN_POINT ( 'NONE',  ( -11.80944000494479873, 2.826328597561450273, -45.03554556751399929 ) ) ;
#11857=CARTESIAN_POINT ( 'NONE',  ( 33.13393739769620083, -15.61618894467929941, -84.65000000000000568 ) ) ;
#11865=VERTEX_POINT ( 'NONE', #29669 ) ;
#11867=CARTESIAN_POINT ( 'NONE',  ( 11.63393739769600010, 10.38381105532060111, -54.64999999999999858 ) ) ;
#11870=ORIENTED_EDGE ( 'NONE', *, *, #33759, .F. ) ;
#11872=CARTESIAN_POINT ( 'NONE',  ( 0.9903310742082500617, -8.665933549137170289, -34.65032322548090349 ) ) ;
#11874=ORIENTED_EDGE ( 'NONE', *, *, #3799, .T. ) ;
#11876=CARTESIAN_POINT ( 'NONE',  ( 44.17051537087078117, 6.707271543636243116, -69.46706789229442336 ) ) ;
#11895=ORIENTED_EDGE ( 'NONE', *, *, #20981, .F. ) ;
#11908=ADVANCED_FACE ( 'NONE', ( #33860 ), #29922, .T. ) ;
#11914=EDGE_CURVE ( 'NONE', #7747, #13116, #4066, .T. ) ;
#11915=AXIS2_PLACEMENT_3D ( 'NONE', #32628, #28977, #4881 ) ;
#11917=PLANE ( 'NONE',  #20351 ) ;
#11923=DIRECTION ( 'NONE',  ( -0.1961161351381836004, -1.134894647394604573E-15, -0.9805806756909204447 ) ) ;
#11926=VERTEX_POINT ( 'NONE', #39877 ) ;
#11933=VERTEX_POINT ( 'NONE', #31213 ) ;
#11937=CARTESIAN_POINT ( 'NONE',  ( 18.13393739769630031, 1.391621760993470014, -35.14999999999999858 ) ) ;
#11939=ORIENTED_EDGE ( 'NONE', *, *, #23058, .T. ) ;
#11942=LINE ( 'NONE', #31308, #16322 ) ;
#11943=EDGE_CURVE ( 'NONE', #24151, #425, #12976, .T. ) ;
#11957=CARTESIAN_POINT ( 'NONE',  ( 42.59271315789397505, -39.82626481978887512, -73.46854499661243665 ) ) ;
#11958=CARTESIAN_POINT ( 'NONE',  ( 46.63393739769619373, 7.878491304262099426, -34.64999999999999858 ) ) ;
#11962=LINE ( 'NONE', #32607, #46568 ) ;
#11963=AXIS2_PLACEMENT_3D ( 'NONE', #8915, #517, #16505 ) ;
#11968=EDGE_LOOP ( 'NONE', ( #48302, #46330, #46112, #41091 ) ) ;
#11970=DIRECTION ( 'NONE',  ( -1.000000000000000000, 0.000000000000000000, 0.000000000000000000 ) ) ;
#11971=ORIENTED_EDGE ( 'NONE', *, *, #43304, .T. ) ;
#11975=FACE_OUTER_BOUND ( 'NONE', #242, .T. ) ;
#11976=CARTESIAN_POINT ( 'NONE',  ( 41.47362262140879352, 8.473564071847876633, -78.87161307600275961 ) ) ;
#11978=CARTESIAN_POINT ( 'NONE',  ( 30.03825186937055136, 4.383319667191443614, -84.60795687872310111 ) ) ;
#11981=CARTESIAN_POINT ( 'NONE',  ( 18.13393739769620083, -37.52509124488599923, -54.64999999999999858 ) ) ;
#11982=ORIENTED_EDGE ( 'NONE', *, *, #4771, .F. ) ;
#11983=ORIENTED_EDGE ( 'NONE', *, *, #5257, .F. ) ;
#11991=DIRECTION ( 'NONE',  ( 0.000000000000000000, 0.000000000000000000, 1.000000000000000000 ) ) ;
#12012=CARTESIAN_POINT ( 'NONE',  ( 46.50679657349800067, -40.08028361939490480, -54.64999999999999858 ) ) ;
#12028=FACE_OUTER_BOUND ( 'NONE', #14354, .T. ) ;
#12031=ORIENTED_EDGE ( 'NONE', *, *, #14057, .F. ) ;
#12033=ORIENTED_EDGE ( 'NONE', *, *, #6621, .F. ) ;
#12034=CARTESIAN_POINT ( 'NONE',  ( 43.68113622443509314, 6.447734790222596324, -71.88154124489368257 ) ) ;
#12036=DIRECTION ( 'NONE',  ( 0.000000000000000000, 0.000000000000000000, -1.000000000000000000 ) ) ;
#12043=EDGE_LOOP ( 'NONE', ( #47705, #40848, #29163, #48593 ) ) ;
#12049=( BOUNDED_CURVE ( )  B_SPLINE_CURVE ( 2, ( #28403, #44409, #40994 ),
 .UNSPECIFIED., .F., .T. ) 
 B_SPLINE_CURVE_WITH_KNOTS ( ( 3, 3 ),
 ( 0.09013418064983300115, 2.097305204717760052 ),
 .UNSPECIFIED. ) 
 CURVE ( )  GEOMETRIC_REPRESENTATION_ITEM ( )  RATIONAL_B_SPLINE_CURVE ( ( 1.000760730674089993, 1.008874108731790065, 1.001093714201390039 ) ) 
 REPRESENTATION_ITEM ( '' )  );
#12054=ORIENTED_EDGE ( 'NONE', *, *, #21655, .T. ) ;
#12067=DIRECTION ( 'NONE',  ( 0.000000000000000000, 0.000000000000000000, 1.000000000000000000 ) ) ;
#12068=DIRECTION ( 'NONE',  ( 0.000000000000000000, 0.000000000000000000, 1.000000000000000000 ) ) ;
#12069=CARTESIAN_POINT ( 'NONE',  ( 44.94022070389028300, 1.883811055320663064, -54.43277924001891677 ) ) ;
#12073=EDGE_CURVE ( 'NONE', #13190, #11926, #46809, .T. ) ;
#12078=VECTOR ( 'NONE', #23492, 1000.000000000000000 ) ;
#12080=CYLINDRICAL_SURFACE ( 'NONE', #1660, 0.4999999999999994449 ) ;
#12081=DIRECTION ( 'NONE',  ( 0.000000000000000000, 0.000000000000000000, 1.000000000000000000 ) ) ;
#12086=DIRECTION ( 'NONE',  ( 0.000000000000000000, 0.000000000000000000, -1.000000000000000000 ) ) ;
#12091=ORIENTED_EDGE ( 'NONE', *, *, #20306, .T. ) ;
#12100=CARTESIAN_POINT ( 'NONE',  ( -0.007164427059776000244, -45.70803162167019451, -34.77269723891829756 ) ) ;
#12102=DIRECTION ( 'NONE',  ( 0.000000000000000000, 0.000000000000000000, 1.000000000000000000 ) ) ;
#12104=DIRECTION ( 'NONE',  ( 0.000000000000000000, 0.000000000000000000, -1.000000000000000000 ) ) ;
#12108=CARTESIAN_POINT ( 'NONE',  ( 2.558369240368420172, -25.18609768228349921, -34.64999999999999858 ) ) ;
#12117=CARTESIAN_POINT ( 'NONE',  ( 13.05521822061467319, 18.23736444591386174, -34.79644660940673617 ) ) ;
#12123=DIRECTION ( 'NONE',  ( 0.7071067811865457964, -0.7071067811865492381, 0.000000000000000000 ) ) ;
#12124=CARTESIAN_POINT ( 'NONE',  ( 17.63499105033400127, 0.9265147500389789847, -34.64999999999999858 ) ) ;
#12127=CARTESIAN_POINT ( 'NONE',  ( 45.16599383043609350, 2.109473049736759975, -34.94655432540119477 ) ) ;
#12128=CONICAL_SURFACE ( 'NONE', #17985, 3.567506086244481622, 0.04995839572194331335 ) ;
#12133=EDGE_CURVE ( 'NONE', #15707, #22659, #7495, .T. ) ;
#12145=AXIS2_PLACEMENT_3D ( 'NONE', #31432, #51638, #15732 ) ;
#12151=ORIENTED_EDGE ( 'NONE', *, *, #37263, .F. ) ;
#12152=FACE_OUTER_BOUND ( 'NONE', #17410, .T. ) ;
#12159=FACE_OUTER_BOUND ( 'NONE', #8619, .T. ) ;
#12162=CARTESIAN_POINT ( 'NONE',  ( -0.05506254389775910169, -20.75690083494706428, -34.81434777529929647 ) ) ;
#12165=CARTESIAN_POINT ( 'NONE',  ( 20.53650276133967267, 10.53025766472739555, -34.79644660940672907 ) ) ;
#12167=VERTEX_POINT ( 'NONE', #32479 ) ;
#12168=LINE ( 'NONE', #24179, #44298 ) ;
#12180=ORIENTED_EDGE ( 'NONE', *, *, #34150, .T. ) ;
#12185=CARTESIAN_POINT ( 'NONE',  ( 18.13393739769630741, 3.536827986686112091, -43.67210485517633600 ) ) ;
#12186=VERTEX_POINT ( 'NONE', #35287 ) ;
#12198=ORIENTED_EDGE ( 'NONE', *, *, #34412, .T. ) ;
#12202=LINE ( 'NONE', #27911, #2765 ) ;
#12203=UNCERTAINTY_MEASURE_WITH_UNIT (LENGTH_MEASURE( 1.000000000000000082E-05 ), #16920, 'distance_accuracy_value', 'NONE');
#12206=CARTESIAN_POINT ( 'NONE',  ( 43.38138188210033519, -39.90126897775567016, -69.65496977589833705 ) ) ;
#12208=CARTESIAN_POINT ( 'NONE',  ( -0.2865249686166205234, -27.40594838884661044, -35.01561944896768352 ) ) ;
#12216=CARTESIAN_POINT ( 'NONE',  ( 16.13393739769620083, -15.61618894467929941, -54.64999999999999858 ) ) ;
#12218=DIRECTION ( 'NONE',  ( -0.5897727341282554825, -0.3900873262218120252, 0.7071067811865473507 ) ) ;
#12220=CARTESIAN_POINT ( 'NONE',  ( 23.53669455186048864, 17.69319178430572137, -34.79644561402099612 ) ) ;
#12221=CARTESIAN_POINT ( 'NONE',  ( 16.13393739769620083, -15.61618894467929941, -54.64999999999999858 ) ) ;
#12222=CARTESIAN_POINT ( 'NONE',  ( 41.85930995561587764, 8.516901924237213706, -77.01048204870357949 ) ) ;
#12230=ORIENTED_EDGE ( 'NONE', *, *, #22464, .T. ) ;
#12257=ADVANCED_FACE ( 'NONE', ( #34708 ), #50708, .T. ) ;
#12264=ORIENTED_EDGE ( 'NONE', *, *, #31014, .F. ) ;
#12268=CARTESIAN_POINT ( 'NONE',  ( 0.3209249304026240424, 19.48649808507980197, -34.64999999999999858 ) ) ;
#12276=CARTESIAN_POINT ( 'NONE',  ( 19.40270147970599979, -49.11618894467930829, -34.64999999999999858 ) ) ;
#12279=VERTEX_POINT ( 'NONE', #42070 ) ;
#12282=CARTESIAN_POINT ( 'NONE',  ( 41.41169172635818541, 6.152627909148373320, -83.24405656875323700 ) ) ;
#12283=AXIS2_PLACEMENT_3D ( 'NONE', #3656, #11522, #11783 ) ;
#12294=EDGE_CURVE ( 'NONE', #13585, #35594, #9181, .T. ) ;
#12307=CYLINDRICAL_SURFACE ( 'NONE', #39453, 0.4999999999999980571 ) ;
#12333=CARTESIAN_POINT ( 'NONE',  ( 29.92723726607434998, -35.62120283203830695, -84.60891090650764568 ) ) ;
#12337=EDGE_LOOP ( 'NONE', ( #21183, #5575, #43546, #35895 ) ) ;
#12347=CARTESIAN_POINT ( 'NONE',  ( -0.4410626023037830246, -8.356009309619699010, -35.14999999999999858 ) ) ;
#12350=DIRECTION ( 'NONE',  ( -0.4999999999999985567, 0.8660254037844394848, 0.000000000000000000 ) ) ;
#12353=CARTESIAN_POINT ( 'NONE',  ( 11.73137203405252826, -41.76263555408610273, -34.79644660940672196 ) ) ;
#12357=FACE_OUTER_BOUND ( 'NONE', #15484, .T. ) ;
#12359=CIRCLE ( 'NONE', #35779, 17.09468304687040785 ) ;
#12361=EDGE_CURVE ( 'NONE', #11933, #43415, #29252, .T. ) ;
#12367=VERTEX_POINT ( 'NONE', #49940 ) ;
#12370=CARTESIAN_POINT ( 'NONE',  ( 47.13393739769619373, 4.883811055320659733, -54.64999999999999858 ) ) ;
#12371=ORIENTED_EDGE ( 'NONE', *, *, #18096, .F. ) ;
#12374=EDGE_CURVE ( 'NONE', #7271, #31635, #21771, .T. ) ;
#12377=CARTESIAN_POINT ( 'NONE',  ( 45.14919548887390022, 2.061487825409429764, -35.12503119152809461 ) ) ;
#12378=CARTESIAN_POINT ( 'NONE',  ( 42.88323645452967270, -37.76021733457542240, -75.90348433167388009 ) ) ;
#12386=DIRECTION ( 'NONE',  ( -0.1961161351384590468, 0.000000000000000000, -0.9805806756908651556 ) ) ;
#12389=DIRECTION ( 'NONE',  ( 1.000000000000000000, 0.000000000000000000, 0.000000000000000000 ) ) ;
#12402=CARTESIAN_POINT ( 'NONE',  ( 16.63320969315425657, 18.38376875625361251, -83.23984175390957319 ) ) ;
#12411=CARTESIAN_POINT ( 'NONE',  ( -0.2826210738582647375, -20.36873564196809738, -35.01222475787349708 ) ) ;
#12414=ADVANCED_FACE ( 'NONE', ( #46012 ), #10103, .T. ) ;
#12423=ORIENTED_EDGE ( 'NONE', *, *, #47030, .T. ) ;
#12427=ORIENTED_EDGE ( 'NONE', *, *, #7933, .F. ) ;
#12432=VECTOR ( 'NONE', #50538, 1000.000000000000000 ) ;
#12442=LINE ( 'NONE', #12714, #40149 ) ;
#12447=FACE_OUTER_BOUND ( 'NONE', #9623, .T. ) ;
#12458=CARTESIAN_POINT ( 'NONE',  ( 42.98926129872933188, -39.86518172765487122, -71.55095433749755784 ) ) ;
#12461=AXIS2_PLACEMENT_3D ( 'NONE', #7831, #44497, #4656 ) ;
#12462=CIRCLE ( 'NONE', #747, 5.251829701412240148 ) ;
#12471=CARTESIAN_POINT ( 'NONE',  ( 13.13393739769619906, -49.61618894467939356, -35.14999999999999858 ) ) ;
#12475=CARTESIAN_POINT ( 'NONE',  ( 29.13393739769619728, -33.11618894467940066, -81.65000000000000568 ) ) ;
#12477=CARTESIAN_POINT ( 'NONE',  ( 41.45690265626797810, 8.471601390023884903, -78.95241774151945435 ) ) ;
#12478=CARTESIAN_POINT ( 'NONE',  ( 44.66180732667802999, -33.16299454025457294, -44.80531609597240106 ) ) ;
#12482=ORIENTED_EDGE ( 'NONE', *, *, #17451, .T. ) ;
#12486=ORIENTED_EDGE ( 'NONE', *, *, #27241, .T. ) ;
#12497=CARTESIAN_POINT ( 'NONE',  ( 13.99784741310209135, 18.38374537013401522, -83.13257468828133767 ) ) ;
#12502=AXIS2_PLACEMENT_3D ( 'NONE', #44024, #4441, #40091 ) ;
#12517=CARTESIAN_POINT ( 'NONE',  ( 4.082512187184037522, -22.57408253408722132, -34.89146800830128825 ) ) ;
#12526=EDGE_CURVE ( 'NONE', #44367, #24387, #10911, .T. ) ;
#12541=CARTESIAN_POINT ( 'NONE',  ( 0.1457841021255935343, -15.61618894467929941, -34.68167779225149161 ) ) ;
#12550=EDGE_CURVE ( 'NONE', #32837, #21889, #20086, .T. ) ;
#12551=CARTESIAN_POINT ( 'NONE',  ( 44.11147024075970080, 1.884029797248020000, -54.64999999999999858 ) ) ;
#12553=AXIS2_PLACEMENT_3D ( 'NONE', #39566, #23041, #23289 ) ;
#12555=ORIENTED_EDGE ( 'NONE', *, *, #26347, .F. ) ;
#12560=B_SPLINE_CURVE_WITH_KNOTS ( 'NONE', 3,
 ( #2402, #18135, #18386, #9765, #17874, #34097, #34623, #14207, #25716, #29909 ),
 .UNSPECIFIED., .F., .F.,
 ( 4, 2, 2, 2, 4 ),
 ( 0.1205773112035685712, 0.1385876512664389881, 0.1499668177668040114, 0.1614008449072590057, 0.1617349454127599839 ),
 .UNSPECIFIED. ) ;
#12567=CARTESIAN_POINT ( 'NONE',  ( 14.13393739769630031, 1.391621760993509982, -35.14999999999999858 ) ) ;
#12584=CARTESIAN_POINT ( 'NONE',  ( 11.96660005458869946, 10.88381105532060111, -34.64999999999999858 ) ) ;
#12588=ADVANCED_FACE ( 'NONE', ( #12951 ), #880, .T. ) ;
#12592=DIRECTION ( 'NONE',  ( 0.000000000000000000, -1.000000000000000000, 0.000000000000000000 ) ) ;
#12593=CARTESIAN_POINT ( 'NONE',  ( 15.08112966403183997, -49.61614526831208849, -83.21862149199232306 ) ) ;
#12595=FACE_OUTER_BOUND ( 'NONE', #30895, .T. ) ;
#12596=CARTESIAN_POINT ( 'NONE',  ( 2.422196078461530178, -5.407548561780520124, -35.02873218748179340 ) ) ;
#12601=ORIENTED_EDGE ( 'NONE', *, *, #203, .T. ) ;
#12610=DIRECTION ( 'NONE',  ( -0.3487035033511790005, 0.9372330909387559528, 0.000000000000000000 ) ) ;
#12612=ORIENTED_EDGE ( 'NONE', *, *, #47093, .T. ) ;
#12613=DIRECTION ( 'NONE',  ( 0.000000000000000000, 0.000000000000000000, -1.000000000000000000 ) ) ;
#12625=CIRCLE ( 'NONE', #42752, 2.999999999999999112 ) ;
#12629=VERTEX_POINT ( 'NONE', #33355 ) ;
#12636=DIRECTION ( 'NONE',  ( 0.000000000000000000, 0.000000000000000000, 1.000000000000000000 ) ) ;
#12644=CARTESIAN_POINT ( 'NONE',  ( 41.73321004121098809, -37.58017348599624086, -81.65362388221058154 ) ) ;
#12649=ADVANCED_FACE ( 'NONE', ( #40969 ), #48847, .T. ) ;
#12654=AXIS2_PLACEMENT_3D ( 'NONE', #21926, #14342, #30312 ) ;
#12655=( BOUNDED_CURVE ( )  B_SPLINE_CURVE ( 3, ( #49920, #13759, #25264, #41271 ),
 .UNSPECIFIED., .F., .T. ) 
 B_SPLINE_CURVE_WITH_KNOTS ( ( 4, 4 ),
 ( 1.776356948991648501E-15, 0.7853981633974506105 ),
 .UNSPECIFIED. ) 
 CURVE ( )  GEOMETRIC_REPRESENTATION_ITEM ( )  RATIONAL_B_SPLINE_CURVE ( ( 1.000000000000000000, 0.9492530216741910110, 0.9492530216741910110, 1.000000000000000000 ) ) 
 REPRESENTATION_ITEM ( '' )  );
#12680=CARTESIAN_POINT ( 'NONE',  ( 22.20417850065088672, -53.99262654159362285, -34.79644414665607144 ) ) ;
#12683=EDGE_CURVE ( 'NONE', #13016, #29610, #7911, .T. ) ;
#12689=CARTESIAN_POINT ( 'NONE',  ( 37.13393739769620083, -49.11618894467930829, -35.14999999999999858 ) ) ;
#12690=LINE ( 'NONE', #25227, #37670 ) ;
#12695=ORIENTED_EDGE ( 'NONE', *, *, #41068, .F. ) ;
#12702=VECTOR ( 'NONE', #12592, 1000.000000000000000 ) ;
#12703=EDGE_CURVE ( 'NONE', #45483, #36729, #33476, .T. ) ;
#12710=CARTESIAN_POINT ( 'NONE',  ( 22.20417850065061671, 22.76024865223504889, -34.79644414665609986 ) ) ;
#12713=CARTESIAN_POINT ( 'NONE',  ( 0.2589946642438165636, -10.52437269067010028, -34.65038329361674840 ) ) ;
#12714=CARTESIAN_POINT ( 'NONE',  ( 15.19952276919313405, -14.93729697828149305, 36.77166666666649775 ) ) ;
#12719=DIRECTION ( 'NONE',  ( 0.000000000000000000, 0.000000000000000000, 1.000000000000000000 ) ) ;
#12721=ADVANCED_FACE ( 'NONE', ( #8750 ), #16600, .T. ) ;
#12728=CARTESIAN_POINT ( 'NONE',  ( 44.03040329333745717, -39.95715391141960282, -66.51246656095132437 ) ) ;
#12730=DIRECTION ( 'NONE',  ( 0.000000000000000000, -1.000000000000000000, 0.000000000000000000 ) ) ;
#12742=ORIENTED_EDGE ( 'NONE', *, *, #35492, .F. ) ;
#12747=CARTESIAN_POINT ( 'NONE',  ( 42.92581320805854972, 8.626641518850258095, -71.85816444028515093 ) ) ;
#12749=CARTESIAN_POINT ( 'NONE',  ( 11.79459217608838806, -41.85765695298068323, -34.70142521051216988 ) ) ;
#12754=ORIENTED_EDGE ( 'NONE', *, *, #46237, .F. ) ;
#12763=CARTESIAN_POINT ( 'NONE',  ( -0.02605860948296716273, 14.44407830860123454, -34.78912696276449878 ) ) ;
#12764=DIRECTION ( 'NONE',  ( 1.000000000000000000, 0.000000000000000000, 0.000000000000000000 ) ) ;
#12766=CARTESIAN_POINT ( 'NONE',  ( 16.13393739769620083, -15.61618894467929941, -35.14999999999999858 ) ) ;
#12771=VECTOR ( 'NONE', #12636, 1000.000000000000000 ) ;
#12773=FACE_OUTER_BOUND ( 'NONE', #1724, .T. ) ;
#12779=CARTESIAN_POINT ( 'NONE',  ( -0.03447620312153085176, -4.141051901845263394, -34.79644660940673617 ) ) ;
#12790=ADVANCED_FACE ( 'NONE', ( #46479 ), #42539, .T. ) ;
#12805=ORIENTED_EDGE ( 'NONE', *, *, #39065, .F. ) ;
#12809=ORIENTED_EDGE ( 'NONE', *, *, #24705, .F. ) ;
#12811=DIRECTION ( 'NONE',  ( 0.5322052227529140422, -0.8460333946355099721, -0.03138623959693901538 ) ) ;
#12812=CARTESIAN_POINT ( 'NONE',  ( 16.13393739769620083, -15.61618894467929941, -44.64999999999999858 ) ) ;
#12820=VERTEX_POINT ( 'NONE', #41748 ) ;
#12823=FACE_OUTER_BOUND ( 'NONE', #2860, .T. ) ;
#12826=ORIENTED_EDGE ( 'NONE', *, *, #8933, .F. ) ;
#12835=CARTESIAN_POINT ( 'NONE',  ( 22.20417850065088672, -53.99262654159362285, -34.79644414665607144 ) ) ;
#12836=EDGE_LOOP ( 'NONE', ( #27882, #40415, #15459, #48863, #20740, #42988, #50911 ) ) ;
#12839=ORIENTED_EDGE ( 'NONE', *, *, #51250, .F. ) ;
#12840=LINE ( 'NONE', #504, #38559 ) ;
#12847=DIRECTION ( 'NONE',  ( -0.8340645993220398013, -0.5516667872527448724, 0.000000000000000000 ) ) ;
#12854=EDGE_CURVE ( 'NONE', #36393, #425, #26653, .T. ) ;
#12856=EDGE_CURVE ( 'NONE', #45896, #37692, #50789, .T. ) ;
#12858=CARTESIAN_POINT ( 'NONE',  ( -0.007164427059776000244, -8.408015226406421405, -34.77269723891829756 ) ) ;
#12860=CARTESIAN_POINT ( 'NONE',  ( 14.11670613118836748, -49.61617733564492738, -83.15271738028131665 ) ) ;
#12864=DIRECTION ( 'NONE',  ( 0.1960104533864299448, 0.03282462862515294483, 0.9800522669321607427 ) ) ;
#12886=FACE_BOUND ( 'NONE', #15022, .T. ) ;
#12905=VERTEX_POINT ( 'NONE', #15657 ) ;
#12906=CYLINDRICAL_SURFACE ( 'NONE', #49367, 2.999999999999999112 ) ;
#12910=AXIS2_PLACEMENT_3D ( 'NONE', #21584, #37333, #24730 ) ;
#12912=CARTESIAN_POINT ( 'NONE',  ( 43.32204027125330015, -37.82422349032574971, -73.70942140953911803 ) ) ;
#12919=VECTOR ( 'NONE', #1657, 1000.000000000000114 ) ;
#12924=VERTEX_POINT ( 'NONE', #31611 ) ;
#12935=LINE ( 'NONE', #24684, #18121 ) ;
#12937=SPHERICAL_SURFACE ( 'NONE', #34453, 3.000000000000000000 ) ;
#12949=CARTESIAN_POINT ( 'NONE',  ( -0.1946058609260517269, -10.66917667990032292, -34.93568796252242237 ) ) ;
#12951=FACE_OUTER_BOUND ( 'NONE', #49580, .T. ) ;
#12966=EDGE_CURVE ( 'NONE', #48439, #28134, #35254, .T. ) ;
#12970=DIRECTION ( 'NONE',  ( 0.000000000000000000, -1.000000000000000000, 0.000000000000000000 ) ) ;
#12971=VERTEX_POINT ( 'NONE', #43693 ) ;
#12976=( BOUNDED_CURVE ( )  B_SPLINE_CURVE ( 3, ( #23853, #6886, #27295, #39619 ),
 .UNSPECIFIED., .F., .T. ) 
 B_SPLINE_CURVE_WITH_KNOTS ( ( 4, 4 ),
 ( 2.356194490192338620, 3.141592653589793116 ),
 .UNSPECIFIED. ) 
 CURVE ( )  GEOMETRIC_REPRESENTATION_ITEM ( )  RATIONAL_B_SPLINE_CURVE ( ( 1.000000000000000000, 0.9492530216741903448, 0.9492530216741903448, 1.000000000000000000 ) ) 
 REPRESENTATION_ITEM ( '' )  );
#12982=CIRCLE ( 'NONE', #41430, 2.999999999999999112 ) ;
#12995=CARTESIAN_POINT ( 'NONE',  ( 14.28038400710302724, 10.53025766472732450, -34.79644660940672907 ) ) ;
#13002=CARTESIAN_POINT ( 'NONE',  ( 16.13393739769620083, -15.61618894467929941, -54.64999999999999858 ) ) ;
#13004=ORIENTED_EDGE ( 'NONE', *, *, #6521, .T. ) ;
#13012=CARTESIAN_POINT ( 'NONE',  ( 44.07620675114476683, 8.728620045891982926, -66.29034569140392819 ) ) ;
#13016=VERTEX_POINT ( 'NONE', #16679 ) ;
#13018=AXIS2_PLACEMENT_3D ( 'NONE', #28807, #16768, #44808 ) ;
#13021=EDGE_CURVE ( 'NONE', #29987, #45454, #48663, .T. ) ;
#13025=EDGE_CURVE ( 'NONE', #621, #1956, #31781, .T. ) ;
#13027=DIRECTION ( 'NONE',  ( 0.000000000000000000, 1.000000000000000000, 0.000000000000000000 ) ) ;
#13030=ORIENTED_EDGE ( 'NONE', *, *, #9593, .T. ) ;
#13034=CARTESIAN_POINT ( 'NONE',  ( -15.76845656909109117, 6.818550277744307664, -48.78419541140080185 ) ) ;
#13044=CARTESIAN_POINT ( 'NONE',  ( 14.15073023633489946, -32.59356659976219817, -35.02127583263639821 ) ) ;
#13050=DIRECTION ( 'NONE',  ( 0.000000000000000000, 0.000000000000000000, 1.000000000000000000 ) ) ;
#13061=CYLINDRICAL_SURFACE ( 'NONE', #3833, 3.000000000000000444 ) ;
#13065=ADVANCED_FACE ( 'NONE', ( #28984 ), #862, .T. ) ;
#13076=ORIENTED_EDGE ( 'NONE', *, *, #23253, .T. ) ;
#13080=CARTESIAN_POINT ( 'NONE',  ( 0.4047412638265869833, -22.38804348994680282, -35.14999999999999858 ) ) ;
#13084=CARTESIAN_POINT ( 'NONE',  ( -0.1295185695944119919, -31.87964491196989414, 4.943674098299959851 ) ) ;
#13103=CARTESIAN_POINT ( 'NONE',  ( 14.13393739769640156, 6.292713355527309815, -54.64999999999999858 ) ) ;
#13113=CARTESIAN_POINT ( 'NONE',  ( 26.13393739769619728, -28.89524513604070322, -84.65000000000000568 ) ) ;
#13116=VERTEX_POINT ( 'NONE', #46493 ) ;
#13121=VECTOR ( 'NONE', #38266, 1000.000000000000000 ) ;
#13125=CARTESIAN_POINT ( 'NONE',  ( 28.74617114340210122, -4.636586115271110309, -34.66275921114419134 ) ) ;
#13127=EDGE_CURVE ( 'NONE', #26692, #13682, #26821, .T. ) ;
#13128=DIRECTION ( 'NONE',  ( 0.000000000000000000, 0.000000000000000000, -1.000000000000000000 ) ) ;
#13132=CARTESIAN_POINT ( 'NONE',  ( 30.61153946640385826, -35.65524129201374848, -84.61437977358458795 ) ) ;
#13133=CARTESIAN_POINT ( 'NONE',  ( 16.13393739769620083, -15.61618894467929941, -34.64999999999999858 ) ) ;
#13155=DIRECTION ( 'NONE',  ( -0.8660254037844387076, 0.4999999999999998890, 1.942890293094024439E-16 ) ) ;
#13161=B_SPLINE_CURVE_WITH_KNOTS ( 'NONE', 3,
 ( #23010, #6801, #47158, #51843, #15686, #3124, #22753, #34813, #27726, #19093 ),
 .UNSPECIFIED., .F., .F.,
 ( 4, 2, 2, 2, 4 ),
 ( -0.1799215976186380184, -0.1795414484423739909, -0.1664059944893910015, -0.1383522341550179890, -0.1329710036334196266 ),
 .UNSPECIFIED. ) ;
#13170=CARTESIAN_POINT ( 'NONE',  ( 16.13393739769620083, -15.61618894467929941, -34.64999999999999858 ) ) ;
#13174=FACE_OUTER_BOUND ( 'NONE', #8826, .T. ) ;
#13190=VERTEX_POINT ( 'NONE', #31236 ) ;
#13201=CARTESIAN_POINT ( 'NONE',  ( 20.63393739769599833, 10.38381105532070059, -54.64999999999999858 ) ) ;
#13206=CARTESIAN_POINT ( 'NONE',  ( 0.4047412638265869833, -22.38804348994680282, -35.14999999999999858 ) ) ;
#13223=EDGE_CURVE ( 'NONE', #28134, #30405, #11594, .T. ) ;
#13224=ORIENTED_EDGE ( 'NONE', *, *, #24673, .T. ) ;
#13250=EDGE_CURVE ( 'NONE', #35178, #7027, #41050, .T. ) ;
#13252=CARTESIAN_POINT ( 'NONE',  ( 28.13393739769619373, -22.54439217495488279, -35.01561944896765510 ) ) ;
#13253=CYLINDRICAL_SURFACE ( 'NONE', #23764, 0.4999999999999983347 ) ;
#13264=VERTEX_POINT ( 'NONE', #43068 ) ;
#13266=CARTESIAN_POINT ( 'NONE',  ( 23.32430482491550094, 18.10127401595489971, -34.64999999999999858 ) ) ;
#13269=CARTESIAN_POINT ( 'NONE',  ( 43.99065823752038540, 8.721581408738890318, -66.70470347308750547 ) ) ;
#13274=ORIENTED_EDGE ( 'NONE', *, *, #38270, .F. ) ;
#13275=ORIENTED_EDGE ( 'NONE', *, *, #29680, .T. ) ;
#13277=VERTEX_POINT ( 'NONE', #19459 ) ;
#13279=DIRECTION ( 'NONE',  ( 0.000000000000000000, 0.000000000000000000, 1.000000000000000000 ) ) ;
#13282=ORIENTED_EDGE ( 'NONE', *, *, #2966, .T. ) ;
#13283=VERTEX_POINT ( 'NONE', #35444 ) ;
#13287=DIRECTION ( 'NONE',  ( 0.000000000000000000, 0.000000000000000000, 1.000000000000000000 ) ) ;
#13299=DIRECTION ( 'NONE',  ( -1.000000000000000000, 0.000000000000000000, 0.000000000000000000 ) ) ;
#13310=CYLINDRICAL_SURFACE ( 'NONE', #22116, 2.999999999999999112 ) ;
#13325=CARTESIAN_POINT ( 'NONE',  ( 19.13393739769623991, -49.61618894467932250, -35.01561944896766221 ) ) ;
#13327=EDGE_CURVE ( 'NONE', #38150, #32888, #24655, .T. ) ;
#13336=ORIENTED_EDGE ( 'NONE', *, *, #43304, .F. ) ;
#13339=CARTESIAN_POINT ( 'NONE',  ( 0.08375394646315241498, 19.63944928676770019, -34.70982966457259522 ) ) ;
#13342=CARTESIAN_POINT ( 'NONE',  ( 0.3209249304026170480, -26.47788675693900018, -34.64999999999999858 ) ) ;
#13345=CARTESIAN_POINT ( 'NONE',  ( -19.05274139337909745, -33.00040335413840609, -51.45066150993559262 ) ) ;
#13370=CONICAL_SURFACE ( 'NONE', #42664, 36.50000000000000711, 0.1651486774146265213 ) ;
#13373=CARTESIAN_POINT ( 'NONE',  ( 20.53650276133985031, -41.76263555408612405, -34.79644660940672907 ) ) ;
#13377=AXIS2_PLACEMENT_3D ( 'NONE', #21808, #25994, #22061 ) ;
#13381=CARTESIAN_POINT ( 'NONE',  ( 46.92684765627410570, -40.29994455800911624, -51.82181065190314229 ) ) ;
#13382=CIRCLE ( 'NONE', #28391, 39.00000000000001421 ) ;
#13396=CARTESIAN_POINT ( 'NONE',  ( -0.1437508118502997256, -8.468281633606618897, -34.89146800830131667 ) ) ;
#13398=ORIENTED_EDGE ( 'NONE', *, *, #51700, .T. ) ;
#13406=CARTESIAN_POINT ( 'NONE',  ( 46.77956775759329133, 7.928029628855391309, -34.67032516424389854 ) ) ;
#13419=VECTOR ( 'NONE', #8574, 1000.000000000000000 ) ;
#13421=CIRCLE ( 'NONE', #15043, 5.251829701412240148 ) ;
#13422=ORIENTED_EDGE ( 'NONE', *, *, #45476, .T. ) ;
#13432=CARTESIAN_POINT ( 'NONE',  ( 42.79704101284554696, -37.74735858493779972, -76.33443527249174565 ) ) ;
#13434=ORIENTED_EDGE ( 'NONE', *, *, #29611, .F. ) ;
#13441=CARTESIAN_POINT ( 'NONE',  ( -1.839728563314089849, -28.30269090235150031, -54.64999999999999858 ) ) ;
#13443=ADVANCED_FACE ( 'NONE', ( #13174 ), #12906, .F. ) ;
#13462=FACE_OUTER_BOUND ( 'NONE', #51689, .T. ) ;
#13468=ORIENTED_EDGE ( 'NONE', *, *, #45781, .T. ) ;
#13486=ORIENTED_EDGE ( 'NONE', *, *, #3625, .F. ) ;
#13500=DIRECTION ( 'NONE',  ( 0.000000000000000000, 1.000000000000000000, 0.000000000000000000 ) ) ;
#13512=DIRECTION ( 'NONE',  ( 0.000000000000000000, 0.000000000000000000, -1.000000000000000000 ) ) ;
#13513=CARTESIAN_POINT ( 'NONE',  ( 10.13393739769589885, 22.91950879131600161, -35.14999999999999858 ) ) ;
#13523=VERTEX_POINT ( 'NONE', #25182 ) ;
#13524=CARTESIAN_POINT ( 'NONE',  ( -0.007164426707907000161, -50.71887597443840434, -34.77269723932290191 ) ) ;
#13525=AXIS2_PLACEMENT_3D ( 'NONE', #13170, #37773, #13667 ) ;
#13529=CARTESIAN_POINT ( 'NONE',  ( 43.73535983031142393, 8.700407067847576670, -67.94015393090442956 ) ) ;
#13531=AXIS2_PLACEMENT_3D ( 'NONE', #51180, #11347, #39637 ) ;
#13532=CARTESIAN_POINT ( 'NONE',  ( 11.73137203405252826, -41.76263555408610273, -34.79644660940672196 ) ) ;
#13544=CARTESIAN_POINT ( 'NONE',  ( -9.005807778154689913, 14.20118441705474410, -42.97877832676560672 ) ) ;
#13545=ADVANCED_FACE ( 'NONE', ( #16553 ), #6672, .F. ) ;
#13556=AXIS2_PLACEMENT_3D ( 'NONE', #44884, #8988, #40946 ) ;
#13559=DIRECTION ( 'NONE',  ( -1.000000000000000000, 0.000000000000000000, 0.000000000000000000 ) ) ;
#13573=VERTEX_POINT ( 'NONE', #9735 ) ;
#13585=VERTEX_POINT ( 'NONE', #22025 ) ;
#13587=B_SPLINE_CURVE_WITH_KNOTS ( 'NONE', 3,
 ( #38096, #5358, #17402, #17914 ),
 .UNSPECIFIED., .F., .F.,
 ( 4, 4 ),
 ( 0.000000000000000000, 1.000000000000000000 ),
 .UNSPECIFIED. ) ;
#13596=CARTESIAN_POINT ( 'NONE',  ( -21.83178109590970095, -6.979653015830420415, -53.75064070593009546 ) ) ;
#13597=FACE_OUTER_BOUND ( 'NONE', #10373, .T. ) ;
#13605=ADVANCED_FACE ( 'NONE', ( #5805 ), #9990, .T. ) ;
#13609=CARTESIAN_POINT ( 'NONE',  ( 37.88393739769619373, -41.76263555408612405, -34.79644660940672907 ) ) ;
#13626=EDGE_CURVE ( 'NONE', #29074, #49316, #18303, .T. ) ;
#13628=VECTOR ( 'NONE', #23748, 1000.000000000000000 ) ;
#13630=AXIS2_PLACEMENT_3D ( 'NONE', #5807, #1872, #1095 ) ;
#13631=CARTESIAN_POINT ( 'NONE',  ( 29.10094820555050177, -4.504588236828580783, -34.97139175453740023 ) ) ;
#13632=CARTESIAN_POINT ( 'NONE',  ( 18.89608595021987725, -49.61618894467940777, -83.05213603404914124 ) ) ;
#13635=CARTESIAN_POINT ( 'NONE',  ( 45.45010799891814202, -40.18496802584400740, -59.12881032271813808 ) ) ;
#13646=CARTESIAN_POINT ( 'NONE',  ( 29.07912664786299928, -26.71971901182079989, -34.92075920103129505 ) ) ;
#13662=ORIENTED_EDGE ( 'NONE', *, *, #48761, .T. ) ;
#13667=DIRECTION ( 'NONE',  ( 0.5112408204145773016, 0.8594375041513080404, 0.000000000000000000 ) ) ;
#13669=EDGE_CURVE ( 'NONE', #32498, #46482, #1870, .T. ) ;
#13674=CIRCLE ( 'NONE', #15310, 16.60961179679784649 ) ;
#13680=CARTESIAN_POINT ( 'NONE',  ( -0.007164427059776000244, -20.74946784552680157, -34.77269723891829756 ) ) ;
#13681=CARTESIAN_POINT ( 'NONE',  ( 45.14904957753085313, -38.06017041830072145, -64.57443011523157850 ) ) ;
#13682=VERTEX_POINT ( 'NONE', #22284 ) ;
#13693=ORIENTED_EDGE ( 'NONE', *, *, #10454, .T. ) ;
#13697=CARTESIAN_POINT ( 'NONE',  ( 41.64058680028773551, -39.72527599113804087, -78.06475774647746846 ) ) ;
#13701=VECTOR ( 'NONE', #44445, 1000.000000000000000 ) ;
#13708=CARTESIAN_POINT ( 'NONE',  ( 22.15575932996800290, 22.87009133999809762, -34.93361312117490058 ) ) ;
#13722=DIRECTION ( 'NONE',  ( 0.8660254037844384856, -0.5000000000000003331, -2.775557561562892337E-16 ) ) ;
#13726=DIRECTION ( 'NONE',  ( 0.3863301728269248891, 0.9223605572461988089, -3.330669073875469621E-16 ) ) ;
#13736=( BOUNDED_CURVE ( )  B_SPLINE_CURVE ( 3, ( #33644, #38113, #33899, #42305 ),
 .UNSPECIFIED., .F., .T. ) 
 B_SPLINE_CURVE_WITH_KNOTS ( ( 4, 4 ),
 ( 2.356194490192482505, 3.141592653589790451 ),
 .UNSPECIFIED. ) 
 CURVE ( )  GEOMETRIC_REPRESENTATION_ITEM ( )  RATIONAL_B_SPLINE_CURVE ( ( 1.000000000000000000, 0.9492530216742089966, 0.9492530216742089966, 1.000000000000000000 ) ) 
 REPRESENTATION_ITEM ( '' )  );
#13739=CARTESIAN_POINT ( 'NONE',  ( 45.45535151068285984, 6.862517011477148543, -63.04287378213577142 ) ) ;
#13755=EDGE_LOOP ( 'NONE', ( #49197, #33990, #31994, #47761, #7585, #1244, #20124, #36635 ) ) ;
#13759=CARTESIAN_POINT ( 'NONE',  ( 47.13393739769619373, -35.30990563848522612, -54.64999999999994884 ) ) ;
#13764=CARTESIAN_POINT ( 'NONE',  ( 20.30127474080349970, -42.11618894467939356, -34.64999999999999858 ) ) ;
#13766=ADVANCED_FACE ( 'NONE', ( #23817 ), #10864, .T. ) ;
#13767=VECTOR ( 'NONE', #14679, 999.9999999999998863 ) ;
#13770=CARTESIAN_POINT ( 'NONE',  ( 16.13393739769620083, -1.480959244941480124, -34.70142521051216988 ) ) ;
#13781=CARTESIAN_POINT ( 'NONE',  ( 43.27650499216790081, 8.659509414535037308, -70.16183350288429210 ) ) ;
#13783=CYLINDRICAL_SURFACE ( 'NONE', #41006, 0.5000000000000000000 ) ;
#13788=CARTESIAN_POINT ( 'NONE',  ( -22.83979347564535800, -16.55049450429037350, -54.74432729527064367 ) ) ;
#13789=FACE_OUTER_BOUND ( 'NONE', #34468, .T. ) ;
#13790=CARTESIAN_POINT ( 'NONE',  ( 24.58073416742070094, -18.76089852590099838, -35.14999999999999858 ) ) ;
#13802=LINE ( 'NONE', #38421, #49826 ) ;
#13804=VECTOR ( 'NONE', #31830, 1000.000000000000000 ) ;
#13809=CARTESIAN_POINT ( 'NONE',  ( -11.80944000494479873, 2.826328597561450273, -45.03554556751399929 ) ) ;
#13829=FACE_OUTER_BOUND ( 'NONE', #20734, .T. ) ;
#13835=DIRECTION ( 'NONE',  ( 0.000000000000000000, 0.000000000000000000, 1.000000000000000000 ) ) ;
#13839=ORIENTED_EDGE ( 'NONE', *, *, #3957, .F. ) ;
#13847=LINE ( 'NONE', #1789, #712 ) ;
#13849=EDGE_CURVE ( 'NONE', #13888, #16348, #35144, .T. ) ;
#13850=CARTESIAN_POINT ( 'NONE',  ( -22.72850738805879800, -18.52594519380850002, -54.52996344323300093 ) ) ;
#13863=AXIS2_PLACEMENT_3D ( 'NONE', #45071, #12081, #522 ) ;
#13866=DIRECTION ( 'NONE',  ( -0.2846079131720438693, 0.9586440088791325920, 0.000000000000000000 ) ) ;
#13882=CARTESIAN_POINT ( 'NONE',  ( -5.122171525981340068, 17.49197490117069620, -39.56459775772290044 ) ) ;
#13884=CARTESIAN_POINT ( 'NONE',  ( 44.62438891534000618, -39.14235344977141295, -67.35856431845091663 ) ) ;
#13888=VERTEX_POINT ( 'NONE', #27511 ) ;
#13891=CARTESIAN_POINT ( 'NONE',  ( 47.23631910128078459, 8.041419318995805199, -54.68400724043278416 ) ) ;
#13892=AXIS2_PLACEMENT_3D ( 'NONE', #20120, #32409, #36113 ) ;
#13893=CARTESIAN_POINT ( 'NONE',  ( 18.13393739769599833, 14.38381105532070059, -49.33749999999999858 ) ) ;
#13897=CARTESIAN_POINT ( 'NONE',  ( 28.93686911782380022, -26.66694171151199910, -34.75221567031800163 ) ) ;
#13927=CARTESIAN_POINT ( 'NONE',  ( -22.84941414684771388, -15.61618224896967355, -54.74986855478772441 ) ) ;
#13930=DIRECTION ( 'NONE',  ( 0.000000000000000000, 0.000000000000000000, 1.000000000000000000 ) ) ;
#13935=CARTESIAN_POINT ( 'NONE',  ( 45.74427000726045378, -38.12636687890177001, -61.59833689282645253 ) ) ;
#13946=EDGE_LOOP ( 'NONE', ( #26527, #8627, #493, #46811, #19256, #17953 ) ) ;
#13950=CARTESIAN_POINT ( 'NONE',  ( 42.13477582370718721, -39.77883744432604374, -75.68159061675045507 ) ) ;
#13957=EDGE_CURVE ( 'NONE', #2565, #15778, #14555, .T. ) ;
#13964=EDGE_CURVE ( 'NONE', #15968, #21893, #14189, .T. ) ;
#13968=CARTESIAN_POINT ( 'NONE',  ( -0.4123484725610440105, -45.29119327467250145, -35.12503119152799513 ) ) ;
#13990=CARTESIAN_POINT ( 'NONE',  ( 4.133937397696209715, -22.54439217495480108, -35.14999999999999858 ) ) ;
#13991=ORIENTED_EDGE ( 'NONE', *, *, #21143, .F. ) ;
#13992=CARTESIAN_POINT ( 'NONE',  ( 45.49907709881001949, 6.867305819722518301, -62.82425208550701257 ) ) ;
#14003=DIRECTION ( 'NONE',  ( 0.000000000000000000, -1.000000000000000000, 0.000000000000000000 ) ) ;
#14009=ORIENTED_EDGE ( 'NONE', *, *, #15240, .F. ) ;
#14015=FACE_OUTER_BOUND ( 'NONE', #1984, .T. ) ;
#14025=VERTEX_POINT ( 'NONE', #40857 ) ;
#14027=( BOUNDED_CURVE ( )  B_SPLINE_CURVE ( 3, ( #39524, #27708, #19848, #35838 ),
 .UNSPECIFIED., .F., .T. ) 
 B_SPLINE_CURVE_WITH_KNOTS ( ( 4, 4 ),
 ( 1.570796326794897890, 2.356194490192353719 ),
 .UNSPECIFIED. ) 
 CURVE ( )  GEOMETRIC_REPRESENTATION_ITEM ( )  RATIONAL_B_SPLINE_CURVE ( ( 1.000000000000000000, 0.9492530216741901228, 0.9492530216741901228, 1.000000000000000000 ) ) 
 REPRESENTATION_ITEM ( '' )  );
#14031=CARTESIAN_POINT ( 'NONE',  ( 46.63393739769619373, -36.11618894467930119, -35.14999999999999858 ) ) ;
#14034=CARTESIAN_POINT ( 'NONE',  ( 43.36638863507317865, 8.667721898220143828, -69.72695248505642951 ) ) ;
#14039=VERTEX_POINT ( 'NONE', #20930 ) ;
#14042=CARTESIAN_POINT ( 'NONE',  ( 17.76831794872871839, 10.74943050428838021, -34.64999999999999858 ) ) ;
#14048=AXIS2_PLACEMENT_3D ( 'NONE', #35219, #51477, #47803 ) ;
#14057=EDGE_CURVE ( 'NONE', #20265, #49113, #42690, .T. ) ;
#14066=CARTESIAN_POINT ( 'NONE',  ( 11.73137203405248385, 10.53025766472752522, -34.79644660940672907 ) ) ;
#14090=DIRECTION ( 'NONE',  ( 0.8660254037844383745, -0.5000000000000003331, 0.000000000000000000 ) ) ;
#14092=ORIENTED_EDGE ( 'NONE', *, *, #46861, .F. ) ;
#14093=DIRECTION ( 'NONE',  ( -0.3502816565540492477, 0.000000000000000000, 0.9366444154970182678 ) ) ;
#14094=ORIENTED_EDGE ( 'NONE', *, *, #38375, .F. ) ;
#14096=FACE_OUTER_BOUND ( 'NONE', #19662, .T. ) ;
#14101=CARTESIAN_POINT ( 'NONE',  ( -20.79634969123249988, -28.70049512919520041, -52.86954696638409246 ) ) ;
#14108=VERTEX_POINT ( 'NONE', #37445 ) ;
#14115=VECTOR ( 'NONE', #41683, 1000.000000000000000 ) ;
#14122=EDGE_CURVE ( 'NONE', #50075, #18993, #17533, .T. ) ;
#14127=CARTESIAN_POINT ( 'NONE',  ( 3.633937397696210159, -19.08029055981709732, -35.14999999999999858 ) ) ;
#14137=CARTESIAN_POINT ( 'NONE',  ( -0.2761815207641740155, 19.58270920947809657, -35.04694460471009876 ) ) ;
#14139=CARTESIAN_POINT ( 'NONE',  ( 43.70467631200691727, -39.04050123248909188, -71.92343701204615058 ) ) ;
#14152=CIRCLE ( 'NONE', #24142, 2.999999999999999112 ) ;
#14157=VERTEX_POINT ( 'NONE', #19843 ) ;
#14168=VERTEX_POINT ( 'NONE', #7038 ) ;
#14174=CARTESIAN_POINT ( 'NONE',  ( 3.633937397696210159, -8.399310579809009525, -34.64999999999999858 ) ) ;
#14180=DIRECTION ( 'NONE',  ( 0.1564344650402237358, -0.9876883405951387696, 0.000000000000000000 ) ) ;
#14186=CARTESIAN_POINT ( 'NONE',  ( 45.01043142363850791, -38.04361682771764208, -65.26752630117056242 ) ) ;
#14188=AXIS2_PLACEMENT_3D ( 'NONE', #24295, #35608, #51597 ) ;
#14189=CIRCLE ( 'NONE', #12502, 1.999999999999998224 ) ;
#14195=VECTOR ( 'NONE', #9401, 999.9999999999998863 ) ;
#14207=CARTESIAN_POINT ( 'NONE',  ( 46.63604585716099393, -39.11158712134929516, -34.65000333419789769 ) ) ;
#14209=EDGE_CURVE ( 'NONE', #42105, #13573, #44336, .T. ) ;
#14212=CARTESIAN_POINT ( 'NONE',  ( 23.62413055734840128, 17.52287609088140030, -35.14999999999999858 ) ) ;
#14220=CARTESIAN_POINT ( 'NONE',  ( 14.28038030992529528, -32.47778390180254604, -34.79644291222909658 ) ) ;
#14224=VECTOR ( 'NONE', #45181, 1000.000000000000000 ) ;
#14227=CARTESIAN_POINT ( 'NONE',  ( 18.13393739769620083, -32.62399965035220362, -35.14999999999999858 ) ) ;
#14235=ORIENTED_EDGE ( 'NONE', *, *, #25631, .F. ) ;
#14238=VECTOR ( 'NONE', #37691, 1000.000000000000000 ) ;
#14247=CARTESIAN_POINT ( 'NONE',  ( 46.80774876147005159, 7.000071986378179290, -56.28089294811472598 ) ) ;
#14266=CLOSED_SHELL ( 'NONE', ( #17675, #15781, #44001, #35360, #2161, #9858, #982, #50169, #10343, #37698, #34167, #46997, #2376, #16988, #12790, #14414, #8155, #20634, #49600, #1754, #40445, #6587, #37421, #19029, #38299, #12649, #10004, #11374, #21912, #38529, #50927, #11465, #4539, #33054, #36760, #7874, #49075, #38937, #51775, #27125, #41711, #20141, #12257, #1494, #3765, #13766, #15228, #38573, #31509, #49712, #15664, #50820, #4426, #37325, #34272, #1239, #16859, #25800, #19908, #13545, #17158, #24445, #21723, #11361, #579, #50235, #28839, #3033, #28331, #37979, #27912, #7500, #39704, #738, #21461, #11821, #49179, #6105, #7296, #3064, #11908, #49538, #25219, #44161, #46443, #35727, #49593, #12414, #14596, #34268, #40680, #10220, #49774, #19617, #18220, #3823, #51002, #39760, #50365, #43034, #32601, #32899, #13443, #38404, #13605, #36026, #18247, #31720, #34638, #40615, #46703, #24769, #43178, #9497, #27380, #49853, #46148, #23441, #40870, #16922, #3102, #8152, #22865, #10122, #6312, #45190, #33883, #17113, #20609, #40217, #48756, #6336, #24251, #6598, #44480, #22755, #22871, #5326, #12588, #25192, #29967, #33819, #20403, #10402, #25964, #34937, #44351, #3693, #1429, #44687, #45037, #5495, #13065, #1574, #48141, #21081, #48892, #46087, #34299, #40414, #23380, #34604, #8408, #12721, #38082, #49399, #24803, #1508, #5261, #34580, #18996, #47647, #45424, #41957, #43615, #45270, #7957, #49947, #32490, #51408, #7966, #19281, #48208, #16714, #19922, #10959, #32596, #7223, #29903, #14909, #26181, #7376, #19807, #29333, #3980, #34417, #40032, #49109, #33161, #24525, #4431, #51225, #4366, #15554, #15299, #491, #1850, #18572, #21625, #35298, #5932, #38020, #49810, #28175, #24346, #49138, #30009, #43592, #43248 ) ) ;
#14274=EDGE_CURVE ( 'NONE', #29692, #46452, #13421, .T. ) ;
#14281=CARTESIAN_POINT ( 'NONE',  ( 9.937051593248220627, -53.70417188095279926, -34.65604926186119172 ) ) ;
#14289=DIRECTION ( 'NONE',  ( 0.000000000000000000, 0.000000000000000000, 1.000000000000000000 ) ) ;
#14290=PLANE ( 'NONE',  #42170 ) ;
#14292=CARTESIAN_POINT ( 'NONE',  ( 45.76294970761291836, 8.847485351248307595, -58.11021846651873091 ) ) ;
#14300=CARTESIAN_POINT ( 'NONE',  ( -21.28852503460515067, -26.72198803963431857, -53.52383174611850336 ) ) ;
#14301=AXIS2_PLACEMENT_3D ( 'NONE', #13133, #1317, #33784 ) ;
#14303=AXIS2_PLACEMENT_3D ( 'NONE', #24852, #16239, #28275 ) ;
#14304=ORIENTED_EDGE ( 'NONE', *, *, #34879, .T. ) ;
#14308=VERTEX_POINT ( 'NONE', #26935 ) ;
#14320=CARTESIAN_POINT ( 'NONE',  ( 38.67452568954060155, -36.11618894467930119, -81.65000000000000568 ) ) ;
#14321=CARTESIAN_POINT ( 'NONE',  ( 28.28038400710292422, -12.15208732954159920, -34.79644660940672907 ) ) ;
#14326=CARTESIAN_POINT ( 'NONE',  ( 46.15610874489437521, -40.10233669974212489, -56.20102867703486282 ) ) ;
#14329=( BOUNDED_CURVE ( )  B_SPLINE_CURVE ( 2, ( #30780, #46805, #10894 ),
 .UNSPECIFIED., .F., .T. ) 
 B_SPLINE_CURVE_WITH_KNOTS ( ( 3, 3 ),
 ( 0.1896353341141479854, 2.672615408357010391 ),
 .UNSPECIFIED. ) 
 CURVE ( )  GEOMETRIC_REPRESENTATION_ITEM ( )  RATIONAL_B_SPLINE_CURVE ( ( 1.004410800606350129, 1.032237589135669875, 1.032581180562780032 ) ) 
 REPRESENTATION_ITEM ( '' )  );
#14330=VECTOR ( 'NONE', #10636, 1000.000000000000114 ) ;
#14340=VERTEX_POINT ( 'NONE', #9094 ) ;
#14342=DIRECTION ( 'NONE',  ( -0.9117581046690675928, 0.4107275965530798323, 0.000000000000000000 ) ) ;
#14352=CARTESIAN_POINT ( 'NONE',  ( 8.711199217769845404, -48.88697541251521983, -34.82978046822304918 ) ) ;
#14353=EDGE_CURVE ( 'NONE', #50419, #21662, #33287, .T. ) ;
#14354=EDGE_LOOP ( 'NONE', ( #252, #47506, #20460, #15301, #27167, #38481, #41720 ) ) ;
#14360=CARTESIAN_POINT ( 'NONE',  ( 37.88393739769619373, -42.11618894467939356, -35.14999999999999858 ) ) ;
#14364=CARTESIAN_POINT ( 'NONE',  ( -22.65260339427180014, -11.81924193806499979, -54.48195099813599995 ) ) ;
#14396=CARTESIAN_POINT ( 'NONE',  ( -9.348292170159599124, 13.97290946334260120, -42.89544360152859781 ) ) ;
#14398=CARTESIAN_POINT ( 'NONE',  ( 46.13944883215520321, -40.23853505593529434, -55.73485720529632204 ) ) ;
#14405=CARTESIAN_POINT ( 'NONE',  ( 43.81109536264059301, 8.794139443671282308, -67.21774360442289264 ) ) ;
#14410=CARTESIAN_POINT ( 'NONE',  ( 28.74617114340210122, -26.59579177408749828, -34.66275921114419134 ) ) ;
#14413=CARTESIAN_POINT ( 'NONE',  ( 15.10238578887313388, -43.89919387818888907, -61.51477253168710035 ) ) ;
#14414=ADVANCED_FACE ( 'NONE', ( #48090 ), #385, .T. ) ;
#14430=FACE_OUTER_BOUND ( 'NONE', #6913, .T. ) ;
#14437=PRODUCT_DEFINITION_SHAPE ( 'NONE', 'NONE',  #46257 ) ;
#14439=CARTESIAN_POINT ( 'NONE',  ( 0.03808610503982497175, -26.96777797282045697, -34.73334895013598356 ) ) ;
#14440=CARTESIAN_POINT ( 'NONE',  ( 46.25525774125583922, -33.99486860111965569, -44.64999999999999858 ) ) ;
#14443=CARTESIAN_POINT ( 'NONE',  ( 16.13393739769620083, -38.61618894467930119, 4.943674098299959851 ) ) ;
#14444=CARTESIAN_POINT ( 'NONE',  ( 44.79480296850380228, -38.01802765133241735, -66.34561246062233408 ) ) ;
#14465=EDGE_LOOP ( 'NONE', ( #39452, #21036 ) ) ;
#14494=ORIENTED_EDGE ( 'NONE', *, *, #10406, .T. ) ;
#14510=EDGE_CURVE ( 'NONE', #12905, #26981, #30100, .T. ) ;
#14511=CARTESIAN_POINT ( 'NONE',  ( 13.13393739769600010, 18.38381105532060289, -35.14999999999999858 ) ) ;
#14518=AXIS2_PLACEMENT_3D ( 'NONE', #1220, #48664, #12764 ) ;
#14533=CARTESIAN_POINT ( 'NONE',  ( 16.13393739769620083, -15.61618894467929941, -54.64999999999999858 ) ) ;
#14538=FACE_OUTER_BOUND ( 'NONE', #7787, .T. ) ;
#14542=EDGE_CURVE ( 'NONE', #885, #5705, #12442, .T. ) ;
#14555=B_SPLINE_CURVE_WITH_KNOTS ( 'NONE', 3,
 ( #8635, #1289, #24587, #24850, #36396, #40346, #8126, #32443 ),
 .UNSPECIFIED., .F., .F.,
 ( 4, 2, 2, 4 ),
 ( 0.04513248637254871354, 0.05146834906984269764, 0.06948743965982991100, 0.08616863070281119419 ),
 .UNSPECIFIED. ) ;
#14556=ORIENTED_EDGE ( 'NONE', *, *, #49523, .F. ) ;
#14559=VECTOR ( 'NONE', #2421, 1000.000000000000000 ) ;
#14569=DIRECTION ( 'NONE',  ( 0.000000000000000000, -1.000000000000000000, 0.000000000000000000 ) ) ;
#14581=ORIENTED_EDGE ( 'NONE', *, *, #37668, .F. ) ;
#14586=CARTESIAN_POINT ( 'NONE',  ( 45.77509190452501997, -40.08057006376965603, -58.05133673132166905 ) ) ;
#14595=ORIENTED_EDGE ( 'NONE', *, *, #21916, .F. ) ;
#14596=ADVANCED_FACE ( 'NONE', ( #38759 ), #26942, .T. ) ;
#14608=CARTESIAN_POINT ( 'NONE',  ( 0.4937122138108709923, -22.40531513632469895, -34.90839531524139971 ) ) ;
#14620=ORIENTED_EDGE ( 'NONE', *, *, #29983, .T. ) ;
#14629=ORIENTED_EDGE ( 'NONE', *, *, #39039, .F. ) ;
#14630=FACE_OUTER_BOUND ( 'NONE', #23680, .T. ) ;
#14634=DIRECTION ( 'NONE',  ( 0.000000000000000000, 1.000000000000000000, 0.000000000000000000 ) ) ;
#14641=DIRECTION ( 'NONE',  ( -0.000000000000000000, -1.000000000000000000, -0.000000000000000000 ) ) ;
#14654=CARTESIAN_POINT ( 'NONE',  ( -0.01911352800862239909, 19.70019394631319898, -34.82369549110249807 ) ) ;
#14656=CARTESIAN_POINT ( 'NONE',  ( 46.44081879553109360, -38.06850544220679922, -58.10139953457039752 ) ) ;
#14659=ORIENTED_EDGE ( 'NONE', *, *, #10406, .F. ) ;
#14662=VERTEX_POINT ( 'NONE', #43207 ) ;
#14663=CARTESIAN_POINT ( 'NONE',  ( 42.66089338409341281, 8.656733235152263006, -72.90937615055806020 ) ) ;
#14664=DIRECTION ( 'NONE',  ( 0.000000000000000000, 1.218758999999999977E-12, 1.000000000000000000 ) ) ;
#14673=ORIENTED_EDGE ( 'NONE', *, *, #25836, .T. ) ;
#14679=DIRECTION ( 'NONE',  ( -0.3863301728269282753, -0.9223605572461974766, 0.000000000000000000 ) ) ;
#14686=CIRCLE ( 'NONE', #43971, 2.999999999999999112 ) ;
#14689=ORIENTED_EDGE ( 'NONE', *, *, #38684, .T. ) ;
#14693=ORIENTED_EDGE ( 'NONE', *, *, #23312, .T. ) ;
#14695=DIRECTION ( 'NONE',  ( 1.000000000000000000, 0.000000000000000000, 0.000000000000000000 ) ) ;
#14701=CARTESIAN_POINT ( 'NONE',  ( 45.36210379758509248, -38.08434548607991132, -63.50911186322624502 ) ) ;
#14713=EDGE_CURVE ( 'NONE', #12186, #43432, #47400, .T. ) ;
#14714=CARTESIAN_POINT ( 'NONE',  ( 38.67452568954060155, 4.883811055320659733, -84.65000000000000568 ) ) ;
#14717=AXIS2_PLACEMENT_3D ( 'NONE', #18902, #51657, #35405 ) ;
#14721=AXIS2_PLACEMENT_3D ( 'NONE', #22497, #6282, #10211 ) ;
#14724=FACE_OUTER_BOUND ( 'NONE', #39961, .T. ) ;
#14740=CARTESIAN_POINT ( 'NONE',  ( 12.86517331568619937, 17.88381105532060289, -34.64999999999999858 ) ) ;
#14742=FACE_OUTER_BOUND ( 'NONE', #5458, .T. ) ;
#14754=ORIENTED_EDGE ( 'NONE', *, *, #38498, .F. ) ;
#14758=CARTESIAN_POINT ( 'NONE',  ( 0.6320745533423631768, -8.781616017679803932, -34.77490583097452514 ) ) ;
#14762=CARTESIAN_POINT ( 'NONE',  ( 43.01395769380430067, 6.547552581025015250, -75.24989832121792688 ) ) ;
#14765=ORIENTED_EDGE ( 'NONE', *, *, #18160, .T. ) ;
#14780=ORIENTED_EDGE ( 'NONE', *, *, #45307, .F. ) ;
#14785=CARTESIAN_POINT ( 'NONE',  ( 38.67452568954060155, 2.762490711761019124, -83.77132034355965118 ) ) ;
#14786=CYLINDRICAL_SURFACE ( 'NONE', #43159, 0.4999999999999986677 ) ;
#14788=DIRECTION ( 'NONE',  ( 0.3535533905932738974, -0.6123724356957941373, 0.7071067811865477948 ) ) ;
#14795=CARTESIAN_POINT ( 'NONE',  ( 37.13393739769620083, -49.11618894467930829, -35.14999999999999858 ) ) ;
#14805=ORIENTED_EDGE ( 'NONE', *, *, #29898, .T. ) ;
#14809=CARTESIAN_POINT ( 'NONE',  ( 45.56486364238802622, 8.835226115373638223, -59.07248904589445715 ) ) ;
#14810=CARTESIAN_POINT ( 'NONE',  ( 19.13393739769592727, 18.38381105532069526, -35.01561944896768352 ) ) ;
#14813=AXIS2_PLACEMENT_3D ( 'NONE', #3246, #51460, #31254 ) ;
#14816=ADVANCED_BREP_SHAPE_REPRESENTATION ( '', ( #10093, #20940 ), #50248 ) ;
#14817=ORIENTED_EDGE ( 'NONE', *, *, #34412, .F. ) ;
#14823=CARTESIAN_POINT ( 'NONE',  ( 20.63541822830437766, -51.88627667935604393, -69.46507341766410093 ) ) ;
#14828=CARTESIAN_POINT ( 'NONE',  ( 29.13393739769619728, 4.555383930574470774, -84.65000000000000568 ) ) ;
#14846=CARTESIAN_POINT ( 'NONE',  ( 45.42364261614932275, -40.05881144132143135, -59.75727053604451555 ) ) ;
#14849=CARTESIAN_POINT ( 'NONE',  ( 20.63393739769620083, -41.61618894467930119, -35.14999999999999858 ) ) ;
#14864=CARTESIAN_POINT ( 'NONE',  ( 8.773163716056640027, 17.21388800179359890, -41.74835365322499570 ) ) ;
#14884=ORIENTED_EDGE ( 'NONE', *, *, #27178, .F. ) ;
#14900=LINE ( 'NONE', #51581, #6858 ) ;
#14901=EDGE_CURVE ( 'NONE', #1290, #4073, #8320, .T. ) ;
#14909=ADVANCED_FACE ( 'NONE', ( #29003 ), #28740, .T. ) ;
#14911=PLANE ( 'NONE',  #12461 ) ;
#14912=CARTESIAN_POINT ( 'NONE',  ( -5.088235941628160397, 17.51416456853099746, -39.61904198186269355 ) ) ;
#14914=CARTESIAN_POINT ( 'NONE',  ( 47.49152231325319207, -38.14496413414819642, -52.84339506842029266 ) ) ;
#14915=DIRECTION ( 'NONE',  ( 1.000000000000000000, 0.000000000000000000, 0.000000000000000000 ) ) ;
#14916=FACE_OUTER_BOUND ( 'NONE', #10749, .T. ) ;
#14922=FACE_OUTER_BOUND ( 'NONE', #28639, .T. ) ;
#14929=DIRECTION ( 'NONE',  ( 0.000000000000000000, 0.000000000000000000, -1.000000000000000000 ) ) ;
#14939=AXIS2_PLACEMENT_3D ( 'NONE', #16963, #41060, #9093 ) ;
#14951=( BOUNDED_CURVE ( )  B_SPLINE_CURVE ( 3, ( #20298, #28162, #20817, #28680 ),
 .UNSPECIFIED., .F., .T. ) 
 B_SPLINE_CURVE_WITH_KNOTS ( ( 4, 4 ),
 ( 0.7853981633974057575, 1.570796326794889231 ),
 .UNSPECIFIED. ) 
 CURVE ( )  GEOMETRIC_REPRESENTATION_ITEM ( )  RATIONAL_B_SPLINE_CURVE ( ( 1.000000000000000000, 0.9492530216741866811, 0.9492530216741866811, 1.000000000000000000 ) ) 
 REPRESENTATION_ITEM ( '' )  );
#14952=ORIENTED_EDGE ( 'NONE', *, *, #45444, .T. ) ;
#14961=VERTEX_POINT ( 'NONE', #8587 ) ;
#14992=CARTESIAN_POINT ( 'NONE',  ( -0.2553902877309514596, -45.40777142809078271, -34.98886107151971459 ) ) ;
#15020=CARTESIAN_POINT ( 'NONE',  ( 43.64772454978100313, 6.637557646638361675, -72.08106405648152304 ) ) ;
#15022=EDGE_LOOP ( 'NONE', ( #5391, #25551 ) ) ;
#15025=AXIS2_PLACEMENT_3D ( 'NONE', #9585, #32877, #20835 ) ;
#15037=CARTESIAN_POINT ( 'NONE',  ( 4.133937397696209715, -8.687985714403829718, -35.14999999999999858 ) ) ;
#15043=AXIS2_PLACEMENT_3D ( 'NONE', #22732, #23242, #19591 ) ;
#15044=CARTESIAN_POINT ( 'NONE',  ( 14.14886614762370165, 1.362847559348080217, -35.02873218748179340 ) ) ;
#15056=CARTESIAN_POINT ( 'NONE',  ( 23.13393739769620083, -28.89524513604070322, -39.64999999999999858 ) ) ;
#15065=CARTESIAN_POINT ( 'NONE',  ( 46.10619593582758569, 8.867239705439473596, -56.44334475430651565 ) ) ;
#15070=ORIENTED_EDGE ( 'NONE', *, *, #38516, .F. ) ;
#15074=CARTESIAN_POINT ( 'NONE',  ( -0.01453923778984735939, -32.60559584230732355, 4.943674098299959851 ) ) ;
#15090=AXIS2_PLACEMENT_3D ( 'NONE', #47815, #11923, #23925 ) ;
#15092=DIRECTION ( 'NONE',  ( 0.6522074047277899300, 0.2731766849828906607, 0.7071067811865471286 ) ) ;
#15093=EDGE_CURVE ( 'NONE', #13277, #26382, #1923, .T. ) ;
#15106=CIRCLE ( 'NONE', #26921, 22.00000000000000000 ) ;
#15107=CARTESIAN_POINT ( 'NONE',  ( 45.44843781540670591, -40.06038511326323004, -59.63698597941407797 ) ) ;
#15118=VECTOR ( 'NONE', #2684, 1000.000000000000114 ) ;
#15122=AXIS2_PLACEMENT_3D ( 'NONE', #29110, #29370, #24641 ) ;
#15127=CARTESIAN_POINT ( 'NONE',  ( 16.13393739769620083, -1.759782484128330049, -47.64999999999999858 ) ) ;
#15131=PLANE ( 'NONE',  #46232 ) ;
#15134=ORIENTED_EDGE ( 'NONE', *, *, #36029, .T. ) ;
#15139=CARTESIAN_POINT ( 'NONE',  ( 16.13393739769620083, -15.61618894467929941, -35.12503119152809461 ) ) ;
#15142=VERTEX_POINT ( 'NONE', #27819 ) ;
#15144=FACE_OUTER_BOUND ( 'NONE', #26452, .T. ) ;
#15149=CARTESIAN_POINT ( 'NONE',  ( 46.98749101202549383, -39.23094825485602399, -34.79644638567071269 ) ) ;
#15159=DIRECTION ( 'NONE',  ( 0.6933752452815363787, 0.7071067811865472397, -0.1386750490563077587 ) ) ;
#15161=CARTESIAN_POINT ( 'NONE',  ( 8.744443678271633047, 17.71880458988568208, -34.77532226276706240 ) ) ;
#15166=CARTESIAN_POINT ( 'NONE',  ( -0.007164427059776000244, -22.82436266295209748, -34.77269723891829756 ) ) ;
#15167=CIRCLE ( 'NONE', #19347, 33.97624844042360337 ) ;
#15184=CARTESIAN_POINT ( 'NONE',  ( 43.06614223494208460, 7.660936950709002602, -75.35385097105195484 ) ) ;
#15187=CARTESIAN_POINT ( 'NONE',  ( 47.12245394960979894, -39.27662683125719667, -35.02700949942419584 ) ) ;
#15200=CONICAL_SURFACE ( 'NONE', #44519, 0.7349999999999987654, 0.06981317007977388966 ) ;
#15210=FACE_OUTER_BOUND ( 'NONE', #30056, .T. ) ;
#15217=ORIENTED_EDGE ( 'NONE', *, *, #39277, .F. ) ;
#15221=EDGE_CURVE ( 'NONE', #11609, #25171, #15777, .T. ) ;
#15224=DIRECTION ( 'NONE',  ( 0.8090169943749464521, -0.5877852522924744694, 0.000000000000000000 ) ) ;
#15228=ADVANCED_FACE ( 'NONE', ( #31731 ), #19449, .T. ) ;
#15232=CARTESIAN_POINT ( 'NONE',  ( 47.13393739769622215, 7.372368883616073454, -54.64997583104464951 ) ) ;
#15238=CIRCLE ( 'NONE', #35316, 3.000000000000004885 ) ;
#15240=EDGE_CURVE ( 'NONE', #14039, #15968, #45242, .T. ) ;
#15248=ORIENTED_EDGE ( 'NONE', *, *, #27849, .F. ) ;
#15270=EDGE_CURVE ( 'NONE', #40473, #50288, #34367, .T. ) ;
#15280=ORIENTED_EDGE ( 'NONE', *, *, #16851, .F. ) ;
#15283=CARTESIAN_POINT ( 'NONE',  ( 43.35947853168794808, 6.597306704977007108, -73.52222986434853169 ) ) ;
#15299=ADVANCED_FACE ( 'NONE', ( #15210 ), #10764, .T. ) ;
#15301=ORIENTED_EDGE ( 'NONE', *, *, #45781, .F. ) ;
#15310=AXIS2_PLACEMENT_3D ( 'NONE', #39522, #40030, #28213 ) ;
#15316=CARTESIAN_POINT ( 'NONE',  ( 0.2019267050627020776, 14.82321529695447992, -34.66067870389102978 ) ) ;
#15342=DIRECTION ( 'NONE',  ( 1.130501000000000083E-17, -8.343543999999999066E-19, -1.000000000000000000 ) ) ;
#15345=ORIENTED_EDGE ( 'NONE', *, *, #24450, .F. ) ;
#15347=CARTESIAN_POINT ( 'NONE',  ( 20.13393739769620083, -2.337132753317949785, -39.64999999999999858 ) ) ;
#15351=VECTOR ( 'NONE', #31355, 1000.000000000000000 ) ;
#15354=DIRECTION ( 'NONE',  ( 0.8660254037844259400, -0.5000000000000219824, 0.000000000000000000 ) ) ;
#15355=LINE ( 'NONE', #44939, #1621 ) ;
#15368=CARTESIAN_POINT ( 'NONE',  ( 45.59441226390927682, -40.06939850403506398, -58.92915879617162744 ) ) ;
#15381=ORIENTED_EDGE ( 'NONE', *, *, #8251, .F. ) ;
#15388=CARTESIAN_POINT ( 'NONE',  ( 29.35444738288253674, 4.484612253612125343, -84.62343415937573354 ) ) ;
#15419=CIRCLE ( 'NONE', #44691, 2.000000000000000000 ) ;
#15428=ORIENTED_EDGE ( 'NONE', *, *, #18899, .F. ) ;
#15440=CARTESIAN_POINT ( 'NONE',  ( 43.22703756266240305, -37.76642993860559727, -74.18277498300450645 ) ) ;
#15446=CARTESIAN_POINT ( 'NONE',  ( 42.37737783785518531, 7.575582158853551462, -78.76371035586005576 ) ) ;
#15459=ORIENTED_EDGE ( 'NONE', *, *, #39034, .T. ) ;
#15476=CARTESIAN_POINT ( 'NONE',  ( 19.31296351478369999, -49.88685839599860117, -82.14319696191608955 ) ) ;
#15481=PLANE ( 'NONE',  #12145 ) ;
#15482=CARTESIAN_POINT ( 'NONE',  ( 46.43957250303571982, -38.19754231318525939, -58.12182445229009886 ) ) ;
#15484=EDGE_LOOP ( 'NONE', ( #47358, #41822, #27362, #33724, #32561 ) ) ;
#15489=DIRECTION ( 'NONE',  ( -1.000000000000000000, 0.000000000000000000, 0.000000000000000000 ) ) ;
#15494=CARTESIAN_POINT ( 'NONE',  ( 16.13393739769620083, -15.61618894467929941, -54.64999999999999858 ) ) ;
#15500=B_SPLINE_CURVE_WITH_KNOTS ( 'NONE', 3,
 ( #1512, #36894, #9390, #1767 ),
 .UNSPECIFIED., .F., .F.,
 ( 4, 4 ),
 ( 0.000000000000000000, 19.53260001849420036 ),
 .UNSPECIFIED. ) ;
#15521=CARTESIAN_POINT ( 'NONE',  ( 11.63245656709279707, 20.65389878998962203, -69.46507341771521737 ) ) ;
#15526=DIRECTION ( 'NONE',  ( 0.000000000000000000, -1.000000000000000000, 0.000000000000000000 ) ) ;
#15528=ORIENTED_EDGE ( 'NONE', *, *, #12073, .T. ) ;
#15529=ORIENTED_EDGE ( 'NONE', *, *, #34538, .F. ) ;
#15539=CARTESIAN_POINT ( 'NONE',  ( 44.88993838878230491, 6.796999361193691414, -65.86996340926405935 ) ) ;
#15541=EDGE_LOOP ( 'NONE', ( #8747, #11454 ) ) ;
#15551=AXIS2_PLACEMENT_3D ( 'NONE', #43216, #34811, #11243 ) ;
#15554=ADVANCED_FACE ( 'NONE', ( #24577 ), #45641, .T. ) ;
#15566=LINE ( 'NONE', #23390, #37185 ) ;
#15567=CARTESIAN_POINT ( 'NONE',  ( 18.13393739769620083, -37.52509124488599923, -54.64999999999999858 ) ) ;
#15568=FACE_OUTER_BOUND ( 'NONE', #9404, .T. ) ;
#15586=ORIENTED_EDGE ( 'NONE', *, *, #22963, .F. ) ;
#15593=ORIENTED_EDGE ( 'NONE', *, *, #42495, .F. ) ;
#15607=ORIENTED_EDGE ( 'NONE', *, *, #44250, .F. ) ;
#15615=CARTESIAN_POINT ( 'NONE',  ( 41.13393739769620083, -15.61618894467929941, -84.65000000000000568 ) ) ;
#15625=CARTESIAN_POINT ( 'NONE',  ( 43.65187991923512101, -39.92530307977908421, -68.34537732784100683 ) ) ;
#15626=CARTESIAN_POINT ( 'NONE',  ( 0.3209249304026170480, -10.53407907283069989, -34.64999999999999858 ) ) ;
#15637=ORIENTED_EDGE ( 'NONE', *, *, #6403, .F. ) ;
#15644=CARTESIAN_POINT ( 'NONE',  ( 30.20787008543632268, 4.384392329102540842, -84.60813810823577796 ) ) ;
#15647=CARTESIAN_POINT ( 'NONE',  ( 0.08561865832223169992, 19.91752656751279815, -35.04144726298140000 ) ) ;
#15657=CARTESIAN_POINT ( 'NONE',  ( 40.79482532997379707, -39.62505393422780031, -82.14319696191608955 ) ) ;
#15658=LINE ( 'NONE', #24001, #15351 ) ;
#15664=ADVANCED_FACE ( 'NONE', ( #23264 ), #39282, .T. ) ;
#15666=VERTEX_POINT ( 'NONE', #19357 ) ;
#15679=CARTESIAN_POINT ( 'NONE',  ( 47.13393649688870113, -39.28050833195659663, -53.76790015415899404 ) ) ;
#15686=CARTESIAN_POINT ( 'NONE',  ( 8.897806153503669435, -49.24610395064770074, -34.65445009297679491 ) ) ;
#15694=ORIENTED_EDGE ( 'NONE', *, *, #36784, .T. ) ;
#15697=CARTESIAN_POINT ( 'NONE',  ( 44.82719368195827769, 6.561635999693602450, -66.13899901678205140 ) ) ;
#15699=DIRECTION ( 'NONE',  ( 1.000000000000000000, 0.000000000000000000, 0.000000000000000000 ) ) ;
#15707=VERTEX_POINT ( 'NONE', #19614 ) ;
#15711=( BOUNDED_CURVE ( )  B_SPLINE_CURVE ( 3, ( #31791, #28120, #47807, #16083 ),
 .UNSPECIFIED., .F., .T. ) 
 B_SPLINE_CURVE_WITH_KNOTS ( ( 4, 4 ),
 ( 1.570796326794896558, 2.356194490192344837 ),
 .UNSPECIFIED. ) 
 CURVE ( )  GEOMETRIC_REPRESENTATION_ITEM ( )  RATIONAL_B_SPLINE_CURVE ( ( 1.000000000000000000, 0.9492530216741911220, 0.9492530216741911220, 1.000000000000000000 ) ) 
 REPRESENTATION_ITEM ( '' )  );
#15721=CARTESIAN_POINT ( 'NONE',  ( 23.53669455186071602, -48.92556967366427756, -34.79644561402096770 ) ) ;
#15726=CARTESIAN_POINT ( 'NONE',  ( 19.40270147970570136, 17.88381105532069881, -34.64999999999999858 ) ) ;
#15729=VECTOR ( 'NONE', #46169, 1000.000000000000000 ) ;
#15732=DIRECTION ( 'NONE',  ( 1.000000000000000000, 0.000000000000000000, 0.000000000000000000 ) ) ;
#15751=CARTESIAN_POINT ( 'NONE',  ( 46.63393739769619373, -15.61618894467929941, -35.14999999999999858 ) ) ;
#15758=VECTOR ( 'NONE', #19590, 1000.000000000000000 ) ;
#15777=LINE ( 'NONE', #47252, #16764 ) ;
#15778=VERTEX_POINT ( 'NONE', #13513 ) ;
#15781=ADVANCED_FACE ( 'NONE', ( #45215 ), #34165, .T. ) ;
#15785=CARTESIAN_POINT ( 'NONE',  ( 1.055648624548729986, -8.645219027462792027, -34.65000333055159842 ) ) ;
#15786=ORIENTED_EDGE ( 'NONE', *, *, #48761, .F. ) ;
#15787=CARTESIAN_POINT ( 'NONE',  ( -0.1295185695944109927, -31.87964491196989414, -59.64999999999999147 ) ) ;
#15788=CARTESIAN_POINT ( 'NONE',  ( 45.02469926346807938, 6.813230800168343926, -65.19619103482980904 ) ) ;
#15796=FACE_OUTER_BOUND ( 'NONE', #27894, .T. ) ;
#15797=AXIS2_PLACEMENT_3D ( 'NONE', #49198, #44993, #29247 ) ;
#15815=DIRECTION ( 'NONE',  ( 0.000000000000000000, 0.000000000000000000, 1.000000000000000000 ) ) ;
#15821=CARTESIAN_POINT ( 'NONE',  ( 0.3188172270368339611, 15.01558124385560156, -34.65000333199999716 ) ) ;
#15828=CARTESIAN_POINT ( 'NONE',  ( 19.13393739769600188, 18.38381105532069881, -34.64999999999999858 ) ) ;
#15831=CARTESIAN_POINT ( 'NONE',  ( 22.15575932996830133, -54.10246922935670000, -34.93361312117490058 ) ) ;
#15834=CIRCLE ( 'NONE', #31698, 3.000000000000005773 ) ;
#15840=ORIENTED_EDGE ( 'NONE', *, *, #25631, .T. ) ;
#15842=AXIS2_PLACEMENT_3D ( 'NONE', #51671, #3206, #27549 ) ;
#15847=CARTESIAN_POINT ( 'NONE',  ( -11.26666115314075967, -34.90345733776890569, -44.56356395724966291 ) ) ;
#15854=B_SPLINE_CURVE_WITH_KNOTS ( 'NONE', 3,
 ( #44535, #17023, #502, #20929 ),
 .UNSPECIFIED., .F., .F.,
 ( 4, 4 ),
 ( 0.000000000000000000, 1.000000000000000000 ),
 .UNSPECIFIED. ) ;
#15866=VECTOR ( 'NONE', #46309, 1000.000000000000000 ) ;
#15867=VECTOR ( 'NONE', #26217, 1000.000000000000000 ) ;
#15876=CARTESIAN_POINT ( 'NONE',  ( 10.13393739769619906, -54.15188668067469990, -54.64999999999999858 ) ) ;
#15880=CARTESIAN_POINT ( 'NONE',  ( 42.24293144673103484, -39.79048127957475600, -75.15823207472831768 ) ) ;
#15897=CARTESIAN_POINT ( 'NONE',  ( 41.30555080485065389, 8.453905220434588585, -79.68287709513984396 ) ) ;
#15899=CARTESIAN_POINT ( 'NONE',  ( 29.58089024243311371, 4.434971018804394483, -84.61624959000400281 ) ) ;
#15902=DIRECTION ( 'NONE',  ( -0.1961161351381840445, 0.000000000000000000, -0.9805806756909201116 ) ) ;
#15912=CIRCLE ( 'NONE', #19272, 2.000000000000000000 ) ;
#15916=DIRECTION ( 'NONE',  ( 0.000000000000000000, -1.000000000000000000, 0.000000000000000000 ) ) ;
#15927=DIRECTION ( 'NONE',  ( 1.000000000000000000, 0.000000000000000000, 0.000000000000000000 ) ) ;
#15935=CARTESIAN_POINT ( 'NONE',  ( 46.47536507427530239, -40.11920440292289669, -54.64999999999999858 ) ) ;
#15939=CARTESIAN_POINT ( 'NONE',  ( 16.13393739769620083, -45.61618894467940066, -34.64999999999999858 ) ) ;
#15946=CARTESIAN_POINT ( 'NONE',  ( -0.007164378094141890356, 19.48649803870589992, -34.77269719633950018 ) ) ;
#15947=AXIS2_PLACEMENT_3D ( 'NONE', #9737, #25696, #21769 ) ;
#15951=CARTESIAN_POINT ( 'NONE',  ( 0.4394934780714839784, -8.845007899843928101, -35.02127583263639821 ) ) ;
#15953=DIRECTION ( 'NONE',  ( 0.000000000000000000, 0.000000000000000000, 1.000000000000000000 ) ) ;
#15955=VERTEX_POINT ( 'NONE', #50385 ) ;
#15959=CARTESIAN_POINT ( 'NONE',  ( 44.91829444253557568, 7.853016399853718355, -66.18824355412928639 ) ) ;
#15960=CARTESIAN_POINT ( 'NONE',  ( 14.13393739769620439, -41.61618894467939356, -35.01561944896766221 ) ) ;
#15966=ORIENTED_EDGE ( 'NONE', *, *, #14542, .T. ) ;
#15968=VERTEX_POINT ( 'NONE', #22830 ) ;
#15981=VERTEX_POINT ( 'NONE', #10289 ) ;
#15989=AXIS2_PLACEMENT_3D ( 'NONE', #29474, #17435, #24486 ) ;
#15995=CARTESIAN_POINT ( 'NONE',  ( 46.64491461174982589, -38.21744283867312220, -57.09507837764103755 ) ) ;
#15996=ORIENTED_EDGE ( 'NONE', *, *, #470, .T. ) ;
#16003=CARTESIAN_POINT ( 'NONE',  ( 0.1039241094638853335, 19.62646979462214603, -34.69896165024965029 ) ) ;
#16005=EDGE_CURVE ( 'NONE', #32504, #20085, #46463, .T. ) ;
#16025=CARTESIAN_POINT ( 'NONE',  ( -0.2175830584369590204, -45.44300788545632486, -34.95572367894526877 ) ) ;
#16039=ORIENTED_EDGE ( 'NONE', *, *, #51371, .T. ) ;
#16040=DIRECTION ( 'NONE',  ( 0.000000000000000000, 0.000000000000000000, -1.000000000000000000 ) ) ;
#16047=CARTESIAN_POINT ( 'NONE',  ( 42.00942139458377511, 6.392864097679653135, -80.27251128686401671 ) ) ;
#16053=CIRCLE ( 'NONE', #5182, 2.500000000000003553 ) ;
#16059=CARTESIAN_POINT ( 'NONE',  ( 19.13393739769620083, -49.61618894467939356, -35.14999999999999858 ) ) ;
#16069=CARTESIAN_POINT ( 'NONE',  ( 15.01109173769490113, 12.72875286183729848, -62.64999999999999858 ) ) ;
#16073=CARTESIAN_POINT ( 'NONE',  ( -0.007164427059776000244, -4.186223695871990280, -34.77269723891829756 ) ) ;
#16079=DIRECTION ( 'NONE',  ( 0.000000000000000000, 0.000000000000000000, -1.000000000000000000 ) ) ;
#16083=CARTESIAN_POINT ( 'NONE',  ( 20.53650276133985031, -41.76263555408612405, -34.79644660940672907 ) ) ;
#16093=EDGE_CURVE ( 'NONE', #46682, #14108, #19688, .T. ) ;
#16095=VERTEX_POINT ( 'NONE', #35681 ) ;
#16112=CARTESIAN_POINT ( 'NONE',  ( 22.13393739769589885, 22.91950879131610108, -54.64999999999999858 ) ) ;
#16126=CARTESIAN_POINT ( 'NONE',  ( 44.17593333301926606, -39.96876567252856205, -65.80818625478011086 ) ) ;
#16127=EDGE_CURVE ( 'NONE', #29610, #17159, #28566, .T. ) ;
#16142=CYLINDRICAL_SURFACE ( 'NONE', #19557, 3.000000000000000444 ) ;
#16145=CARTESIAN_POINT ( 'NONE',  ( 42.89541628683672059, 8.623681277660011801, -72.00529067016060480 ) ) ;
#16146=CARTESIAN_POINT ( 'NONE',  ( 44.66436339216802764, -33.16345305600000870, -44.75696816342043860 ) ) ;
#16148=CARTESIAN_POINT ( 'NONE',  ( 8.943569970476740849, -49.33365190531349498, -34.64999999999999858 ) ) ;
#16164=CARTESIAN_POINT ( 'NONE',  ( -20.68272678989470847, -2.738091952025576425, -53.00346737314672652 ) ) ;
#16166=CARTESIAN_POINT ( 'NONE',  ( 40.57649240635721100, 6.328436186825659782, -83.97002642401369599 ) ) ;
#16168=CARTESIAN_POINT ( 'NONE',  ( 9.894687805641389389, -53.60726374558549878, -34.64999999999999858 ) ) ;
#16169=ORIENTED_EDGE ( 'NONE', *, *, #32427, .T. ) ;
#16186=EDGE_CURVE ( 'NONE', #621, #32837, #33792, .T. ) ;
#16197=EDGE_CURVE ( 'NONE', #42105, #37038, #37742, .T. ) ;
#16203=ORIENTED_EDGE ( 'NONE', *, *, #24022, .F. ) ;
#16206=CARTESIAN_POINT ( 'NONE',  ( 42.09413162889060089, 6.247507344166270293, -79.82720547731395300 ) ) ;
#16216=ORIENTED_EDGE ( 'NONE', *, *, #23519, .T. ) ;
#16219=EDGE_CURVE ( 'NONE', #4886, #42739, #16950, .T. ) ;
#16220=ORIENTED_EDGE ( 'NONE', *, *, #29496, .T. ) ;
#16226=CARTESIAN_POINT ( 'NONE',  ( 0.03129314105497079529, -10.48887801743429904, -34.73925587534019854 ) ) ;
#16231=VERTEX_POINT ( 'NONE', #45873 ) ;
#16232=CARTESIAN_POINT ( 'NONE',  ( 17.20688454841970128, 14.56395709402249850, -35.14999999999999858 ) ) ;
#16236=ORIENTED_EDGE ( 'NONE', *, *, #32723, .F. ) ;
#16239=DIRECTION ( 'NONE',  ( 0.000000000000000000, 0.000000000000000000, 1.000000000000000000 ) ) ;
#16240=CARTESIAN_POINT ( 'NONE',  ( 2.423250969874880312, -25.81972099615670047, -35.01387690002259490 ) ) ;
#16244=DIRECTION ( 'NONE',  ( 0.000000000000000000, 1.000000000000000000, 0.000000000000000000 ) ) ;
#16246=ORIENTED_EDGE ( 'NONE', *, *, #22376, .T. ) ;
#16249=CYLINDRICAL_SURFACE ( 'NONE', #17826, 0.4999999999999991118 ) ;
#16252=DIRECTION ( 'NONE',  ( 1.000000000000000000, 0.000000000000000000, 0.000000000000000000 ) ) ;
#16278=EDGE_LOOP ( 'NONE', ( #18138, #12423, #51537, #4525, #33251 ) ) ;
#16279=CARTESIAN_POINT ( 'NONE',  ( -1.839728563314089849, -28.30269090235150031, -54.64999999999999858 ) ) ;
#16285=LINE ( 'NONE', #32491, #18296 ) ;
#16289=ORIENTED_EDGE ( 'NONE', *, *, #40885, .F. ) ;
#16293=FACE_BOUND ( 'NONE', #10438, .T. ) ;
#16299=CARTESIAN_POINT ( 'NONE',  ( 42.30872906436815128, 6.440492890468437537, -78.77604134614341547 ) ) ;
#16303=EDGE_CURVE ( 'NONE', #20524, #29117, #10227, .T. ) ;
#16306=CARTESIAN_POINT ( 'NONE',  ( 42.22142201539555373, -37.65884987249721405, -79.21256181789661355 ) ) ;
#16315=( BOUNDED_CURVE ( )  B_SPLINE_CURVE ( 3, ( #7818, #3889, #23771, #15166 ),
 .UNSPECIFIED., .F., .T. ) 
 B_SPLINE_CURVE_WITH_KNOTS ( ( 4, 4 ),
 ( 5.907914484323606885, 5.977569058052071505 ),
 .UNSPECIFIED. ) 
 CURVE ( )  GEOMETRIC_REPRESENTATION_ITEM ( )  RATIONAL_B_SPLINE_CURVE ( ( 1.000000000000000000, 0.9995957275622183724, 0.9995957275622183724, 1.000000000000000000 ) ) 
 REPRESENTATION_ITEM ( '' )  );
#16320=ORIENTED_EDGE ( 'NONE', *, *, #11528, .F. ) ;
#16322=VECTOR ( 'NONE', #27648, 1000.000000000000114 ) ;
#16348=VERTEX_POINT ( 'NONE', #47171 ) ;
#16358=EDGE_LOOP ( 'NONE', ( #19539, #30567, #38133, #10358 ) ) ;
#16360=CIRCLE ( 'NONE', #29737, 3.000000000000001776 ) ;
#16365=EDGE_CURVE ( 'NONE', #2651, #41542, #2621, .T. ) ;
#16369=VERTEX_POINT ( 'NONE', #18076 ) ;
#16371=CARTESIAN_POINT ( 'NONE',  ( 21.50893739769619728, 1.920825481955539926, -35.14999999999999858 ) ) ;
#16376=DIRECTION ( 'NONE',  ( 0.6339889056055382222, 0.000000000000000000, -0.7733421413379021336 ) ) ;
#16382=CARTESIAN_POINT ( 'NONE',  ( 23.53017837589169048, -48.93815596428016335, -34.78557451168259718 ) ) ;
#16387=CARTESIAN_POINT ( 'NONE',  ( 42.67110578209099714, -39.83399799466496205, -73.09004855766275455 ) ) ;
#16401=CYLINDRICAL_SURFACE ( 'NONE', #783, 0.4999999999999983347 ) ;
#16405=CARTESIAN_POINT ( 'NONE',  ( 42.55931733926811233, 8.590583294249910296, -73.62972220888975983 ) ) ;
#16407=CARTESIAN_POINT ( 'NONE',  ( 29.75529164732110132, 4.407650919513039334, -84.61197749185016903 ) ) ;
#16408=CYLINDRICAL_SURFACE ( 'NONE', #19419, 0.4999999999999982236 ) ;
#16422=CARTESIAN_POINT ( 'NONE',  ( -0.2999272097369983237, 14.12533709486001499, -35.02742413524038767 ) ) ;
#16424=CARTESIAN_POINT ( 'NONE',  ( 0.1457841021255935343, -22.91266753744946527, -34.68167779225149161 ) ) ;
#16431=CYLINDRICAL_SURFACE ( 'NONE', #40040, 0.4999999999999993894 ) ;
#16445=EDGE_LOOP ( 'NONE', ( #2247, #44192, #24252, #24120 ) ) ;
#16448=FACE_OUTER_BOUND ( 'NONE', #3674, .T. ) ;
#16453=CIRCLE ( 'NONE', #44937, 0.4905819419822178840 ) ;
#16463=CARTESIAN_POINT ( 'NONE',  ( 14.13393739769619906, -41.61618894467930119, -35.14999999999999858 ) ) ;
#16464=DIRECTION ( 'NONE',  ( 0.000000000000000000, 0.000000000000000000, 1.000000000000000000 ) ) ;
#16471=VERTEX_POINT ( 'NONE', #7840 ) ;
#16483=VECTOR ( 'NONE', #19081, 1000.000000000000000 ) ;
#16484=EDGE_CURVE ( 'NONE', #7979, #16490, #27642, .T. ) ;
#16486=CARTESIAN_POINT ( 'NONE',  ( 18.13393739769630031, 0.3838110553206460218, -34.64999999999999858 ) ) ;
#16487=FACE_OUTER_BOUND ( 'NONE', #37669, .T. ) ;
#16490=VERTEX_POINT ( 'NONE', #16463 ) ;
#16500=EDGE_LOOP ( 'NONE', ( #15840, #49765, #45044, #501, #49029, #11378 ) ) ;
#16503=AXIS2_PLACEMENT_3D ( 'NONE', #24872, #20954, #31964 ) ;
#16505=DIRECTION ( 'NONE',  ( 1.000000000000000000, 0.000000000000000000, 0.000000000000000000 ) ) ;
#16521=EDGE_CURVE ( 'NONE', #4162, #7979, #476, .T. ) ;
#16541=DIRECTION ( 'NONE',  ( 0.5320619775582980937, 0.8460488748893841837, -0.03333696649607501700 ) ) ;
#16543=ORIENTED_EDGE ( 'NONE', *, *, #3732, .F. ) ;
#16544=VERTEX_POINT ( 'NONE', #23273 ) ;
#16553=FACE_OUTER_BOUND ( 'NONE', #30006, .T. ) ;
#16559=CARTESIAN_POINT ( 'NONE',  ( 41.92858229088276545, -37.61218635125683107, -80.67670930047889044 ) ) ;
#16597=VERTEX_POINT ( 'NONE', #28765 ) ;
#16600=CYLINDRICAL_SURFACE ( 'NONE', #48569, 0.4999999999999982236 ) ;
#16602=VERTEX_POINT ( 'NONE', #37165 ) ;
#16608=CARTESIAN_POINT ( 'NONE',  ( 28.63393739769619728, -8.399310579809030841, -34.64999999999999858 ) ) ;
#16617=EDGE_CURVE ( 'NONE', #9565, #31436, #29016, .T. ) ;
#16623=CARTESIAN_POINT ( 'NONE',  ( 19.40270147970570136, 17.88381105532069881, -34.64999999999999858 ) ) ;
#16632=DIRECTION ( 'NONE',  ( 0.000000000000000000, 1.000000000000000000, 0.000000000000000000 ) ) ;
#16636=CARTESIAN_POINT ( 'NONE',  ( 17.98749448546718455, 1.245406012443906807, -34.79644291222912500 ) ) ;
#16637=CARTESIAN_POINT ( 'NONE',  ( 23.32557412215910020, -49.33122573608360284, -34.65000333295999724 ) ) ;
#16640=CARTESIAN_POINT ( 'NONE',  ( 43.29044952474772145, -39.89310745266933367, -70.09458329593303461 ) ) ;
#16645=CARTESIAN_POINT ( 'NONE',  ( -0.3016046179078940015, -10.91500322974829906, -35.02873218748179340 ) ) ;
#16662=CARTESIAN_POINT ( 'NONE',  ( 42.51301359343917596, 8.585954781958603732, -73.85330097299451779 ) ) ;
#16663=CARTESIAN_POINT ( 'NONE',  ( -0.03447620312152044342, -8.421650097910747590, -34.79644660940672196 ) ) ;
#16665=PLANE ( 'NONE',  #193 ) ;
#16671=FACE_OUTER_BOUND ( 'NONE', #3803, .T. ) ;
#16679=CARTESIAN_POINT ( 'NONE',  ( 28.28038400710291356, -22.62894316431776431, -34.79644660940672907 ) ) ;
#16681=CARTESIAN_POINT ( 'NONE',  ( 25.43010376912519988, -1.113097814880039893, -35.14999999999999858 ) ) ;
#16714=ADVANCED_FACE ( 'NONE', ( #33214 ), #1000, .T. ) ;
#16722=ORIENTED_EDGE ( 'NONE', *, *, #49918, .T. ) ;
#16724=CARTESIAN_POINT ( 'NONE',  ( 2.458146360389407370, -5.580163940743402051, -34.79644291222906105 ) ) ;
#16725=CARTESIAN_POINT ( 'NONE',  ( -27.57791469522849681, 115.8715079793770144, -50.15833750720749862 ) ) ;
#16731=DIRECTION ( 'NONE',  ( -0.5516667872527352134, -0.8340645993220461296, 0.000000000000000000 ) ) ;
#16743=ORIENTED_EDGE ( 'NONE', *, *, #41482, .F. ) ;
#16744=EDGE_CURVE ( 'NONE', #4837, #29074, #51152, .T. ) ;
#16749=DIRECTION ( 'NONE',  ( -0.5897727341282608116, 0.3900873262218075288, 0.7071067811865454633 ) ) ;
#16751=CARTESIAN_POINT ( 'NONE',  ( 22.37318698975099807, -53.60726374558549878, -34.64999999999999858 ) ) ;
#16757=CARTESIAN_POINT ( 'NONE',  ( 45.68512934788851965, 2.192362318393687115, -54.50653973161867327 ) ) ;
#16763=PLANE ( 'NONE',  #7794 ) ;
#16764=VECTOR ( 'NONE', #30973, 1000.000000000000000 ) ;
#16768=DIRECTION ( 'NONE',  ( -0.000000000000000000, -1.000000000000000000, -0.000000000000000000 ) ) ;
#16769=FACE_OUTER_BOUND ( 'NONE', #40026, .T. ) ;
#16776=( BOUNDED_CURVE ( )  B_SPLINE_CURVE ( 3, ( #1981, #18989, #14810, #46018 ),
 .UNSPECIFIED., .F., .T. ) 
 B_SPLINE_CURVE_WITH_KNOTS ( ( 4, 4 ),
 ( 2.356194490192476731, 3.141592653589780237 ),
 .UNSPECIFIED. ) 
 CURVE ( )  GEOMETRIC_REPRESENTATION_ITEM ( )  RATIONAL_B_SPLINE_CURVE ( ( 1.000000000000000000, 0.9492530216742096627, 0.9492530216742096627, 1.000000000000000000 ) ) 
 REPRESENTATION_ITEM ( '' )  );
#16811=AXIS2_PLACEMENT_3D ( 'NONE', #25030, #30004, #45763 ) ;
#16817=CARTESIAN_POINT ( 'NONE',  ( 11.63393739769600010, 10.38381105532060111, -34.64999999999999858 ) ) ;
#16825=ORIENTED_EDGE ( 'NONE', *, *, #6568, .T. ) ;
#16830=CARTESIAN_POINT ( 'NONE',  ( 41.70677336635860399, -37.57567824672890566, -81.78581377007661501 ) ) ;
#16834=EDGE_CURVE ( 'NONE', #21125, #49316, #34232, .T. ) ;
#16839=CONICAL_SURFACE ( 'NONE', #47828, 19.50000000000000000, 0.2449786631268651149 ) ;
#16851=EDGE_CURVE ( 'NONE', #46513, #621, #35245, .T. ) ;
#16852=EDGE_LOOP ( 'NONE', ( #45626, #28763, #30852, #22971 ) ) ;
#16859=ADVANCED_FACE ( 'NONE', ( #22960 ), #31887, .F. ) ;
#16871=CARTESIAN_POINT ( 'NONE',  ( 37.88393739769619373, -42.11618894467939356, -35.14999999999999858 ) ) ;
#16890=ORIENTED_EDGE ( 'NONE', *, *, #20981, .T. ) ;
#16895=CARTESIAN_POINT ( 'NONE',  ( 47.13393657218789912, 8.048130458325550407, -53.76789950451890121 ) ) ;
#16903=EDGE_CURVE ( 'NONE', #42065, #9584, #38723, .T. ) ;
#16916=CARTESIAN_POINT ( 'NONE',  ( 41.33525829054640610, -39.68972903983045342, -79.53966819202405247 ) ) ;
#16920=( LENGTH_UNIT ( ) NAMED_UNIT ( * ) SI_UNIT ( .MILLI., .METRE. ) );
#16922=ADVANCED_FACE ( 'NONE', ( #13829 ), #26906, .T. ) ;
#16935=CARTESIAN_POINT ( 'NONE',  ( 44.13393739769620083, 4.883811055320659733, -44.64999999999999858 ) ) ;
#16937=CARTESIAN_POINT ( 'NONE',  ( 42.57056998323533747, 8.591712343070616598, -73.57535562139177898 ) ) ;
#16938=CARTESIAN_POINT ( 'NONE',  ( 44.66663217887202109, -33.16386166677794733, -44.71403636873775156 ) ) ;
#16945=ORIENTED_EDGE ( 'NONE', *, *, #47880, .F. ) ;
#16946=DIRECTION ( 'NONE',  ( 1.000000000000000000, 0.000000000000000000, 0.000000000000000000 ) ) ;
#16948=CARTESIAN_POINT ( 'NONE',  ( 3.633937397696210159, -22.83306730954970121, -34.64999999999999858 ) ) ;
#16950=( BOUNDED_CURVE ( )  B_SPLINE_CURVE ( 3, ( #40891, #17313, #9957, #29602 ),
 .UNSPECIFIED., .F., .T. ) 
 B_SPLINE_CURVE_WITH_KNOTS ( ( 4, 4 ),
 ( 0.7853981633974557175, 1.570796326794896558 ),
 .UNSPECIFIED. ) 
 CURVE ( )  GEOMETRIC_REPRESENTATION_ITEM ( )  RATIONAL_B_SPLINE_CURVE ( ( 1.000000000000000000, 0.9492530216741921212, 0.9492530216741921212, 1.000000000000000000 ) ) 
 REPRESENTATION_ITEM ( '' )  );
#16951=DIRECTION ( 'NONE',  ( 0.000000000000000000, 0.000000000000000000, -1.000000000000000000 ) ) ;
#16954=CARTESIAN_POINT ( 'NONE',  ( -0.1800306480951155419, 14.24857142054698755, -34.92293865398471553 ) ) ;
#16956=CYLINDRICAL_SURFACE ( 'NONE', #34599, 0.4999999999999985012 ) ;
#16958=CARTESIAN_POINT ( 'NONE',  ( 16.13393739769620083, -1.759782484128330049, -35.14999999999999858 ) ) ;
#16959=CARTESIAN_POINT ( 'NONE',  ( 29.13393739769619728, 4.883811055320659733, -81.65000000000000568 ) ) ;
#16963=CARTESIAN_POINT ( 'NONE',  ( 16.13393739769620083, -15.61618894467929941, -84.65000000000000568 ) ) ;
#16983=CARTESIAN_POINT ( 'NONE',  ( 0.3188167964973340207, 19.48786055945209839, -34.65000333314139169 ) ) ;
#16988=ADVANCED_FACE ( 'NONE', ( #28184 ), #4092, .T. ) ;
#16999=LINE ( 'NONE', #12541, #261 ) ;
#17001=CARTESIAN_POINT ( 'NONE',  ( 0.4371248283887909647, -22.38658506580789975, -35.02873218748179340 ) ) ;
#17021=CARTESIAN_POINT ( 'NONE',  ( 22.33082320214449723, -53.70417188095220240, -34.65604926186109935 ) ) ;
#17023=CARTESIAN_POINT ( 'NONE',  ( 17.16548900651949694, -43.89919387818898855, -61.51477253168923909 ) ) ;
#17037=CARTESIAN_POINT ( 'NONE',  ( 0.08961746015897585627, -22.88023971159056202, -34.70268271585497644 ) ) ;
#17045=VECTOR ( 'NONE', #49491, 999.9999999999998863 ) ;
#17046=DIRECTION ( 'NONE',  ( -1.000000000000000000, 0.000000000000000000, 0.000000000000000000 ) ) ;
#17050=CARTESIAN_POINT ( 'NONE',  ( 9.133937397696369587, 7.383811055320710359, -59.64999999999999147 ) ) ;
#17052=ORIENTED_EDGE ( 'NONE', *, *, #22376, .F. ) ;
#17065=ORIENTED_EDGE ( 'NONE', *, *, #43621, .F. ) ;
#17067=ORIENTED_EDGE ( 'NONE', *, *, #45697, .T. ) ;
#17076=CIRCLE ( 'NONE', #3683, 0.5000000000000004441 ) ;
#17090=CARTESIAN_POINT ( 'NONE',  ( 30.13393739769619728, -38.61618894467930119, -72.14999999999999147 ) ) ;
#17097=CARTESIAN_POINT ( 'NONE',  ( 42.64205722919412267, -37.72423225234104649, -77.10933407075954449 ) ) ;
#17113=ADVANCED_FACE ( 'NONE', ( #11975 ), #48122, .T. ) ;
#17120=CARTESIAN_POINT ( 'NONE',  ( 18.08251218718402953, -41.66761415519155776, -34.89146800830128825 ) ) ;
#17127=CIRCLE ( 'NONE', #29637, 5.251829701412240148 ) ;
#17131=ORIENTED_EDGE ( 'NONE', *, *, #19140, .T. ) ;
#17132=DIRECTION ( 'NONE',  ( -1.000000000000000000, 0.000000000000000000, 0.000000000000000000 ) ) ;
#17134=CARTESIAN_POINT ( 'NONE',  ( 33.38393739769599478, 10.88381105532080007, -35.14999999999999858 ) ) ;
#17157=VERTEX_POINT ( 'NONE', #19307 ) ;
#17158=ADVANCED_FACE ( 'NONE', ( #43932 ), #15200, .F. ) ;
#17159=VERTEX_POINT ( 'NONE', #40258 ) ;
#17189=CARTESIAN_POINT ( 'NONE',  ( 0.1155611319282749960, -51.17475502668380472, -35.14999999933320396 ) ) ;
#17193=CARTESIAN_POINT ( 'NONE',  ( 45.02421615755568496, 8.799843003901896665, -61.69522525134451740 ) ) ;
#17194=EDGE_CURVE ( 'NONE', #14108, #19168, #28444, .T. ) ;
#17195=VECTOR ( 'NONE', #12386, 1000.000000000000114 ) ;
#17196=DIRECTION ( 'NONE',  ( 0.6522074047277948150, -0.2731766849828846100, 0.7071067811865450192 ) ) ;
#17206=EDGE_LOOP ( 'NONE', ( #11707, #38945, #50829, #44076, #39507 ) ) ;
#17209=ORIENTED_EDGE ( 'NONE', *, *, #21679, .F. ) ;
#17211=DIRECTION ( 'NONE',  ( -0.6522074047277899300, 0.2731766849828906607, 0.7071067811865471286 ) ) ;
#17214=CYLINDRICAL_SURFACE ( 'NONE', #45199, 2.999999999999999556 ) ;
#17215=ORIENTED_EDGE ( 'NONE', *, *, #48367, .T. ) ;
#17219=CARTESIAN_POINT ( 'NONE',  ( -13.73674066540309902, -30.55263188852779876, -46.71145918530379504 ) ) ;
#17221=EDGE_CURVE ( 'NONE', #31048, #7271, #16053, .T. ) ;
#17223=CARTESIAN_POINT ( 'NONE',  ( 11.63393739769619906, -41.61618894467930119, -35.14999999999999858 ) ) ;
#17247=ORIENTED_EDGE ( 'NONE', *, *, #22464, .F. ) ;
#17249=CARTESIAN_POINT ( 'NONE',  ( 2.501736331312110373, -5.785742375864720621, -34.68801049095939959 ) ) ;
#17259=VECTOR ( 'NONE', #41022, 1000.000000000000000 ) ;
#17262=EDGE_LOOP ( 'NONE', ( #14659, #10539, #43700, #47464 ) ) ;
#17266=CYLINDRICAL_SURFACE ( 'NONE', #43277, 3.000000000000005773 ) ;
#17267=CYLINDRICAL_SURFACE ( 'NONE', #33558, 1.999999999999998224 ) ;
#17271=CARTESIAN_POINT ( 'NONE',  ( -22.71231100707319683, -11.80202241275389952, -54.61438712110569327 ) ) ;
#17279=ORIENTED_EDGE ( 'NONE', *, *, #29715, .T. ) ;
#17282=ORIENTED_EDGE ( 'NONE', *, *, #45729, .T. ) ;
#17296=CIRCLE ( 'NONE', #46601, 3.000000000000004885 ) ;
#17297=ORIENTED_EDGE ( 'NONE', *, *, #24022, .T. ) ;
#17307=CARTESIAN_POINT ( 'NONE',  ( 44.49954724606238443, -40.10969356087659321, -63.76892652563923036 ) ) ;
#17313=CARTESIAN_POINT ( 'NONE',  ( 16.13393739769620083, -29.75141864441723882, -34.70142521051216278 ) ) ;
#17330=LINE ( 'NONE', #806, #10121 ) ;
#17332=CARTESIAN_POINT ( 'NONE',  ( 2.528703657258640103, -25.32162763854480048, -34.65800258959620095 ) ) ;
#17340=ORIENTED_EDGE ( 'NONE', *, *, #19027, .F. ) ;
#17352=CARTESIAN_POINT ( 'NONE',  ( 42.30362988516652223, -37.67198729731079254, -78.80153692937045662 ) ) ;
#17360=DIRECTION ( 'NONE',  ( -0.8660254037844381525, -0.5000000000000007772, 0.000000000000000000 ) ) ;
#17367=DIRECTION ( 'NONE',  ( -0.3487035033511760029, -0.9372330909387569520, 0.000000000000000000 ) ) ;
#17377=FACE_OUTER_BOUND ( 'NONE', #46020, .T. ) ;
#17389=DIRECTION ( 'NONE',  ( 0.000000000000000000, 0.000000000000000000, 1.000000000000000000 ) ) ;
#17402=CARTESIAN_POINT ( 'NONE',  ( 17.16548900651931220, 12.66681598883031867, -61.51477253168783221 ) ) ;
#17410=EDGE_LOOP ( 'NONE', ( #51283, #14595, #12486, #43897 ) ) ;
#17411=CARTESIAN_POINT ( 'NONE',  ( -35.14957093606200544, -34.88797072816932143, -65.33131159457242632 ) ) ;
#17418=DIRECTION ( 'NONE',  ( 0.000000000000000000, 0.000000000000000000, -1.000000000000000000 ) ) ;
#17430=CARTESIAN_POINT ( 'NONE',  ( 14.28038400710293487, -41.76263555408612405, -34.79644660940672907 ) ) ;
#17435=DIRECTION ( 'NONE',  ( 8.462868000000000073E-18, -1.066343000000000058E-17, 1.000000000000000000 ) ) ;
#17444=CARTESIAN_POINT ( 'NONE',  ( 0.07473234491190286488, -51.15631565001774561, -35.09349432427395499 ) ) ;
#17449=CARTESIAN_POINT ( 'NONE',  ( 44.64173248798216775, 8.772533778425639639, -63.54959783062244583 ) ) ;
#17451=EDGE_CURVE ( 'NONE', #5164, #39608, #9601, .T. ) ;
#17466=CYLINDRICAL_SURFACE ( 'NONE', #25340, 0.4999999999999993894 ) ;
#17469=LINE ( 'NONE', #41826, #46032 ) ;
#17474=DIRECTION ( 'NONE',  ( 0.04332574401194498603, 0.02501412996813699718, -0.9987478026047158508 ) ) ;
#17476=CARTESIAN_POINT ( 'NONE',  ( 8.644451877215649560, 17.52530927293000218, -35.10565360069929852 ) ) ;
#17481=AXIS2_PLACEMENT_3D ( 'NONE', #7691, #31759, #19725 ) ;
#17490=DIRECTION ( 'NONE',  ( 0.05643417272666773760, -0.04100182651872436024, -0.9975640502598241977 ) ) ;
#17492=DIRECTION ( 'NONE',  ( 0.8660254037844390407, 0.4999999999999995004, 2.775557561562887037E-17 ) ) ;
#17504=LINE ( 'NONE', #21927, #17045 ) ;
#17509=EDGE_CURVE ( 'NONE', #38446, #25427, #14951, .T. ) ;
#17512=ORIENTED_EDGE ( 'NONE', *, *, #30909, .F. ) ;
#17513=EDGE_LOOP ( 'NONE', ( #2186, #623, #27562, #129 ) ) ;
#17516=CARTESIAN_POINT ( 'NONE',  ( 23.63393739769620083, -48.77866774226020397, -34.64999999999999858 ) ) ;
#17523=CARTESIAN_POINT ( 'NONE',  ( -22.55228448404800190, -11.83808067235150041, -54.37716480558419363 ) ) ;
#17530=CARTESIAN_POINT ( 'NONE',  ( 16.13393739769599833, 14.38381105532070059, -49.33749999999999858 ) ) ;
#17533=LINE ( 'NONE', #33502, #41005 ) ;
#17544=EDGE_CURVE ( 'NONE', #25171, #45038, #22411, .T. ) ;
#17546=CARTESIAN_POINT ( 'NONE',  ( 1.058369240368480124, -8.644356418428410294, -34.64999999999999858 ) ) ;
#17555=AXIS2_PLACEMENT_3D ( 'NONE', #41101, #13835, #29792 ) ;
#17560=CARTESIAN_POINT ( 'NONE',  ( 14.13393739769600010, 14.38381105532060111, -62.64999999999999858 ) ) ;
#17561=CARTESIAN_POINT ( 'NONE',  ( 44.86670720216029196, -39.15407246580593892, -66.17957604452888631 ) ) ;
#17565=ORIENTED_EDGE ( 'NONE', *, *, #50302, .T. ) ;
#17568=ORIENTED_EDGE ( 'NONE', *, *, #11914, .T. ) ;
#17572=CARTESIAN_POINT ( 'NONE',  ( 28.63393739769619728, -26.55370255794280254, -34.64999999999999858 ) ) ;
#17589=ORIENTED_EDGE ( 'NONE', *, *, #21396, .F. ) ;
#17593=CARTESIAN_POINT ( 'NONE',  ( 38.67452568954050207, -36.11618894467930119, -81.65000000000000568 ) ) ;
#17599=ORIENTED_EDGE ( 'NONE', *, *, #20863, .F. ) ;
#17609=CARTESIAN_POINT ( 'NONE',  ( 44.33306693287859446, -37.96050983500394693, -68.65435001593694153 ) ) ;
#17611=PLANE ( 'NONE',  #22509 ) ;
#17639=FACE_OUTER_BOUND ( 'NONE', #30265, .T. ) ;
#17656=CARTESIAN_POINT ( 'NONE',  ( 16.13393739769620083, -1.590680505402594314, -34.79644660940672196 ) ) ;
#17663=ORIENTED_EDGE ( 'NONE', *, *, #37973, .F. ) ;
#17664=CARTESIAN_POINT ( 'NONE',  ( 45.57987257403829773, 6.876088038916404521, -62.42029362287482996 ) ) ;
#17670=CARTESIAN_POINT ( 'NONE',  ( -0.007164426707907000161, -50.71887597443840434, -34.77269723932290191 ) ) ;
#17675=ADVANCED_FACE ( 'NONE', ( #45143 ), #49549, .T. ) ;
#17687=CARTESIAN_POINT ( 'NONE',  ( 23.08073416742070094, -9.873403152104399894, -35.14999999999999858 ) ) ;
#17696=( BOUNDED_CURVE ( )  B_SPLINE_CURVE ( 3, ( #18195, #13252, #45727, #5380 ),
 .UNSPECIFIED., .F., .T. ) 
 B_SPLINE_CURVE_WITH_KNOTS ( ( 4, 4 ),
 ( 3.076739999030396445E-15, 0.7853981633974360665 ),
 .UNSPECIFIED. ) 
 CURVE ( )  GEOMETRIC_REPRESENTATION_ITEM ( )  RATIONAL_B_SPLINE_CURVE ( ( 1.000000000000000000, 0.9492530216741930094, 0.9492530216741930094, 1.000000000000000000 ) ) 
 REPRESENTATION_ITEM ( '' )  );
#17704=CARTESIAN_POINT ( 'NONE',  ( 44.94429346996862762, 8.794140527020607223, -62.08337702003966996 ) ) ;
#17713=CARTESIAN_POINT ( 'NONE',  ( -22.84941414684771388, -15.61618224896967355, -54.74986855478772441 ) ) ;
#17724=AXIS2_PLACEMENT_3D ( 'NONE', #34548, #47405, #39270 ) ;
#17733=AXIS2_PLACEMENT_3D ( 'NONE', #7011, #41865, #38982 ) ;
#17744=FACE_OUTER_BOUND ( 'NONE', #38578, .T. ) ;
#17749=EDGE_CURVE ( 'NONE', #40473, #15666, #25654, .T. ) ;
#17751=ORIENTED_EDGE ( 'NONE', *, *, #27834, .F. ) ;
#17760=CARTESIAN_POINT ( 'NONE',  ( -0.007164378094141890356, 19.48649803870589992, -34.77269719633950018 ) ) ;
#17772=AXIS2_PLACEMENT_3D ( 'NONE', #18295, #22735, #34537 ) ;
#17774=CARTESIAN_POINT ( 'NONE',  ( -20.84921622758820092, -28.80579560280489915, -53.14778043205649993 ) ) ;
#17785=FACE_OUTER_BOUND ( 'NONE', #23737, .T. ) ;
#17794=EDGE_CURVE ( 'NONE', #22337, #31736, #48490, .T. ) ;
#17799=ORIENTED_EDGE ( 'NONE', *, *, #38602, .T. ) ;
#17803=TOROIDAL_SURFACE ( 'NONE', #38736, 16.60961179679779676, 0.5000000000000000000 ) ;
#17807=CARTESIAN_POINT ( 'NONE',  ( -5.174310700386709705, 17.42459025154530039, -39.45610452538490165 ) ) ;
#17809=CARTESIAN_POINT ( 'NONE',  ( 46.37359821032702456, -40.25881220143922690, -54.56558613226453502 ) ) ;
#17810=CARTESIAN_POINT ( 'NONE',  ( 21.79705635832106125, 3.269314289273323126, -84.65000000000000568 ) ) ;
#17817=CARTESIAN_POINT ( 'NONE',  ( 41.71914574866418945, 8.547687252698329630, -77.49492017313852443 ) ) ;
#17821=CARTESIAN_POINT ( 'NONE',  ( 29.11414631625610028, -26.73267003105300077, -35.00928286143069812 ) ) ;
#17826=AXIS2_PLACEMENT_3D ( 'NONE', #9437, #25386, #41387 ) ;
#17844=DIRECTION ( 'NONE',  ( 1.000000000000000000, 0.000000000000000000, 0.000000000000000000 ) ) ;
#17851=AXIS2_PLACEMENT_3D ( 'NONE', #33382, #45457, #9308 ) ;
#17857=CARTESIAN_POINT ( 'NONE',  ( 43.41780707837584430, -37.83780770426486839, -73.23058605696958523 ) ) ;
#17858=VERTEX_POINT ( 'NONE', #36677 ) ;
#17864=CIRCLE ( 'NONE', #5350, 0.5000000000000004441 ) ;
#17874=CARTESIAN_POINT ( 'NONE',  ( 46.77956775759329133, -39.16040751821400079, -34.67032516424389854 ) ) ;
#17877=CIRCLE ( 'NONE', #51375, 8.000000000000000000 ) ;
#17878=ORIENTED_EDGE ( 'NONE', *, *, #50624, .F. ) ;
#17880=CIRCLE ( 'NONE', #304, 34.41780050634729804 ) ;
#17914=CARTESIAN_POINT ( 'NONE',  ( 17.25678305769729803, 12.72875286183739973, -62.64999999999999858 ) ) ;
#17916=CARTESIAN_POINT ( 'NONE',  ( 45.41914672974152722, 6.858506551998131862, -63.22389523773885855 ) ) ;
#17933=CARTESIAN_POINT ( 'NONE',  ( 38.67452568954060155, 1.883811055320659955, -81.65000000000000568 ) ) ;
#17943=CARTESIAN_POINT ( 'NONE',  ( 9.916610038437418950, -53.65744759104700279, -34.65028073423250277 ) ) ;
#17953=ORIENTED_EDGE ( 'NONE', *, *, #38571, .F. ) ;
#17955=CARTESIAN_POINT ( 'NONE',  ( 16.13393739769620083, -15.61618894467929941, -35.12503119152809461 ) ) ;
#17958=CARTESIAN_POINT ( 'NONE',  ( 44.53450647839624565, 8.764688726411476338, -64.06879138189025014 ) ) ;
#17960=CARTESIAN_POINT ( 'NONE',  ( -0.007164427059776000244, 14.47565373231149977, -34.77269723891829756 ) ) ;
#17967=CARTESIAN_POINT ( 'NONE',  ( -22.81250826063345727, -17.44330766158130785, -54.72902440807905577 ) ) ;
#17985=AXIS2_PLACEMENT_3D ( 'NONE', #8260, #5377, #396 ) ;
#17998=CARTESIAN_POINT ( 'NONE',  ( 16.72856488856198354, 6.951788894885693182, 4.943674098299959851 ) ) ;
#18003=CIRCLE ( 'NONE', #28057, 33.97624844042361048 ) ;
#18011=FACE_OUTER_BOUND ( 'NONE', #21320, .T. ) ;
#18022=DIRECTION ( 'NONE',  ( 0.000000000000000000, -1.000000000000000000, 0.000000000000000000 ) ) ;
#18024=ORIENTED_EDGE ( 'NONE', *, *, #19714, .F. ) ;
#18029=FACE_OUTER_BOUND ( 'NONE', #36055, .T. ) ;
#18033=CARTESIAN_POINT ( 'NONE',  ( -18.91827871269439854, -32.83363571916979851, -51.21716275619940006 ) ) ;
#18053=ORIENTED_EDGE ( 'NONE', *, *, #16303, .T. ) ;
#18058=CARTESIAN_POINT ( 'NONE',  ( 29.13393739769619728, 1.883811055320659955, -34.64999999999999858 ) ) ;
#18063=CARTESIAN_POINT ( 'NONE',  ( 28.98356459125609774, -4.548084906195380306, -34.79124076679859456 ) ) ;
#18066=CARTESIAN_POINT ( 'NONE',  ( -15.88451588308629603, 7.113652344613260681, -48.88624781813099673 ) ) ;
#18068=CARTESIAN_POINT ( 'NONE',  ( 46.74265266493473092, -40.28841859069392228, -52.72914385014497896 ) ) ;
#18071=ORIENTED_EDGE ( 'NONE', *, *, #35446, .F. ) ;
#18074=CARTESIAN_POINT ( 'NONE',  ( 43.58458626024809490, 8.765430566770698206, -68.35028911638491422 ) ) ;
#18076=CARTESIAN_POINT ( 'NONE',  ( 27.13393739769620083, -38.61618894467930119, -59.64999999999999147 ) ) ;
#18079=CARTESIAN_POINT ( 'NONE',  ( 29.04782745927229826, -26.70812982677800207, -34.86734588637909837 ) ) ;
#18094=CARTESIAN_POINT ( 'NONE',  ( 11.88511791769077064, 10.47075910136237376, -59.64999999999999147 ) ) ;
#18096=EDGE_CURVE ( 'NONE', #12971, #12279, #42887, .T. ) ;
#18097=ORIENTED_EDGE ( 'NONE', *, *, #36029, .F. ) ;
#18101=CARTESIAN_POINT ( 'NONE',  ( 0.3209249304026170480, -15.61618894467929941, -35.14999999999999858 ) ) ;
#18103=FACE_OUTER_BOUND ( 'NONE', #23855, .T. ) ;
#18116=CARTESIAN_POINT ( 'NONE',  ( 44.62762076536061784, -37.99767204670846610, -67.18153134414910710 ) ) ;
#18121=VECTOR ( 'NONE', #40698, 1000.000000000000114 ) ;
#18132=AXIS2_PLACEMENT_3D ( 'NONE', #2474, #1703, #6417 ) ;
#18135=CARTESIAN_POINT ( 'NONE',  ( 46.94631559364366780, -39.21699915129384806, -34.75526898281329835 ) ) ;
#18138=ORIENTED_EDGE ( 'NONE', *, *, #6563, .F. ) ;
#18146=CARTESIAN_POINT ( 'NONE',  ( 38.67452568954060155, -37.56081407618430035, -81.65000000000000568 ) ) ;
#18160=EDGE_CURVE ( 'NONE', #35235, #24503, #41729, .T. ) ;
#18172=DIRECTION ( 'NONE',  ( 0.8204012560548787913, -0.5717882292104107256, 0.000000000000000000 ) ) ;
#18173=CARTESIAN_POINT ( 'NONE',  ( 46.49483455572801915, 6.970689097494132014, -57.84551077717584633 ) ) ;
#18174=VERTEX_POINT ( 'NONE', #7789 ) ;
#18176=VECTOR ( 'NONE', #4639, 1000.000000000000000 ) ;
#18185=LINE ( 'NONE', #45718, #5817 ) ;
#18187=AXIS2_PLACEMENT_3D ( 'NONE', #32115, #44198, #40781 ) ;
#18195=CARTESIAN_POINT ( 'NONE',  ( 28.13393739769619728, -22.54439217495490055, -35.14999999999999858 ) ) ;
#18199=LINE ( 'NONE', #42579, #32321 ) ;
#18207=CARTESIAN_POINT ( 'NONE',  ( 38.67452568954060155, 6.328436186825659782, -81.65000000000000568 ) ) ;
#18220=ADVANCED_FACE ( 'NONE', ( #16671 ), #37114, .T. ) ;
#18221=ORIENTED_EDGE ( 'NONE', *, *, #30064, .F. ) ;
#18223=ORIENTED_EDGE ( 'NONE', *, *, #36959, .T. ) ;
#18224=CARTESIAN_POINT ( 'NONE',  ( -22.69491836354699288, -19.22720705397727059, -54.67294082763422125 ) ) ;
#18227=ORIENTED_EDGE ( 'NONE', *, *, #51871, .F. ) ;
#18232=VERTEX_POINT ( 'NONE', #21112 ) ;
#18233=CARTESIAN_POINT ( 'NONE',  ( 0.3188172270368339611, -46.24795913321420215, -34.65000333199999716 ) ) ;
#18243=CARTESIAN_POINT ( 'NONE',  ( 47.13393657218789912, 8.048130458325550407, -53.76789950451890121 ) ) ;
#18245=ORIENTED_EDGE ( 'NONE', *, *, #33822, .T. ) ;
#18247=ADVANCED_FACE ( 'NONE', ( #28454, #33159 ), #48390, .T. ) ;
#18250=CARTESIAN_POINT ( 'NONE',  ( 45.08270409799413869, -40.03629360808191961, -61.41132920995301703 ) ) ;
#18263=CYLINDRICAL_SURFACE ( 'NONE', #8679, 2.999999999999999112 ) ;
#18275=EDGE_CURVE ( 'NONE', #44695, #3841, #39331, .T. ) ;
#18280=DIRECTION ( 'NONE',  ( -0.5000000000000012212, -0.8660254037844380415, 0.000000000000000000 ) ) ;
#18283=CARTESIAN_POINT ( 'NONE',  ( -22.72850738805879800, -13.72396512373410005, -54.52996344323300093 ) ) ;
#18294=VECTOR ( 'NONE', #26548, 1000.000000000000000 ) ;
#18295=CARTESIAN_POINT ( 'NONE',  ( 16.13393739769620083, -29.47259540523039689, -47.64999999999999858 ) ) ;
#18296=VECTOR ( 'NONE', #32239, 1000.000000000000000 ) ;
#18303=( BOUNDED_CURVE ( )  B_SPLINE_CURVE ( 3, ( #50604, #26733, #42491, #25953 ),
 .UNSPECIFIED., .F., .T. ) 
 B_SPLINE_CURVE_WITH_KNOTS ( ( 4, 4 ),
 ( 1.558720328957954759, 1.570796326794896558 ),
 .UNSPECIFIED. ) 
 CURVE ( )  GEOMETRIC_REPRESENTATION_ITEM ( )  RATIONAL_B_SPLINE_CURVE ( ( 1.000000000000000000, 0.9999878475599406347, 0.9999878475599406347, 1.000000000000000000 ) ) 
 REPRESENTATION_ITEM ( '' )  );
#18314=CARTESIAN_POINT ( 'NONE',  ( 16.13393739769620083, -38.61618894467930119, -59.64999999999999147 ) ) ;
#18316=CARTESIAN_POINT ( 'NONE',  ( 0.2534322734540089828, 19.67561520348110093, -34.54509924001159504 ) ) ;
#18318=CARTESIAN_POINT ( 'NONE',  ( 43.00218716632829796, -37.73344212960819988, -75.30702696467470503 ) ) ;
#18331=AXIS2_PLACEMENT_3D ( 'NONE', #16232, #32188, #16749 ) ;
#18349=EDGE_LOOP ( 'NONE', ( #19131, #315, #25592, #31935 ) ) ;
#18352=LINE ( 'NONE', #38029, #51824 ) ;
#18362=CARTESIAN_POINT ( 'NONE',  ( 44.36550484164386177, -37.96472317729350721, -68.49216281759998992 ) ) ;
#18365=AXIS2_PLACEMENT_3D ( 'NONE', #30150, #46170, #14695 ) ;
#18386=CARTESIAN_POINT ( 'NONE',  ( 46.89857864678852195, -39.20081467324785507, -34.72191413131642435 ) ) ;
#18395=CARTESIAN_POINT ( 'NONE',  ( 20.53650276133967267, 10.53025766472739555, -34.79644660940672907 ) ) ;
#18404=EDGE_CURVE ( 'NONE', #4073, #2764, #33626, .T. ) ;
#18416=ORIENTED_EDGE ( 'NONE', *, *, #47019, .T. ) ;
#18420=ORIENTED_EDGE ( 'NONE', *, *, #29343, .T. ) ;
#18428=CARTESIAN_POINT ( 'NONE',  ( 46.71043997899148081, 6.991105343399341088, -56.76743462289293518 ) ) ;
#18440=CARTESIAN_POINT ( 'NONE',  ( -0.03447620312153085176, -4.141051901845263394, -34.79644660940673617 ) ) ;
#18443=VECTOR ( 'NONE', #13726, 999.9999999999998863 ) ;
#18445=CIRCLE ( 'NONE', #14301, 38.49999999999998579 ) ;
#18448=AXIS2_PLACEMENT_3D ( 'NONE', #50666, #10837, #30730 ) ;
#18461=DIRECTION ( 'NONE',  ( 0.5813178231270340612, 0.8136765871738268485, 0.000000000000000000 ) ) ;
#18469=EDGE_CURVE ( 'NONE', #29987, #34524, #34163, .T. ) ;
#18470=ORIENTED_EDGE ( 'NONE', *, *, #24738, .F. ) ;
#18474=DIRECTION ( 'NONE',  ( 0.000000000000000000, 0.000000000000000000, -1.000000000000000000 ) ) ;
#18480=CARTESIAN_POINT ( 'NONE',  ( 10.09871813756559966, -54.07211264381389526, -34.88336916441289759 ) ) ;
#18486=DIRECTION ( 'NONE',  ( 0.4743737082415240836, -0.8803235683140521184, 0.000000000000000000 ) ) ;
#18487=VECTOR ( 'NONE', #31713, 1000.000000000000000 ) ;
#18489=CONICAL_SURFACE ( 'NONE', #15989, 3.567506086244481622, 0.04995839572194331335 ) ;
#18491=VERTEX_POINT ( 'NONE', #50918 ) ;
#18512=ORIENTED_EDGE ( 'NONE', *, *, #37668, .T. ) ;
#18516=CARTESIAN_POINT ( 'NONE',  ( 44.35599058648487159, -39.98315081151604744, -64.93502037408133276 ) ) ;
#18536=CARTESIAN_POINT ( 'NONE',  ( 19.13393739769620083, -49.61618894467939356, -35.14999999999999858 ) ) ;
#18537=ORIENTED_EDGE ( 'NONE', *, *, #8832, .F. ) ;
#18538=DIRECTION ( 'NONE',  ( -0.3863301728269175062, -0.9223605572462019175, 3.330669073875470114E-16 ) ) ;
#18539=VERTEX_POINT ( 'NONE', #40663 ) ;
#18561=FACE_OUTER_BOUND ( 'NONE', #20815, .T. ) ;
#18569=DIRECTION ( 'NONE',  ( 0.000000000000000000, 0.000000000000000000, -1.000000000000000000 ) ) ;
#18571=DIRECTION ( 'NONE',  ( -0.04100182651872445044, -0.05643417272666771678, -0.9975640502598241977 ) ) ;
#18572=ADVANCED_FACE ( 'NONE', ( #20732 ), #49063, .T. ) ;
#18579=DIRECTION ( 'NONE',  ( 1.000000000000000000, 0.000000000000000000, 0.000000000000000000 ) ) ;
#18582=CARTESIAN_POINT ( 'NONE',  ( 44.13393739769620083, -36.11618894467930119, -35.14999999999999858 ) ) ;
#18583=CARTESIAN_POINT ( 'NONE',  ( 46.38156616808179677, -40.25946647325027783, -54.52593885421595132 ) ) ;
#18592=CARTESIAN_POINT ( 'NONE',  ( 45.46242224712364077, 8.938650005438001145, -59.13099268088515714 ) ) ;
#18597=CARTESIAN_POINT ( 'NONE',  ( 28.88047141014000019, -26.64595108362729903, -34.71367995918279092 ) ) ;
#18601=ORIENTED_EDGE ( 'NONE', *, *, #28201, .F. ) ;
#18614=EDGE_CURVE ( 'NONE', #32183, #25882, #45118, .T. ) ;
#18617=CARTESIAN_POINT ( 'NONE',  ( 0.3209249304026170480, -8.218592747557250888, -34.64999999999999858 ) ) ;
#18621=EDGE_LOOP ( 'NONE', ( #37891, #41878, #12482, #12264, #40099 ) ) ;
#18628=CARTESIAN_POINT ( 'NONE',  ( 45.23524973664237336, -38.07011267116087794, -64.14340693299787688 ) ) ;
#18631=CARTESIAN_POINT ( 'NONE',  ( -22.82535044970985538, -14.17006684274750583, -54.73606930856294639 ) ) ;
#18636=EDGE_CURVE ( 'NONE', #36069, #25155, #44334, .T. ) ;
#18638=EDGE_CURVE ( 'NONE', #43625, #13682, #40922, .T. ) ;
#18640=LINE ( 'NONE', #14714, #51611 ) ;
#18644=ORIENTED_EDGE ( 'NONE', *, *, #18636, .T. ) ;
#18649=CARTESIAN_POINT ( 'NONE',  ( 41.42428665458552928, -39.70010360968180407, -79.11029697435235164 ) ) ;
#18650=CARTESIAN_POINT ( 'NONE',  ( 20.53650276133967267, 10.53025766472739555, -34.79644660940672907 ) ) ;
#18659=DIRECTION ( 'NONE',  ( 0.000000000000000000, 0.000000000000000000, -1.000000000000000000 ) ) ;
#18665=VECTOR ( 'NONE', #48568, 1000.000000000000000 ) ;
#18677=CARTESIAN_POINT ( 'NONE',  ( 10.47081843707153581, -34.50169217863195570, -84.65000000000000568 ) ) ;
#18687=CARTESIAN_POINT ( 'NONE',  ( 44.42648819202516108, 6.740347691462509339, -68.18724196164413343 ) ) ;
#18689=ORIENTED_EDGE ( 'NONE', *, *, #45476, .F. ) ;
#18694=DIRECTION ( 'NONE',  ( 1.000000000000000000, 0.000000000000000000, 0.000000000000000000 ) ) ;
#18719=DIRECTION ( 'NONE',  ( -0.6522074047277899300, 0.2731766849828906607, 0.7071067811865471286 ) ) ;
#18727=VERTEX_POINT ( 'NONE', #41436 ) ;
#18732=DIRECTION ( 'NONE',  ( 0.000000000000000000, -1.000000000000000000, 0.000000000000000000 ) ) ;
#18737=ORIENTED_EDGE ( 'NONE', *, *, #23177, .F. ) ;
#18740=DIRECTION ( 'NONE',  ( 0.000000000000000000, 0.000000000000000000, -1.000000000000000000 ) ) ;
#18741=CARTESIAN_POINT ( 'NONE',  ( -22.40543978572512174, -21.82123808744384164, -54.48262838077054226 ) ) ;
#18744=EDGE_LOOP ( 'NONE', ( #34485, #44924, #40141, #36865, #28775, #25893 ) ) ;
#18748=CARTESIAN_POINT ( 'NONE',  ( -10.98165337464593350, -35.31681881277557977, -44.31573110638452562 ) ) ;
#18750=ORIENTED_EDGE ( 'NONE', *, *, #40612, .T. ) ;
#18755=AXIS2_PLACEMENT_3D ( 'NONE', #42936, #7035, #27187 ) ;
#18756=EDGE_CURVE ( 'NONE', #17858, #46747, #23333, .T. ) ;
#18758=CARTESIAN_POINT ( 'NONE',  ( 0.3209249304026240424, 19.48649808507980197, -34.64999999999999858 ) ) ;
#18760=( BOUNDED_CURVE ( )  B_SPLINE_CURVE ( 3, ( #36523, #7740, #15847, #40212 ),
 .UNSPECIFIED., .F., .T. ) 
 B_SPLINE_CURVE_WITH_KNOTS ( ( 4, 4 ),
 ( 3.701430267445704914, 3.744786642406928934 ),
 .UNSPECIFIED. ) 
 CURVE ( )  GEOMETRIC_REPRESENTATION_ITEM ( )  RATIONAL_B_SPLINE_CURVE ( ( 1.000000000000000000, 0.9998433581970664896, 0.9998433581970664896, 1.000000000000000000 ) ) 
 REPRESENTATION_ITEM ( '' )  );
#18762=CARTESIAN_POINT ( 'NONE',  ( 10.13393739769589885, 22.91950879131600161, -35.14999999999999858 ) ) ;
#18771=CARTESIAN_POINT ( 'NONE',  ( 44.72493418209450056, -40.01092346187889603, -63.14659530062845505 ) ) ;
#18777=CARTESIAN_POINT ( 'NONE',  ( 23.14288469598330167, 17.63186702652449966, -35.14566363178219888 ) ) ;
#18781=EDGE_LOOP ( 'NONE', ( #28974, #30819, #36256, #15996 ) ) ;
#18786=DIRECTION ( 'NONE',  ( 0.000000000000000000, -1.000000000000000000, 0.000000000000000000 ) ) ;
#18787=CARTESIAN_POINT ( 'NONE',  ( 40.80516388273994721, 8.393954547589055792, -82.09339948163508893 ) ) ;
#18794=EDGE_LOOP ( 'NONE', ( #787, #33061, #30475, #10949 ) ) ;
#18798=FACE_OUTER_BOUND ( 'NONE', #34594, .T. ) ;
#18801=ORIENTED_EDGE ( 'NONE', *, *, #3732, .T. ) ;
#18805=AXIS2_PLACEMENT_3D ( 'NONE', #22369, #9566, #9825 ) ;
#18806=CARTESIAN_POINT ( 'NONE',  ( 22.13393739769589885, 22.91950879131610108, -54.64999999999999858 ) ) ;
#18813=ORIENTED_EDGE ( 'NONE', *, *, #17544, .T. ) ;
#18823=DIRECTION ( 'NONE',  ( 0.4743737082415271922, 0.8803235683140504531, 0.000000000000000000 ) ) ;
#18829=LINE ( 'NONE', #10471, #21236 ) ;
#18835=CARTESIAN_POINT ( 'NONE',  ( -0.1226425999238490022, 19.83525116875770067, -35.35669575663299469 ) ) ;
#18837=CARTESIAN_POINT ( 'NONE',  ( 47.12472940097700302, -38.11604021042080603, -54.67813498204329647 ) ) ;
#18846=CARTESIAN_POINT ( 'NONE',  ( 46.60861704013112217, 9.031941543785155346, -53.45405854682181968 ) ) ;
#18854=EDGE_LOOP ( 'NONE', ( #16216, #36740, #40775, #51868, #14765, #1320 ) ) ;
#18873=CARTESIAN_POINT ( 'NONE',  ( 23.60377752213949876, -48.79579064807929711, -34.96018206680719942 ) ) ;
#18883=LINE ( 'NONE', #50356, #10466 ) ;
#18888=DIRECTION ( 'NONE',  ( 0.000000000000000000, 0.000000000000000000, -1.000000000000000000 ) ) ;
#18899=EDGE_CURVE ( 'NONE', #46602, #23939, #36326, .T. ) ;
#18902=CARTESIAN_POINT ( 'NONE',  ( 44.13393739769620083, -36.11618894467930119, -35.14999999999999858 ) ) ;
#18906=ORIENTED_EDGE ( 'NONE', *, *, #44650, .F. ) ;
#18916=CARTESIAN_POINT ( 'NONE',  ( 0.1457840807894888180, 19.59951024407514097, -34.68167773519660813 ) ) ;
#18919=CARTESIAN_POINT ( 'NONE',  ( 12.93740664656254680, 18.01819160635294992, -34.64999999999999858 ) ) ;
#18944=CARTESIAN_POINT ( 'NONE',  ( 43.26664544300862048, 6.584138943362735752, -73.98639579103669917 ) ) ;
#18950=DIRECTION ( 'NONE',  ( 0.000000000000000000, 0.000000000000000000, -1.000000000000000000 ) ) ;
#18958=AXIS2_PLACEMENT_3D ( 'NONE', #24418, #19484, #35477 ) ;
#18977=CARTESIAN_POINT ( 'NONE',  ( 30.13393739769619728, -38.61618894467930119, -72.14999999999999147 ) ) ;
#18978=DIRECTION ( 'NONE',  ( 0.000000000000000000, -1.000000000000000000, 0.000000000000000000 ) ) ;
#18979=B_SPLINE_CURVE_WITH_KNOTS ( 'NONE', 3,
 ( #40880, #13632, #21468, #29590, #32998, #33263, #9691, #25651, #41656, #5759, #21721, #20952, #37729, #1051, #32460, #48489, #12593, #28554, #44556, #21206, #36948, #9182, #12860, #29338, #8654 ),
 .UNSPECIFIED., .F., .F.,
 ( 4, 2, 2, 1, 1, 2, 2, 2, 2, 1, 1, 1, 2, 2, 4 ),
 ( 0.000000000000000000, 0.1250000000000096312, 0.1875000000000144329, 0.2187500000000176803, 0.2343750000000193179, 0.2421875000000198452, 0.2500000000000204281, 0.5000000000000174305, 0.6250000000000159872, 0.6875000000000153211, 0.7187500000000150990, 0.7343750000000154321, 0.7421875000000155431, 0.7500000000000156541, 1.000000000000000000 ),
 .UNSPECIFIED. ) ;
#18988=CARTESIAN_POINT ( 'NONE',  ( 45.35172597471413525, 8.821878553838054415, -60.10595750932078118 ) ) ;
#18989=CARTESIAN_POINT ( 'NONE',  ( 19.16157989668684891, 18.33238584480854527, -34.89146800830132378 ) ) ;
#18993=VERTEX_POINT ( 'NONE', #41055 ) ;
#18994=ORIENTED_EDGE ( 'NONE', *, *, #12133, .F. ) ;
#18996=ADVANCED_FACE ( 'NONE', ( #29241 ), #17803, .T. ) ;
#19000=DIRECTION ( 'NONE',  ( -0.9304380493636940086, -0.3664492274467011645, 0.000000000000000000 ) ) ;
#19001=CARTESIAN_POINT ( 'NONE',  ( -13.34911547993528025, -41.36128161159584238, -46.70844658446259956 ) ) ;
#19006=DIRECTION ( 'NONE',  ( 0.000000000000000000, 0.000000000000000000, 1.000000000000000000 ) ) ;
#19008=CARTESIAN_POINT ( 'NONE',  ( 45.15332781221579239, -33.30556177572260168, -35.04110570142709946 ) ) ;
#19010=CARTESIAN_POINT ( 'NONE',  ( 41.61626771661330082, 4.883811055320659733, -82.23834840541459812 ) ) ;
#19018=CARTESIAN_POINT ( 'NONE',  ( 1.055648624549950121, -22.58715886189619937, -34.65000333055159842 ) ) ;
#19026=CARTESIAN_POINT ( 'NONE',  ( 45.49125530861236655, -40.06305810151475555, -59.42936724080989563 ) ) ;
#19027=EDGE_CURVE ( 'NONE', #46513, #18727, #24506, .T. ) ;
#19029=ADVANCED_FACE ( 'NONE', ( #37125 ), #17466, .T. ) ;
#19032=EDGE_CURVE ( 'NONE', #19145, #16544, #11746, .T. ) ;
#19033=CARTESIAN_POINT ( 'NONE',  ( -2.751565836256447906, -9.953069984054630837, -84.65000000000000568 ) ) ;
#19035=DIRECTION ( 'NONE',  ( -0.2201791028874051093, -0.9741803703649114521, 0.04993764759559501942 ) ) ;
#19045=EDGE_CURVE ( 'NONE', #23591, #50655, #37933, .T. ) ;
#19052=CARTESIAN_POINT ( 'NONE',  ( 0.09524056481075650338, 19.92956581399739946, -35.08026080309999628 ) ) ;
#19056=EDGE_LOOP ( 'NONE', ( #20184, #18537, #294, #33667 ) ) ;
#19057=DIRECTION ( 'NONE',  ( -1.000000000000000000, 0.000000000000000000, 0.000000000000000000 ) ) ;
#19059=CARTESIAN_POINT ( 'NONE',  ( 18.11497263573659922, 5.664030231104960400, -35.14999999999999858 ) ) ;
#19066=DIRECTION ( 'NONE',  ( -1.000000000000000000, 0.000000000000000000, 0.000000000000000000 ) ) ;
#19081=DIRECTION ( 'NONE',  ( -0.5516667872527333261, 0.8340645993220474619, 0.000000000000000000 ) ) ;
#19085=CARTESIAN_POINT ( 'NONE',  ( 46.89353120241150208, -39.59222692223529805, -54.28157613336880161 ) ) ;
#19092=EDGE_CURVE ( 'NONE', #24575, #46028, #597, .T. ) ;
#19093=CARTESIAN_POINT ( 'NONE',  ( 8.731180243531696306, -48.92556967366426335, -34.79644561402096770 ) ) ;
#19104=B_SPLINE_CURVE_WITH_KNOTS ( 'NONE', 3,
 ( #32711, #3946, #36398, #8129, #44537, #16240, #35899, #13 ),
 .UNSPECIFIED., .F., .F.,
 ( 4, 2, 2, 4 ),
 ( -0.1350635247397186933, -0.1243669311588919968, -0.1075965482636490056, -0.1052074838081890062 ),
 .UNSPECIFIED. ) ;
#19106=CARTESIAN_POINT ( 'NONE',  ( 42.77403168035458236, 6.335355339735892599, -76.42259866880976915 ) ) ;
#19113=DIRECTION ( 'NONE',  ( 0.000000000000000000, -1.000000000000000000, 0.000000000000000000 ) ) ;
#19114=ORIENTED_EDGE ( 'NONE', *, *, #36735, .T. ) ;
#19127=VERTEX_POINT ( 'NONE', #39672 ) ;
#19131=ORIENTED_EDGE ( 'NONE', *, *, #35243, .F. ) ;
#19135=ORIENTED_EDGE ( 'NONE', *, *, #47691, .F. ) ;
#19139=CARTESIAN_POINT ( 'NONE',  ( 17.63604474694280100, -32.15985502643049898, -34.65000333055159842 ) ) ;
#19140=EDGE_CURVE ( 'NONE', #9837, #18174, #8645, .T. ) ;
#19145=VERTEX_POINT ( 'NONE', #4796 ) ;
#19149=B_SPLINE_CURVE_WITH_KNOTS ( 'NONE', 3,
 ( #16636, #28679, #44681, #40750, #20816, #916, #32857, #38119 ),
 .UNSPECIFIED., .F., .F.,
 ( 4, 2, 2, 4 ),
 ( 0.05028014561772611163, 0.06097673919850660207, 0.07774712209370319982, 0.08013618654915889705 ),
 .UNSPECIFIED. ) ;
#19153=CARTESIAN_POINT ( 'NONE',  ( 17.63393739769639978, 10.88381105532070059, -34.64999999999999858 ) ) ;
#19154=LINE ( 'NONE', #43533, #45165 ) ;
#19155=CARTESIAN_POINT ( 'NONE',  ( 9.894687805641289913, 22.37488585622680048, -34.64999999999999858 ) ) ;
#19168=VERTEX_POINT ( 'NONE', #13201 ) ;
#19193=ORIENTED_EDGE ( 'NONE', *, *, #40577, .F. ) ;
#19197=ORIENTED_EDGE ( 'NONE', *, *, #36735, .F. ) ;
#19200=CARTESIAN_POINT ( 'NONE',  ( 45.07403613745758264, 6.819010629880603247, -64.94950603516362264 ) ) ;
#19203=ORIENTED_EDGE ( 'NONE', *, *, #15221, .F. ) ;
#19205=EDGE_CURVE ( 'NONE', #36007, #51641, #28606, .T. ) ;
#19220=EDGE_CURVE ( 'NONE', #30264, #23002, #21350, .T. ) ;
#19226=LINE ( 'NONE', #48051, #5586 ) ;
#19236=DIRECTION ( 'NONE',  ( -1.000000000000000000, 0.000000000000000000, 0.000000000000000000 ) ) ;
#19237=FACE_OUTER_BOUND ( 'NONE', #48849, .T. ) ;
#19250=CARTESIAN_POINT ( 'NONE',  ( 46.47536507427530239, 8.886826513564159313, -54.64999999999999858 ) ) ;
#19256=ORIENTED_EDGE ( 'NONE', *, *, #33822, .F. ) ;
#19257=CARTESIAN_POINT ( 'NONE',  ( 38.67452568954060155, -37.56081407618430035, -81.65000000000000568 ) ) ;
#19260=ORIENTED_EDGE ( 'NONE', *, *, #10787, .F. ) ;
#19266=FACE_OUTER_BOUND ( 'NONE', #34793, .T. ) ;
#19268=AXIS2_PLACEMENT_3D ( 'NONE', #50595, #26723, #34850 ) ;
#19272=AXIS2_PLACEMENT_3D ( 'NONE', #3019, #34711, #46543 ) ;
#19281=ADVANCED_FACE ( 'NONE', ( #8997 ), #21154, .T. ) ;
#19286=VERTEX_POINT ( 'NONE', #41471 ) ;
#19290=CARTESIAN_POINT ( 'NONE',  ( 45.78260039019426131, -40.08104085361300406, -58.01479249339848110 ) ) ;
#19292=CARTESIAN_POINT ( 'NONE',  ( 22.23620501646692915, 22.68747772516199035, -34.73809820100316870 ) ) ;
#19302=EDGE_LOOP ( 'NONE', ( #1141, #51802, #11779, #43389 ) ) ;
#19303=DIRECTION ( 'NONE',  ( -1.000000000000000000, 0.000000000000000000, 0.000000000000000000 ) ) ;
#19307=CARTESIAN_POINT ( 'NONE',  ( -13.39236625349549925, -0.8785706602474749882, -54.64999999999999858 ) ) ;
#19311=CARTESIAN_POINT ( 'NONE',  ( -0.2277270843104434728, -10.73582424797172585, -34.96449406573682239 ) ) ;
#19317=VERTEX_POINT ( 'NONE', #8732 ) ;
#19320=LINE ( 'NONE', #51298, #3092 ) ;
#19323=ORIENTED_EDGE ( 'NONE', *, *, #49237, .F. ) ;
#19333=EDGE_LOOP ( 'NONE', ( #44933, #14805, #36020, #46548 ) ) ;
#19346=CARTESIAN_POINT ( 'NONE',  ( 46.66336238603499709, -39.88456775088300077, -54.57128118813670170 ) ) ;
#19347=AXIS2_PLACEMENT_3D ( 'NONE', #15139, #2833, #30837 ) ;
#19357=CARTESIAN_POINT ( 'NONE',  ( 29.46622902366960162, -33.11618894467940066, -54.64999999999999858 ) ) ;
#19359=CARTESIAN_POINT ( 'NONE',  ( 45.74957564526550158, -38.01398953213499965, -61.56096017950429911 ) ) ;
#19363=ORIENTED_EDGE ( 'NONE', *, *, #7026, .T. ) ;
#19365=ORIENTED_EDGE ( 'NONE', *, *, #38268, .T. ) ;
#19366=CARTESIAN_POINT ( 'NONE',  ( 42.54139083816280476, 6.317655820708358405, -77.59090943095287685 ) ) ;
#19381=VECTOR ( 'NONE', #28701, 1000.000000000000000 ) ;
#19382=( BOUNDED_CURVE ( )  B_SPLINE_CURVE ( 3, ( #24527, #40544, #4634, #12779 ),
 .UNSPECIFIED., .F., .F. ) 
 B_SPLINE_CURVE_WITH_KNOTS ( ( 4, 4 ),
 ( 4.302261639843196761, 5.087659803240767609 ),
 .UNSPECIFIED. ) 
 CURVE ( )  GEOMETRIC_REPRESENTATION_ITEM ( )  RATIONAL_B_SPLINE_CURVE ( ( 1.000000000000000000, 0.9492530216741755789, 0.9492530216741755789, 1.000000000000000000 ) ) 
 REPRESENTATION_ITEM ( '' )  );
#19385=CARTESIAN_POINT ( 'NONE',  ( 12.98614995704637032, -49.83962866466749375, -82.44267625234935792 ) ) ;
#19386=AXIS2_PLACEMENT_3D ( 'NONE', #29337, #36165, #32211 ) ;
#19387=ORIENTED_EDGE ( 'NONE', *, *, #29983, .F. ) ;
#19395=DIRECTION ( 'NONE',  ( 0.000000000000000000, 0.000000000000000000, 1.000000000000000000 ) ) ;
#19406=CARTESIAN_POINT ( 'NONE',  ( 46.32873999300467460, -38.18646364691427664, -58.67597187213492305 ) ) ;
#19409=EDGE_LOOP ( 'NONE', ( #26078, #15607 ) ) ;
#19410=LINE ( 'NONE', #51133, #32554 ) ;
#19417=CARTESIAN_POINT ( 'NONE',  ( 23.13393739769620083, -2.337132753317950229, -62.14999999999999858 ) ) ;
#19419=AXIS2_PLACEMENT_3D ( 'NONE', #48384, #24499, #40517 ) ;
#19438=DIRECTION ( 'NONE',  ( -0.8090169943749478954, -0.5877852522924724710, 0.000000000000000000 ) ) ;
#19440=LINE ( 'NONE', #27043, #14559 ) ;
#19449=CYLINDRICAL_SURFACE ( 'NONE', #9258, 3.000000000000003997 ) ;
#19459=CARTESIAN_POINT ( 'NONE',  ( 8.731180243531696306, -48.92556967366426335, -34.79644561402096770 ) ) ;
#19460=CARTESIAN_POINT ( 'NONE',  ( 42.68436296462748203, 6.498366103123425219, -76.89780545169345771 ) ) ;
#19473=DIRECTION ( 'NONE',  ( -0.5516667872527448724, 0.8340645993220398013, 0.000000000000000000 ) ) ;
#19477=DIRECTION ( 'NONE',  ( -1.000000000000000000, 0.000000000000000000, 0.000000000000000000 ) ) ;
#19484=DIRECTION ( 'NONE',  ( 0.000000000000000000, 0.000000000000000000, 1.000000000000000000 ) ) ;
#19486=CARTESIAN_POINT ( 'NONE',  ( 14.19338055721690139, 1.323206481297250159, -34.90839531524139971 ) ) ;
#19490=CARTESIAN_POINT ( 'NONE',  ( 30.13393739769619728, 7.383811055320659733, -84.65000000000000568 ) ) ;
#19507=DIRECTION ( 'NONE',  ( 0.000000000000000000, 0.000000000000000000, 1.000000000000000000 ) ) ;
#19515=VECTOR ( 'NONE', #267, 1000.000000000000227 ) ;
#19526=CARTESIAN_POINT ( 'NONE',  ( 45.25735649856909504, -33.62123980734720163, -34.70630702260449851 ) ) ;
#19528=EDGE_LOOP ( 'NONE', ( #38177, #16169, #44196, #25172 ) ) ;
#19533=FACE_OUTER_BOUND ( 'NONE', #24226, .T. ) ;
#19534=CARTESIAN_POINT ( 'NONE',  ( 18.13393739769639978, 10.38381105532070059, -35.14999999999999858 ) ) ;
#19539=ORIENTED_EDGE ( 'NONE', *, *, #30916, .F. ) ;
#19544=CARTESIAN_POINT ( 'NONE',  ( 42.57739974420819351, -39.82473145808468473, -73.54253346003443426 ) ) ;
#19552=CARTESIAN_POINT ( 'NONE',  ( 13.13393739769619906, -49.61618894467939356, -35.14999999999999858 ) ) ;
#19557=AXIS2_PLACEMENT_3D ( 'NONE', #16935, #49175, #20837 ) ;
#19565=DIRECTION ( 'NONE',  ( 1.000000000000000000, 0.000000000000000000, 0.000000000000000000 ) ) ;
#19571=CARTESIAN_POINT ( 'NONE',  ( 15.29511290902269849, 12.56821928479459949, -59.64999999999999147 ) ) ;
#19581=CARTESIAN_POINT ( 'NONE',  ( -19.56713115153528904, 0.1666088194093528763, -52.04600499236246947 ) ) ;
#19590=DIRECTION ( 'NONE',  ( 0.000000000000000000, 0.000000000000000000, -1.000000000000000000 ) ) ;
#19591=DIRECTION ( 'NONE',  ( 0.000000000000000000, -1.000000000000000000, 0.000000000000000000 ) ) ;
#19593=DIRECTION ( 'NONE',  ( 0.5112408204145791890, -0.8594375041513071523, 0.000000000000000000 ) ) ;
#19599=CARTESIAN_POINT ( 'NONE',  ( -0.03447620312153643757, -27.09132598751343579, -34.79644660940672907 ) ) ;
#19600=CARTESIAN_POINT ( 'NONE',  ( 8.897806153503289295, 18.01372606128879639, -34.65445009297679491 ) ) ;
#19614=CARTESIAN_POINT ( 'NONE',  ( 8.943569970476479725, 18.10127401595480023, -34.64999999999999858 ) ) ;
#19616=CARTESIAN_POINT ( 'NONE',  ( 43.91162071577659987, -37.84375841978030053, -70.75826489186619028 ) ) ;
#19617=ADVANCED_FACE ( 'NONE', ( #14922 ), #51833, .T. ) ;
#19618=CYLINDRICAL_SURFACE ( 'NONE', #14188, 3.000000000000005773 ) ;
#19623=ORIENTED_EDGE ( 'NONE', *, *, #12966, .T. ) ;
#19624=CARTESIAN_POINT ( 'NONE',  ( 44.22423880582511657, 7.784288628886946171, -69.62787953467274349 ) ) ;
#19626=CARTESIAN_POINT ( 'NONE',  ( 16.13393739769620083, -45.61618894467940066, -59.64999999999999147 ) ) ;
#19649=CARTESIAN_POINT ( 'NONE',  ( 23.62342291817649809, -48.75768716228870403, -35.10565360069929852 ) ) ;
#19651=DIRECTION ( 'NONE',  ( 0.000000000000000000, 0.000000000000000000, -1.000000000000000000 ) ) ;
#19655=DIRECTION ( 'NONE',  ( 0.000000000000000000, 0.000000000000000000, -1.000000000000000000 ) ) ;
#19662=EDGE_LOOP ( 'NONE', ( #40608, #32910, #7348, #24645 ) ) ;
#19675=FACE_OUTER_BOUND ( 'NONE', #49896, .T. ) ;
#19679=CARTESIAN_POINT ( 'NONE',  ( 22.37268434111610205, 22.37603658786960281, -34.64999999999999858 ) ) ;
#19681=EDGE_CURVE ( 'NONE', #27937, #7583, #4203, .T. ) ;
#19683=( BOUNDED_CURVE ( )  B_SPLINE_CURVE ( 2, ( #23623, #23877, #31739 ),
 .UNSPECIFIED., .F., .T. ) 
 B_SPLINE_CURVE_WITH_KNOTS ( ( 3, 3 ),
 ( 2.734699209162410050, 5.217679283405229462 ),
 .UNSPECIFIED. ) 
 CURVE ( )  GEOMETRIC_REPRESENTATION_ITEM ( )  RATIONAL_B_SPLINE_CURVE ( ( 1.032581180562790024, 1.032237589135679867, 1.004410800606350129 ) ) 
 REPRESENTATION_ITEM ( '' )  );
#19688=LINE ( 'NONE', #536, #18487 ) ;
#19694=CARTESIAN_POINT ( 'NONE',  ( 0.2019507440921959052, -4.548421796940673723, -34.66067286864801389 ) ) ;
#19700=CARTESIAN_POINT ( 'NONE',  ( 28.63393739769619728, -4.678675331415849570, -34.64999999999999858 ) ) ;
#19709=ORIENTED_EDGE ( 'NONE', *, *, #39039, .T. ) ;
#19713=ORIENTED_EDGE ( 'NONE', *, *, #13849, .F. ) ;
#19714=EDGE_CURVE ( 'NONE', #4357, #47961, #16999, .T. ) ;
#19719=CARTESIAN_POINT ( 'NONE',  ( 45.08397438503814669, 6.820184756207779309, -64.89981427032263639 ) ) ;
#19725=DIRECTION ( 'NONE',  ( -1.000000000000000000, 0.000000000000000000, 0.000000000000000000 ) ) ;
#19742=ORIENTED_EDGE ( 'NONE', *, *, #9163, .T. ) ;
#19746=CARTESIAN_POINT ( 'NONE',  ( 14.64034768018736798, 18.38379310215821505, -83.19069868277145474 ) ) ;
#19760=FACE_OUTER_BOUND ( 'NONE', #34366, .T. ) ;
#19767=VECTOR ( 'NONE', #21408, 999.9999999999998863 ) ;
#19772=AXIS2_PLACEMENT_3D ( 'NONE', #50188, #6946, #18719 ) ;
#19773=EDGE_LOOP ( 'NONE', ( #4048, #20695, #39391, #44326 ) ) ;
#19774=ORIENTED_EDGE ( 'NONE', *, *, #36951, .F. ) ;
#19776=CARTESIAN_POINT ( 'NONE',  ( 8.643872352928719138, 17.52418497763089889, -35.12503119152809461 ) ) ;
#19785=DIRECTION ( 'NONE',  ( 0.1960104533864304444, -0.03282462862514614471, 0.9800522669321607427 ) ) ;
#19791=DIRECTION ( 'NONE',  ( 1.000000000000000000, 0.000000000000000000, 0.000000000000000000 ) ) ;
#19794=DIRECTION ( 'NONE',  ( 0.000000000000000000, -1.000000000000000000, 0.000000000000000000 ) ) ;
#19803=CARTESIAN_POINT ( 'NONE',  ( 43.76496993594255969, -39.93523117063323014, -67.79702779702520843 ) ) ;
#19807=ADVANCED_FACE ( 'NONE', ( #50511 ), #26118, .T. ) ;
#19808=CARTESIAN_POINT ( 'NONE',  ( 16.13393739769620083, -29.47259540523039689, -47.64999999999999858 ) ) ;
#19821=CARTESIAN_POINT ( 'NONE',  ( 0.3188076311095680571, -20.69863068615319790, -34.65000336222090027 ) ) ;
#19823=CARTESIAN_POINT ( 'NONE',  ( 42.10508499193715437, 8.543310626597461876, -75.82482327354601637 ) ) ;
#19828=CARTESIAN_POINT ( 'NONE',  ( 0.06051628023451229715, 19.81643162424870042, -34.85735264049939985 ) ) ;
#19832=DIRECTION ( 'NONE',  ( 0.6522074047277948150, -0.2731766849828846100, 0.7071067811865450192 ) ) ;
#19835=DIRECTION ( 'NONE',  ( -0.8660254037844321573, 0.5000000000000111022, 0.000000000000000000 ) ) ;
#19841=CARTESIAN_POINT ( 'NONE',  ( 29.13393739769619728, -35.78776181993320193, -84.63196841427449613 ) ) ;
#19843=CARTESIAN_POINT ( 'NONE',  ( 9.026390854478798076, 16.60930999848670098, -54.64999999999999858 ) ) ;
#19848=CARTESIAN_POINT ( 'NONE',  ( 17.89246938939492182, -41.85765695298068323, -34.70142521051216988 ) ) ;
#19855=CARTESIAN_POINT ( 'NONE',  ( 46.69650754312519325, -39.84281285528089711, -54.54193493916549329 ) ) ;
#19863=DIRECTION ( 'NONE',  ( -0.1961161351381830731, 0.000000000000000000, -0.9805806756909203337 ) ) ;
#19869=DIRECTION ( 'NONE',  ( 0.000000000000000000, 0.000000000000000000, 1.000000000000000000 ) ) ;
#19874=CARTESIAN_POINT ( 'NONE',  ( 41.91430865176237575, 7.521317205359935087, -81.04388926812714544 ) ) ;
#19895=EDGE_LOOP ( 'NONE', ( #25298, #8498, #34975, #26009 ) ) ;
#19902=DIRECTION ( 'NONE',  ( -1.000000000000000000, -1.006844464268868150E-16, 0.000000000000000000 ) ) ;
#19903=FACE_OUTER_BOUND ( 'NONE', #36005, .T. ) ;
#19908=ADVANCED_FACE ( 'NONE', ( #18011 ), #18263, .F. ) ;
#19922=ADVANCED_FACE ( 'NONE', ( #34231 ), #29785, .T. ) ;
#19925=DIRECTION ( 'NONE',  ( 0.000000000000000000, 1.000000000000000000, 0.000000000000000000 ) ) ;
#19956=ORIENTED_EDGE ( 'NONE', *, *, #29270, .T. ) ;
#19961=CARTESIAN_POINT ( 'NONE',  ( 17.63604474694339785, 0.9274771370723400299, -34.65000333055159842 ) ) ;
#19974=( BOUNDED_CURVE ( )  B_SPLINE_CURVE ( 3, ( #2648, #10770, #50079, #14174 ),
 .UNSPECIFIED., .F., .T. ) 
 B_SPLINE_CURVE_WITH_KNOTS ( ( 4, 4 ),
 ( 0.7853981633974705945, 1.570796326794917430 ),
 .UNSPECIFIED. ) 
 CURVE ( )  GEOMETRIC_REPRESENTATION_ITEM ( )  RATIONAL_B_SPLINE_CURVE ( ( 1.000000000000000000, 0.9492530216741912330, 0.9492530216741912330, 1.000000000000000000 ) ) 
 REPRESENTATION_ITEM ( '' )  );
#19977=DIRECTION ( 'NONE',  ( 0.000000000000000000, 0.000000000000000000, 1.000000000000000000 ) ) ;
#19979=EDGE_LOOP ( 'NONE', ( #36021, #38290, #41049, #49667 ) ) ;
#19989=CARTESIAN_POINT ( 'NONE',  ( 15.13982274958659247, 18.38378545640599171, -83.22692977633533928 ) ) ;
#19994=PLANE ( 'NONE',  #7362 ) ;
#19996=CARTESIAN_POINT ( 'NONE',  ( -0.3016046179078940015, -20.31737465961040101, -35.02873218748179340 ) ) ;
#20007=AXIS2_PLACEMENT_3D ( 'NONE', #42042, #38367, #49661 ) ;
#20014=ORIENTED_EDGE ( 'NONE', *, *, #2966, .F. ) ;
#20018=ORIENTED_EDGE ( 'NONE', *, *, #28477, .T. ) ;
#20019=LINE ( 'NONE', #32836, #50032 ) ;
#20027=CARTESIAN_POINT ( 'NONE',  ( 44.47986911915002395, 1.897766893668719312, -48.24899763051212886 ) ) ;
#20030=EDGE_CURVE ( 'NONE', #22337, #51786, #38569, .T. ) ;
#20040=AXIS2_PLACEMENT_3D ( 'NONE', #45941, #30958, #43806 ) ;
#20049=CARTESIAN_POINT ( 'NONE',  ( 43.05557787259338909, -39.87155913697362308, -71.22985127916425085 ) ) ;
#20050=B_SPLINE_CURVE_WITH_KNOTS ( 'NONE', 3,
 ( #774, #16003, #31957, #47978 ),
 .UNSPECIFIED., .F., .F.,
 ( 4, 4 ),
 ( 0.1435918933159660016, 0.1514974462201259253 ),
 .UNSPECIFIED. ) ;
#20065=CARTESIAN_POINT ( 'NONE',  ( 0.3209249304026170480, -20.69829881652800196, -34.64999999999999858 ) ) ;
#20067=CARTESIAN_POINT ( 'NONE',  ( 42.54370938950081182, 8.589020448392009399, -73.70510818031742417 ) ) ;
#20068=CARTESIAN_POINT ( 'NONE',  ( -0.007164427059776000244, -8.408015226406421405, -34.77269723891829756 ) ) ;
#20070=CARTESIAN_POINT ( 'NONE',  ( 30.34915280000618409, 4.391813942490763623, -84.60938206585605315 ) ) ;
#20080=AXIS2_PLACEMENT_3D ( 'NONE', #16371, #7750, #39967 ) ;
#20085=VERTEX_POINT ( 'NONE', #35019 ) ;
#20086=CIRCLE ( 'NONE', #30104, 34.47562460986260646 ) ;
#20088=CARTESIAN_POINT ( 'NONE',  ( -21.49961078222543520, -5.348885346992251932, -53.70438154331316127 ) ) ;
#20095=DIRECTION ( 'NONE',  ( -0.000000000000000000, 1.000000000000000000, 0.000000000000000000 ) ) ;
#20119=DIRECTION ( 'NONE',  ( 0.000000000000000000, 0.000000000000000000, 1.000000000000000000 ) ) ;
#20120=CARTESIAN_POINT ( 'NONE',  ( 16.13393739769639623, 7.383811055320659733, -62.64999999999999858 ) ) ;
#20124=ORIENTED_EDGE ( 'NONE', *, *, #34467, .T. ) ;
#20127=CARTESIAN_POINT ( 'NONE',  ( 45.51548074848881242, 6.624593763210348207, -62.69088906692822860 ) ) ;
#20141=ADVANCED_FACE ( 'NONE', ( #670 ), #16142, .T. ) ;
#20144=DIRECTION ( 'NONE',  ( -1.000000000000000000, 0.000000000000000000, 0.000000000000000000 ) ) ;
#20157=VECTOR ( 'NONE', #32739, 1000.000000000000000 ) ;
#20159=CIRCLE ( 'NONE', #21011, 2.999999999999999556 ) ;
#20160=CARTESIAN_POINT ( 'NONE',  ( 18.07449423817559975, -32.55558437065590027, -34.90839531524139971 ) ) ;
#20171=CARTESIAN_POINT ( 'NONE',  ( 16.13393739769620083, -15.61618894467929941, -35.12503119152809461 ) ) ;
#20175=FACE_OUTER_BOUND ( 'NONE', #39706, .T. ) ;
#20179=CARTESIAN_POINT ( 'NONE',  ( 15.31199894099709979, -16.87369336301570044, -35.14999999999999858 ) ) ;
#20184=ORIENTED_EDGE ( 'NONE', *, *, #48527, .F. ) ;
#20185=VECTOR ( 'NONE', #6034, 1000.000000000000000 ) ;
#20195=CARTESIAN_POINT ( 'NONE',  ( -0.2865249686166103094, -8.445231654028917845, -35.01561944896767642 ) ) ;
#20200=EDGE_CURVE ( 'NONE', #21257, #33273, #24132, .T. ) ;
#20219=CARTESIAN_POINT ( 'NONE',  ( 42.36605831465526251, 6.449731470917973830, -78.48939217686074699 ) ) ;
#20221=EDGE_CURVE ( 'NONE', #46925, #11609, #45229, .T. ) ;
#20224=CARTESIAN_POINT ( 'NONE',  ( 42.19548255040618301, -37.65468939562691730, -79.34225115792774830 ) ) ;
#20226=ORIENTED_EDGE ( 'NONE', *, *, #26644, .F. ) ;
#20242=CARTESIAN_POINT ( 'NONE',  ( 2.414204846871564669, -5.385696586492555227, -35.10658870009159216 ) ) ;
#20254=CARTESIAN_POINT ( 'NONE',  ( -0.2068757739851316280, -20.53916885483576849, -34.94635309924921529 ) ) ;
#20261=ORIENTED_EDGE ( 'NONE', *, *, #28600, .F. ) ;
#20262=CYLINDRICAL_SURFACE ( 'NONE', #45498, 0.4999999999999982236 ) ;
#20265=VERTEX_POINT ( 'NONE', #24232 ) ;
#20278=EDGE_CURVE ( 'NONE', #32200, #51495, #416, .T. ) ;
#20281=( BOUNDED_CURVE ( )  B_SPLINE_CURVE ( 3, ( #5894, #38125, #34164, #2220 ),
 .UNSPECIFIED., .F., .T. ) 
 B_SPLINE_CURVE_WITH_KNOTS ( ( 4, 4 ),
 ( 0.7853981633974498333, 1.570796326794903219 ),
 .UNSPECIFIED. ) 
 CURVE ( )  GEOMETRIC_REPRESENTATION_ITEM ( )  RATIONAL_B_SPLINE_CURVE ( ( 1.000000000000000000, 0.9492530216741903448, 0.9492530216741903448, 1.000000000000000000 ) ) 
 REPRESENTATION_ITEM ( '' )  );
#20293=PLANE ( 'NONE',  #34650 ) ;
#20298=CARTESIAN_POINT ( 'NONE',  ( 28.28038400710289935, -8.603434725040973063, -34.79644660940672907 ) ) ;
#20301=CARTESIAN_POINT ( 'NONE',  ( 44.01566611027487141, -39.95595433770805016, -66.58381346753706964 ) ) ;
#20306=EDGE_CURVE ( 'NONE', #6210, #885, #17877, .T. ) ;
#20308=CARTESIAN_POINT ( 'NONE',  ( 14.43662147174949872, -32.33724466207230108, -34.68801049095930011 ) ) ;
#20309=DIRECTION ( 'NONE',  ( -0.6561787149247867434, 0.000000000000000000, 0.7546055221635046273 ) ) ;
#20319=CARTESIAN_POINT ( 'NONE',  ( 41.23411137459665810, 8.445767796141971928, -80.02631633623509799 ) ) ;
#20320=CARTESIAN_POINT ( 'NONE',  ( 45.14832757675640096, -33.29289077328009938, -35.14999999999999858 ) ) ;
#20328=EDGE_LOOP ( 'NONE', ( #6027, #39751, #14092, #6810, #35560, #12054 ) ) ;
#20336=VERTEX_POINT ( 'NONE', #38397 ) ;
#20351=AXIS2_PLACEMENT_3D ( 'NONE', #15828, #22186, #39434 ) ;
#20388=VECTOR ( 'NONE', #12719, 1000.000000000000000 ) ;
#20390=EDGE_LOOP ( 'NONE', ( #38615, #8882, #27201, #21362 ) ) ;
#20403=ADVANCED_FACE ( 'NONE', ( #26326 ), #14290, .T. ) ;
#20422=AXIS2_PLACEMENT_3D ( 'NONE', #47017, #18950, #22355 ) ;
#20427=( BOUNDED_CURVE ( )  B_SPLINE_CURVE ( 3, ( #17670, #17411, #22098, #6656 ),
 .UNSPECIFIED., .F., .T. ) 
 B_SPLINE_CURVE_WITH_KNOTS ( ( 4, 4 ),
 ( 5.135640914169340654, 7.430729701136489673 ),
 .UNSPECIFIED. ) 
 CURVE ( )  GEOMETRIC_REPRESENTATION_ITEM ( )  RATIONAL_B_SPLINE_CURVE ( ( 1.000000000000000000, 0.6071517307476801406, 0.6071517307476801406, 1.000000000000000000 ) ) 
 REPRESENTATION_ITEM ( '' )  );
#20433=CARTESIAN_POINT ( 'NONE',  ( 30.55306054313505371, -35.64636550620694777, -84.61298601366885919 ) ) ;
#20458=LINE ( 'NONE', #1344, #41910 ) ;
#20460=ORIENTED_EDGE ( 'NONE', *, *, #5721, .F. ) ;
#20465=B_SPLINE_CURVE_WITH_KNOTS ( 'NONE', 3,
 ( #16751, #1286, #45571, #41117, #17021, #5231, #9664, #32703, #41371, #12835 ),
 .UNSPECIFIED., .F., .F.,
 ( 4, 2, 2, 2, 4 ),
 ( -0.0003767167459391999786, 0.000000000000000000, 0.01529901560024879946, 0.03030530679091670079, 0.04513248637320322471 ),
 .UNSPECIFIED. ) ;
#20475=CARTESIAN_POINT ( 'NONE',  ( 45.27534771981950001, 2.448353903276920374, -34.68491900127439465 ) ) ;
#20476=AXIS2_PLACEMENT_3D ( 'NONE', #35531, #3307, #23448 ) ;
#20477=CARTESIAN_POINT ( 'NONE',  ( 42.51983742818366352, -37.70581418102509019, -77.72045495091650480 ) ) ;
#20506=EDGE_CURVE ( 'NONE', #51641, #47003, #49788, .T. ) ;
#20518=CARTESIAN_POINT ( 'NONE',  ( 16.13393739769620083, -15.61618894467929941, -54.64999999999999858 ) ) ;
#20523=VERTEX_POINT ( 'NONE', #7644 ) ;
#20524=VERTEX_POINT ( 'NONE', #35676 ) ;
#20529=CARTESIAN_POINT ( 'NONE',  ( 0.4142048468714032983, -8.849798201630209249, -35.10658870009234533 ) ) ;
#20533=DIRECTION ( 'NONE',  ( 0.4999999999999998890, -0.8660254037844387076, 0.000000000000000000 ) ) ;
#20536=VECTOR ( 'NONE', #19863, 1000.000000000000114 ) ;
#20540=CARTESIAN_POINT ( 'NONE',  ( 22.13393739769619728, -54.15188668067469990, -35.14999999999999858 ) ) ;
#20541=CARTESIAN_POINT ( 'NONE',  ( 38.67452568954050207, -37.56081407618439982, -81.65000000000000568 ) ) ;
#20556=CARTESIAN_POINT ( 'NONE',  ( 43.46623457429583226, -39.90877955095767504, -69.24476199280557864 ) ) ;
#20558=AXIS2_PLACEMENT_3D ( 'NONE', #18777, #19035, #35543 ) ;
#20572=EDGE_LOOP ( 'NONE', ( #22987, #1011, #46922, #32175 ) ) ;
#20575=CARTESIAN_POINT ( 'NONE',  ( 23.32557412215919967, 18.09884784672449953, -34.65000333295999724 ) ) ;
#20577=CARTESIAN_POINT ( 'NONE',  ( 41.80405099542780789, 8.510870798982260510, -77.27697826269607617 ) ) ;
#20590=VECTOR ( 'NONE', #22040, 1000.000000000000114 ) ;
#20595=DIRECTION ( 'NONE',  ( 1.000000000000000000, 0.000000000000000000, 0.000000000000000000 ) ) ;
#20600=ORIENTED_EDGE ( 'NONE', *, *, #37084, .T. ) ;
#20609=ADVANCED_FACE ( 'NONE', ( #10218 ), #26178, .T. ) ;
#20612=CARTESIAN_POINT ( 'NONE',  ( -0.02503409344755289437, -27.07639387936528763, -34.78823607925544081 ) ) ;
#20623=DIRECTION ( 'NONE',  ( 0.000000000000000000, 0.000000000000000000, -1.000000000000000000 ) ) ;
#20627=CARTESIAN_POINT ( 'NONE',  ( 24.58073416742070094, -18.76089852590099838, -35.14999999999999858 ) ) ;
#20634=ADVANCED_FACE ( 'NONE', ( #14916 ), #27734, .T. ) ;
#20639=CARTESIAN_POINT ( 'NONE',  ( 2.543036500622879892, -5.976568861398989796, -34.65032322548090349 ) ) ;
#20649=ORIENTED_EDGE ( 'NONE', *, *, #31232, .T. ) ;
#20650=B_SPLINE_CURVE_WITH_KNOTS ( 'NONE', 3,
 ( #14227, #29929, #30199, #30453 ),
 .UNSPECIFIED., .F., .F.,
 ( 4, 4 ),
 ( 0.000000000000000000, 1.000000000000000000 ),
 .UNSPECIFIED. ) ;
#20662=DIRECTION ( 'NONE',  ( 0.000000000000000000, 1.000000000000000000, 0.000000000000000000 ) ) ;
#20665=ORIENTED_EDGE ( 'NONE', *, *, #11943, .F. ) ;
#20679=CARTESIAN_POINT ( 'NONE',  ( 47.13393739769619373, -36.11618894467930119, -35.14999999999999858 ) ) ;
#20685=CARTESIAN_POINT ( 'NONE',  ( 28.63604668330599878, -4.677882819536359982, -34.65000333679609668 ) ) ;
#20689=CARTESIAN_POINT ( 'NONE',  ( 42.64825840273801560, -39.90276718693228730, -72.90723142289991188 ) ) ;
#20695=ORIENTED_EDGE ( 'NONE', *, *, #19092, .F. ) ;
#20721=DIRECTION ( 'NONE',  ( 0.8660254037844379305, -0.5000000000000011102, -2.498001805406606160E-16 ) ) ;
#20729=ORIENTED_EDGE ( 'NONE', *, *, #14209, .T. ) ;
#20732=FACE_OUTER_BOUND ( 'NONE', #23693, .T. ) ;
#20734=EDGE_LOOP ( 'NONE', ( #2388, #49319, #22766, #29753, #38740 ) ) ;
#20736=CARTESIAN_POINT ( 'NONE',  ( 42.65553098943552612, 6.494013008808203757, -77.04196490166894762 ) ) ;
#20739=CARTESIAN_POINT ( 'NONE',  ( 43.27761160094991766, -37.81795400707816412, -73.93156894824470271 ) ) ;
#20740=ORIENTED_EDGE ( 'NONE', *, *, #29699, .T. ) ;
#20742=( BOUNDED_CURVE ( )  B_SPLINE_CURVE ( 3, ( #31349, #7790, #6766, #23742 ),
 .UNSPECIFIED., .F., .T. ) 
 B_SPLINE_CURVE_WITH_KNOTS ( ( 4, 4 ),
 ( 5.964622971501799320, 6.208697808690975428 ),
 .UNSPECIFIED. ) 
 CURVE ( )  GEOMETRIC_REPRESENTATION_ITEM ( )  RATIONAL_B_SPLINE_CURVE ( ( 1.000000000000000000, 0.9950417810232484728, 0.9950417810232484728, 1.000000000000000000 ) ) 
 REPRESENTATION_ITEM ( '' )  );
#20746=EDGE_CURVE ( 'NONE', #1986, #14340, #30563, .T. ) ;
#20753=ORIENTED_EDGE ( 'NONE', *, *, #17221, .F. ) ;
#20767=DIRECTION ( 'NONE',  ( 0.000000000000000000, 1.000000000000000000, 0.000000000000000000 ) ) ;
#20777=CARTESIAN_POINT ( 'NONE',  ( -0.2828855350156033732, -10.86435776103753881, -35.01245472409725323 ) ) ;
#20793=ORIENTED_EDGE ( 'NONE', *, *, #27247, .T. ) ;
#20806=DIRECTION ( 'NONE',  ( -0.06538141124691354555, 0.04750237581189065833, -0.9967290481146758863 ) ) ;
#20815=EDGE_LOOP ( 'NONE', ( #30583, #33756, #16203, #12033 ) ) ;
#20816=CARTESIAN_POINT ( 'NONE',  ( 18.09749211374589706, 1.343694785579789830, -34.95504743437659556 ) ) ;
#20817=CARTESIAN_POINT ( 'NONE',  ( 28.49955684666384670, -8.476895227121406862, -34.64999999999999858 ) ) ;
#20820=CARTESIAN_POINT ( 'NONE',  ( 41.88138692637217275, -39.75166464432179936, -76.90407068535067481 ) ) ;
#20821=CARTESIAN_POINT ( 'NONE',  ( 14.49955684666382716, -41.98180839364702166, -34.65000000000001279 ) ) ;
#20824=VECTOR ( 'NONE', #10437, 1000.000000000000000 ) ;
#20829=CARTESIAN_POINT ( 'NONE',  ( 14.28038030992529528, -32.47778390180254604, -34.79644291222909658 ) ) ;
#20830=DIRECTION ( 'NONE',  ( -0.3863301728269291635, 0.9223605572461970326, 0.000000000000000000 ) ) ;
#20835=DIRECTION ( 'NONE',  ( -1.000000000000000000, 0.000000000000000000, 0.000000000000000000 ) ) ;
#20837=DIRECTION ( 'NONE',  ( 0.7071067811865472397, -0.7071067811865479058, 0.000000000000000000 ) ) ;
#20839=CARTESIAN_POINT ( 'NONE',  ( 42.21804547344670056, 8.555463751753345392, -75.27853559423084562 ) ) ;
#20854=ORIENTED_EDGE ( 'NONE', *, *, #6265, .T. ) ;
#20857=CARTESIAN_POINT ( 'NONE',  ( -8.492060748862416020, 14.62552918811035063, -42.53773143905051768 ) ) ;
#20861=CARTESIAN_POINT ( 'NONE',  ( 38.67452568954060155, -36.11618894467930119, -84.65000000000000568 ) ) ;
#20863=EDGE_CURVE ( 'NONE', #4176, #29074, #28792, .T. ) ;
#20864=VERTEX_POINT ( 'NONE', #48903 ) ;
#20877=EDGE_CURVE ( 'NONE', #37366, #4162, #11051, .T. ) ;
#20904=CARTESIAN_POINT ( 'NONE',  ( 18.63393739769619728, -45.61618894467940066, -35.14999999999999858 ) ) ;
#20923=FACE_OUTER_BOUND ( 'NONE', #27592, .T. ) ;
#20929=CARTESIAN_POINT ( 'NONE',  ( 16.97276188636960015, -43.80059717415329601, -59.64999999999999147 ) ) ;
#20930=CARTESIAN_POINT ( 'NONE',  ( 15.01109173769499883, -43.96113075119600211, -62.64999999999999858 ) ) ;
#20940=AXIS2_PLACEMENT_3D ( 'NONE', #26546, #22357, #18694 ) ;
#20952=CARTESIAN_POINT ( 'NONE',  ( 17.12805204922614877, -49.61616334567082021, -83.22692977624372190 ) ) ;
#20954=DIRECTION ( 'NONE',  ( 0.000000000000000000, 0.000000000000000000, 1.000000000000000000 ) ) ;
#20955=CARTESIAN_POINT ( 'NONE',  ( 29.13393739769619728, -35.78776181993320193, -84.63196841427449613 ) ) ;
#20973=ORIENTED_EDGE ( 'NONE', *, *, #16127, .T. ) ;
#20979=CARTESIAN_POINT ( 'NONE',  ( 27.68571409299283914, -36.31111876860410348, -34.79644660940672907 ) ) ;
#20981=EDGE_CURVE ( 'NONE', #31098, #39196, #1018, .T. ) ;
#20982=CARTESIAN_POINT ( 'NONE',  ( 2.501736331312110373, -25.44663551349389863, -34.68801049095939959 ) ) ;
#20999=CARTESIAN_POINT ( 'NONE',  ( 10.06369629473941352, -53.99262654158863484, -34.79644414665150975 ) ) ;
#21005=ORIENTED_EDGE ( 'NONE', *, *, #12966, .F. ) ;
#21011=AXIS2_PLACEMENT_3D ( 'NONE', #19257, #51246, #47825 ) ;
#21013=EDGE_CURVE ( 'NONE', #11609, #26529, #15711, .T. ) ;
#21025=CARTESIAN_POINT ( 'NONE',  ( 22.19769533645140314, 22.77497238916379274, -34.80997524099235818 ) ) ;
#21030=LINE ( 'NONE', #40957, #29253 ) ;
#21036=ORIENTED_EDGE ( 'NONE', *, *, #37329, .T. ) ;
#21052=( BOUNDED_CURVE ( )  B_SPLINE_CURVE ( 2, ( #30832, #39239, #11981 ),
 .UNSPECIFIED., .F., .T. ) 
 B_SPLINE_CURVE_WITH_KNOTS ( ( 3, 3 ),
 ( 0.1321855491173860031, 2.139356573168320175 ),
 .UNSPECIFIED. ) 
 CURVE ( )  GEOMETRIC_REPRESENTATION_ITEM ( )  RATIONAL_B_SPLINE_CURVE ( ( 1.001093714201189977, 1.008874108730310137, 1.000760730674130183 ) ) 
 REPRESENTATION_ITEM ( '' )  );
#21054=DIRECTION ( 'NONE',  ( 0.000000000000000000, 0.000000000000000000, 1.000000000000000000 ) ) ;
#21072=CARTESIAN_POINT ( 'NONE',  ( 16.72856488856178458, -39.04821110511426951, 4.943674098299959851 ) ) ;
#21076=VERTEX_POINT ( 'NONE', #51167 ) ;
#21078=EDGE_CURVE ( 'NONE', #19127, #14308, #19440, .T. ) ;
#21081=ADVANCED_FACE ( 'NONE', ( #26516 ), #6620, .T. ) ;
#21091=CARTESIAN_POINT ( 'NONE',  ( 14.39116781407879841, -32.37825826146760733, -34.70985242058469566 ) ) ;
#21101=CARTESIAN_POINT ( 'NONE',  ( 43.68437078864629086, 8.695783843854092865, -68.18794609937623363 ) ) ;
#21112=CARTESIAN_POINT ( 'NONE',  ( 19.21265657477716005, 18.23736444591407135, -34.79644660940672907 ) ) ;
#21114=DIRECTION ( 'NONE',  ( -0.8660254037844351549, 0.5000000000000061062, 0.000000000000000000 ) ) ;
#21116=ORIENTED_EDGE ( 'NONE', *, *, #5369, .T. ) ;
#21125=VERTEX_POINT ( 'NONE', #38859 ) ;
#21143=EDGE_CURVE ( 'NONE', #9803, #24151, #32059, .T. ) ;
#21154=TOROIDAL_SURFACE ( 'NONE', #4450, 34.47562460986249988, 0.5000000000000000000 ) ;
#21177=CARTESIAN_POINT ( 'NONE',  ( -10.09487475708679938, -44.93564566225139600, -43.84234880612240204 ) ) ;
#21180=LINE ( 'NONE', #44790, #29182 ) ;
#21183=ORIENTED_EDGE ( 'NONE', *, *, #26854, .F. ) ;
#21186=ORIENTED_EDGE ( 'NONE', *, *, #50472, .T. ) ;
#21192=AXIS2_PLACEMENT_3D ( 'NONE', #32047, #9012, #32819 ) ;
#21198=CIRCLE ( 'NONE', #46376, 2.999999999999999112 ) ;
#21206=CARTESIAN_POINT ( 'NONE',  ( 14.71607358137469213, -49.61616928914560987, -83.19610070255293977 ) ) ;
#21208=DIRECTION ( 'NONE',  ( 0.000000000000000000, 1.000000000000000000, 0.000000000000000000 ) ) ;
#21209=CARTESIAN_POINT ( 'NONE',  ( 14.13958958331975602, 1.371102756008198975, -35.06583844469734146 ) ) ;
#21236=VECTOR ( 'NONE', #50816, 1000.000000000000000 ) ;
#21244=DIRECTION ( 'NONE',  ( 0.3863301728269178947, 0.9223605572462016955, 0.000000000000000000 ) ) ;
#21250=LINE ( 'NONE', #1357, #26786 ) ;
#21257=VERTEX_POINT ( 'NONE', #27810 ) ;
#21261=EDGE_CURVE ( 'NONE', #30405, #51582, #10979, .T. ) ;
#21267=EDGE_CURVE ( 'NONE', #5164, #41828, #34673, .T. ) ;
#21281=CARTESIAN_POINT ( 'NONE',  ( -11.39236625349560050, -33.81790884424879806, -54.64999999999999858 ) ) ;
#21290=VECTOR ( 'NONE', #43583, 1000.000000000000114 ) ;
#21305=DIRECTION ( 'NONE',  ( -0.5000000000000003331, -0.8660254037844385966, 0.000000000000000000 ) ) ;
#21313=CARTESIAN_POINT ( 'NONE',  ( 16.13393739769620083, -15.61618894467929941, -35.02873218748179340 ) ) ;
#21315=EDGE_CURVE ( 'NONE', #46086, #40660, #9413, .T. ) ;
#21317=ORIENTED_EDGE ( 'NONE', *, *, #16365, .F. ) ;
#21320=EDGE_LOOP ( 'NONE', ( #12809, #49825, #26538, #47121 ) ) ;
#21326=DIRECTION ( 'NONE',  ( 1.000000000000000000, 0.000000000000000000, 0.000000000000000000 ) ) ;
#21339=CARTESIAN_POINT ( 'NONE',  ( 14.63393739769620083, -42.11618894467930119, -34.64999999999999858 ) ) ;
#21347=EDGE_CURVE ( 'NONE', #45957, #9803, #28315, .T. ) ;
#21348=VERTEX_POINT ( 'NONE', #16279 ) ;
#21350=( BOUNDED_CURVE ( )  B_SPLINE_CURVE ( 2, ( #21281, #9520, #5837 ),
 .UNSPECIFIED., .F., .T. ) 
 B_SPLINE_CURVE_WITH_KNOTS ( ( 3, 3 ),
 ( 0.1016765273446490064, 1.071465066788269915 ),
 .UNSPECIFIED. ) 
 CURVE ( )  GEOMETRIC_REPRESENTATION_ITEM ( )  RATIONAL_B_SPLINE_CURVE ( ( 1.000011650623809922, 1.000064461280040007, 1.000064793140389874 ) ) 
 REPRESENTATION_ITEM ( '' )  );
#21355=CARTESIAN_POINT ( 'NONE',  ( 23.43760361721910002, 17.88421590754850143, -34.68023162149790295 ) ) ;
#21357=CARTESIAN_POINT ( 'NONE',  ( 43.93192822685114152, 8.716773305526617222, -66.98897554911386010 ) ) ;
#21362=ORIENTED_EDGE ( 'NONE', *, *, #23152, .T. ) ;
#21372=ORIENTED_EDGE ( 'NONE', *, *, #37134, .T. ) ;
#21375=PLANE ( 'NONE',  #14518 ) ;
#21384=CIRCLE ( 'NONE', #28079, 11.00000000000000000 ) ;
#21386=LINE ( 'NONE', #41575, #9607 ) ;
#21391=EDGE_CURVE ( 'NONE', #33379, #1986, #33985, .T. ) ;
#21394=CARTESIAN_POINT ( 'NONE',  ( 46.53794730597209650, 8.809177800381760903, -54.64300708228900305 ) ) ;
#21396=EDGE_CURVE ( 'NONE', #31436, #16348, #45814, .T. ) ;
#21402=CARTESIAN_POINT ( 'NONE',  ( 46.43766614693377903, -40.11729158708158849, -54.83318600516120966 ) ) ;
#21408=DIRECTION ( 'NONE',  ( -0.8660254037844428154, -0.4999999999999928946, 0.000000000000000000 ) ) ;
#21413=ORIENTED_EDGE ( 'NONE', *, *, #33687, .F. ) ;
#21414=VECTOR ( 'NONE', #25604, 1000.000000000000000 ) ;
#21431=CARTESIAN_POINT ( 'NONE',  ( 17.98749078828956982, -7.616188944679219475, -34.79644660940672907 ) ) ;
#21434=CARTESIAN_POINT ( 'NONE',  ( -10.08776064405109985, -44.63142044503610606, -43.53771261949579952 ) ) ;
#21435=AXIS2_PLACEMENT_3D ( 'NONE', #18977, #50699, #34957 ) ;
#21438=FACE_OUTER_BOUND ( 'NONE', #27428, .T. ) ;
#21461=ADVANCED_FACE ( 'NONE', ( #37682 ), #46598, .T. ) ;
#21465=LINE ( 'NONE', #37465, #50677 ) ;
#21468=CARTESIAN_POINT ( 'NONE',  ( 18.65038606164732826, -49.61612828316260249, -83.08753104956571178 ) ) ;
#21472=CARTESIAN_POINT ( 'NONE',  ( 44.74727839785828110, -40.12401933091472728, -62.58727147069981100 ) ) ;
#21507=CARTESIAN_POINT ( 'NONE',  ( 9.026390854479029002, -47.84168788784550230, -54.64999999999999858 ) ) ;
#21513=PRODUCT ( 'Foot Base', 'Foot Base', '', ( #36662 ) ) ;
#21514=CARTESIAN_POINT ( 'NONE',  ( 29.13393739769619728, -35.78776181993320193, -84.65000000000000568 ) ) ;
#21520=CARTESIAN_POINT ( 'NONE',  ( 44.97398337673284630, -38.03923227423459963, -65.44976038934856888 ) ) ;
#21558=DIRECTION ( 'NONE',  ( 1.000000000000000000, 0.000000000000000000, 0.000000000000000000 ) ) ;
#21563=CARTESIAN_POINT ( 'NONE',  ( 15.29511290902269849, 12.56821928479459949, -59.64999999999999147 ) ) ;
#21572=CARTESIAN_POINT ( 'NONE',  ( 45.77379034717539241, 6.897320639510064133, -61.45073446201022449 ) ) ;
#21584=CARTESIAN_POINT ( 'NONE',  ( 16.13393739769620083, -15.61618894467929941, -35.14999999999999858 ) ) ;
#21587=VERTEX_POINT ( 'NONE', #31860 ) ;
#21593=CYLINDRICAL_SURFACE ( 'NONE', #11451, 0.4999999999999980571 ) ;
#21602=EDGE_LOOP ( 'NONE', ( #20649, #38997, #25403, #3800, #11725 ) ) ;
#21610=CARTESIAN_POINT ( 'NONE',  ( 44.69570754105031085, 8.776462964268782585, -63.28808277378300318 ) ) ;
#21615=ORIENTED_EDGE ( 'NONE', *, *, #8510, .T. ) ;
#21621=DIRECTION ( 'NONE',  ( -1.000000000000000000, 0.000000000000000000, 0.000000000000000000 ) ) ;
#21625=ADVANCED_FACE ( 'NONE', ( #23984 ), #15131, .T. ) ;
#21631=CARTESIAN_POINT ( 'NONE',  ( 0.3209249304026170480, -8.218592747557250888, -34.64999999999999858 ) ) ;
#21636=CARTESIAN_POINT ( 'NONE',  ( 8.664097273252640008, 17.56341275872060237, -34.96018206680729890 ) ) ;
#21655=EDGE_CURVE ( 'NONE', #41542, #44367, #15238, .T. ) ;
#21660=ORIENTED_EDGE ( 'NONE', *, *, #5369, .F. ) ;
#21662=VERTEX_POINT ( 'NONE', #22966 ) ;
#21664=DIRECTION ( 'NONE',  ( 1.000000000000000000, 0.000000000000000000, 0.000000000000000000 ) ) ;
#21679=EDGE_CURVE ( 'NONE', #44397, #7182, #51292, .T. ) ;
#21682=DIRECTION ( 'NONE',  ( -0.8660254037844379305, 0.5000000000000011102, 0.000000000000000000 ) ) ;
#21685=ORIENTED_EDGE ( 'NONE', *, *, #46107, .F. ) ;
#21687=CARTESIAN_POINT ( 'NONE',  ( -3.761964000850550160, -48.86336368874830072, -38.03777212193249824 ) ) ;
#21694=ORIENTED_EDGE ( 'NONE', *, *, #457, .F. ) ;
#21717=CARTESIAN_POINT ( 'NONE',  ( 28.96098294488700020, -4.556468692969050771, -34.77057949856879304 ) ) ;
#21721=CARTESIAN_POINT ( 'NONE',  ( 17.62752711509774883, -49.61617099151992250, -83.19069868277399848 ) ) ;
#21723=ADVANCED_FACE ( 'NONE', ( #4874 ), #16665, .T. ) ;
#21725=PLANE ( 'NONE',  #24898 ) ;
#21726=CARTESIAN_POINT ( 'NONE',  ( 47.54692373198528088, -39.37158465659037887, -52.87480529148079711 ) ) ;
#21734=CARTESIAN_POINT ( 'NONE',  ( 47.04924918918376164, 9.060206648678184038, -51.28166297163371468 ) ) ;
#21738=CARTESIAN_POINT ( 'NONE',  ( 28.78179405415149716, -26.60912525585749933, -34.67096478998279707 ) ) ;
#21754=ORIENTED_EDGE ( 'NONE', *, *, #4383, .T. ) ;
#21769=DIRECTION ( 'NONE',  ( -0.3502816565540492477, 0.000000000000000000, 0.9366444154970182678 ) ) ;
#21771=CIRCLE ( 'NONE', #45204, 0.5000000000000004441 ) ;
#21777=CARTESIAN_POINT ( 'NONE',  ( 45.66390452674965417, -38.11751718055511162, -62.00015498513875656 ) ) ;
#21778=EDGE_LOOP ( 'NONE', ( #44460, #47180, #51817, #4665 ) ) ;
#21784=VECTOR ( 'NONE', #33956, 1000.000000000000000 ) ;
#21785=DIRECTION ( 'NONE',  ( 0.6975711590030510001, -0.7165155114351260401, 0.000000000000000000 ) ) ;
#21794=CARTESIAN_POINT ( 'NONE',  ( 41.89882026671822501, -39.75356028169188249, -76.81997356724833992 ) ) ;
#21805=TOROIDAL_SURFACE ( 'NONE', #7653, 2.500000000000000000, 0.5000000000000000000 ) ;
#21808=CARTESIAN_POINT ( 'NONE',  ( 28.63393739769619728, -12.15208732954159920, -35.14999999999999858 ) ) ;
#21815=ORIENTED_EDGE ( 'NONE', *, *, #50717, .F. ) ;
#21816=PLANE ( 'NONE',  #6212 ) ;
#21831=CARTESIAN_POINT ( 'NONE',  ( 0.08961746015897842366, -4.353854841787279106, -34.70268271585497644 ) ) ;
#21834=CARTESIAN_POINT ( 'NONE',  ( 46.46313271365296771, 6.967551557107034554, -58.00402283214241805 ) ) ;
#21844=VECTOR ( 'NONE', #23170, 1000.000000000000114 ) ;
#21861=CARTESIAN_POINT ( 'NONE',  ( 23.13393739769620083, -2.337132753317950229, -39.64999999999999858 ) ) ;
#21868=ORIENTED_EDGE ( 'NONE', *, *, #24976, .F. ) ;
#21877=CARTESIAN_POINT ( 'NONE',  ( 44.34077148419982706, 8.749635085101930443, -65.00859125368401692 ) ) ;
#21888=FACE_OUTER_BOUND ( 'NONE', #38992, .T. ) ;
#21889=VERTEX_POINT ( 'NONE', #16148 ) ;
#21890=ORIENTED_EDGE ( 'NONE', *, *, #29651, .F. ) ;
#21891=CARTESIAN_POINT ( 'NONE',  ( 23.13393739769620083, -28.89524513604070322, -62.14999999999999858 ) ) ;
#21893=VERTEX_POINT ( 'NONE', #49181 ) ;
#21911=CARTESIAN_POINT ( 'NONE',  ( 46.17042861094817852, -40.10310485825260685, -56.13152800437062240 ) ) ;
#21912=ADVANCED_FACE ( 'NONE', ( #36311 ), #16408, .T. ) ;
#21916=EDGE_CURVE ( 'NONE', #18727, #218, #5935, .T. ) ;
#21919=DIRECTION ( 'NONE',  ( 0.000000000000000000, -1.000000000000000000, 0.000000000000000000 ) ) ;
#21922=ORIENTED_EDGE ( 'NONE', *, *, #40384, .F. ) ;
#21924=EDGE_LOOP ( 'NONE', ( #30521, #36233, #38705, #8294, #4610 ) ) ;
#21926=CARTESIAN_POINT ( 'NONE',  ( 0.3209249304026170480, -50.71887597443840434, -35.14999999999999858 ) ) ;
#21927=CARTESIAN_POINT ( 'NONE',  ( 22.90395747212406619, -9.567216934256503436, -34.79644660940672907 ) ) ;
#21945=CARTESIAN_POINT ( 'NONE',  ( -22.85259296468129975, -13.70909830080150016, -54.73566662495469615 ) ) ;
#21957=ORIENTED_EDGE ( 'NONE', *, *, #30921, .F. ) ;
#21968=( BOUNDED_CURVE ( )  B_SPLINE_CURVE ( 3, ( #15037, #47535, #11632, #22884 ),
 .UNSPECIFIED., .F., .F. ) 
 B_SPLINE_CURVE_WITH_KNOTS ( ( 4, 4 ),
 ( 1.585967333057443135E-14, 0.7853981633974705945 ),
 .UNSPECIFIED. ) 
 CURVE ( )  GEOMETRIC_REPRESENTATION_ITEM ( )  RATIONAL_B_SPLINE_CURVE ( ( 1.000000000000000000, 0.9492530216741903448, 0.9492530216741903448, 1.000000000000000000 ) ) 
 REPRESENTATION_ITEM ( '' )  );
#21971=FACE_OUTER_BOUND ( 'NONE', #45235, .T. ) ;
#21982=CARTESIAN_POINT ( 'NONE',  ( -21.07041245915929650, -4.022908985583359964, -53.08810431803729557 ) ) ;
#21984=CARTESIAN_POINT ( 'NONE',  ( 43.01334310488699941, -38.96107795727259315, -75.34527945086897205 ) ) ;
#21991=CARTESIAN_POINT ( 'NONE',  ( 46.15168749950237270, 8.992152203351947648, -55.73704961754241083 ) ) ;
#22000=TOROIDAL_SURFACE ( 'NONE', #42107, 38.50000000000000000, 0.5000000000000000000 ) ;
#22009=FACE_OUTER_BOUND ( 'NONE', #32191, .T. ) ;
#22011=CARTESIAN_POINT ( 'NONE',  ( 0.1457839871805953758, -45.96255801450852374, -34.68167748489142355 ) ) ;
#22017=DIRECTION ( 'NONE',  ( 0.9223605572462016955, -0.3863301728269178947, 0.000000000000000000 ) ) ;
#22025=CARTESIAN_POINT ( 'NONE',  ( 23.62400244246320113, 17.52418497763099836, -35.12503119152809461 ) ) ;
#22031=CARTESIAN_POINT ( 'NONE',  ( 45.79168803806123123, -38.13146365633215140, -61.36124641343345587 ) ) ;
#22032=EDGE_CURVE ( 'NONE', #11240, #51433, #49946, .T. ) ;
#22040=DIRECTION ( 'NONE',  ( 0.1961161351381840445, -2.713878504639270283E-16, 0.9805806756909201116 ) ) ;
#22047=CARTESIAN_POINT ( 'NONE',  ( 42.22239453466733750, -39.78826103684639293, -75.25768512366673235 ) ) ;
#22061=DIRECTION ( 'NONE',  ( -0.7071067811865475727, 0.000000000000000000, 0.7071067811865475727 ) ) ;
#22069=CARTESIAN_POINT ( 'NONE',  ( 17.98749078828957337, 10.53025766472752522, -34.79644660940672907 ) ) ;
#22080=ORIENTED_EDGE ( 'NONE', *, *, #30464, .F. ) ;
#22088=CARTESIAN_POINT ( 'NONE',  ( 45.78920227927463316, 6.898993018891284024, -61.37367372640163410 ) ) ;
#22098=CARTESIAN_POINT ( 'NONE',  ( -35.14957091781822385, 3.655592887048059403, -65.33131157870826655 ) ) ;
#22102=CARTESIAN_POINT ( 'NONE',  ( 22.37318698975080267, 22.37488585622680048, -34.64999999999999858 ) ) ;
#22114=PLANE ( 'NONE',  #18132 ) ;
#22116=AXIS2_PLACEMENT_3D ( 'NONE', #37404, #29269, #45272 ) ;
#22120=CARTESIAN_POINT ( 'NONE',  ( 16.13393739769620083, -1.182432214938700099, -34.64999999999999858 ) ) ;
#22130=CARTESIAN_POINT ( 'NONE',  ( -0.1295185695942999982, 0.6472670226113349523, -59.64999999999999147 ) ) ;
#22134=CARTESIAN_POINT ( 'NONE',  ( 44.44582319305163054, 8.758006262679185028, -64.49853979666923465 ) ) ;
#22141=CARTESIAN_POINT ( 'NONE',  ( -22.73139975955365344, -18.77686687743244320, -54.68857781686908481 ) ) ;
#22149=CARTESIAN_POINT ( 'NONE',  ( 18.63393739769599833, 14.38381105532070059, -34.64999999999999858 ) ) ;
#22151=LINE ( 'NONE', #1741, #6597 ) ;
#22163=CARTESIAN_POINT ( 'NONE',  ( 46.63357160382179956, 8.689668561411270531, -54.59574113304929455 ) ) ;
#22176=DIRECTION ( 'NONE',  ( 0.000000000000000000, 0.000000000000000000, -1.000000000000000000 ) ) ;
#22186=DIRECTION ( 'NONE',  ( -0.8340645993220436871, 0.5516667872527389882, 0.000000000000000000 ) ) ;
#22196=VECTOR ( 'NONE', #39468, 1000.000000000000000 ) ;
#22200=LINE ( 'NONE', #25358, #3953 ) ;
#22205=CARTESIAN_POINT ( 'NONE',  ( -1.572464511459390035, -50.27926404661009485, -36.17267532414179954 ) ) ;
#22218=DIRECTION ( 'NONE',  ( 1.000000000000000000, 0.000000000000000000, 0.000000000000000000 ) ) ;
#22235=EDGE_CURVE ( 'NONE', #26382, #36140, #37442, .T. ) ;
#22243=CARTESIAN_POINT ( 'NONE',  ( 41.86472757144029799, -37.59316321825600227, -80.99597773300310166 ) ) ;
#22244=DIRECTION ( 'NONE',  ( 0.000000000000000000, -0.7071067811865492381, 0.7071067811865457964 ) ) ;
#22249=EDGE_CURVE ( 'NONE', #12167, #51433, #40362, .T. ) ;
#22260=TOROIDAL_SURFACE ( 'NONE', #50744, 2.500000000000000000, 0.5000000000000000000 ) ;
#22261=ORIENTED_EDGE ( 'NONE', *, *, #44650, .T. ) ;
#22277=CARTESIAN_POINT ( 'NONE',  ( 20.30127474080329719, 10.88381105532070059, -34.64999999999999858 ) ) ;
#22284=CARTESIAN_POINT ( 'NONE',  ( 47.13393739769619373, 4.883811055320659733, -35.14999999999999858 ) ) ;
#22285=VECTOR ( 'NONE', #5313, 1000.000000000000000 ) ;
#22288=EDGE_CURVE ( 'NONE', #26276, #36069, #6937, .T. ) ;
#22291=CARTESIAN_POINT ( 'NONE',  ( 43.95557740140245784, -37.91148288773651132, -70.54174288651782376 ) ) ;
#22304=ORIENTED_EDGE ( 'NONE', *, *, #43490, .T. ) ;
#22308=CARTESIAN_POINT ( 'NONE',  ( 41.96035236647510658, -39.76017481032943124, -76.52331057427426231 ) ) ;
#22310=DIRECTION ( 'NONE',  ( 0.000000000000000000, 0.000000000000000000, 1.000000000000000000 ) ) ;
#22315=EDGE_CURVE ( 'NONE', #15981, #20265, #27828, .T. ) ;
#22337=VERTEX_POINT ( 'NONE', #11035 ) ;
#22346=EDGE_CURVE ( 'NONE', #45450, #18491, #2655, .T. ) ;
#22350=CARTESIAN_POINT ( 'NONE',  ( 45.17780009201627678, 6.831281286145213016, -64.43066996210254160 ) ) ;
#22355=DIRECTION ( 'NONE',  ( -1.000000000000000000, 0.000000000000000000, 0.000000000000000000 ) ) ;
#22357=DIRECTION ( 'NONE',  ( 0.000000000000000000, 0.000000000000000000, 1.000000000000000000 ) ) ;
#22369=CARTESIAN_POINT ( 'NONE',  ( 44.13393739769620083, -36.11618894467930119, -35.14999999999999858 ) ) ;
#22376=EDGE_CURVE ( 'NONE', #20336, #16602, #51123, .T. ) ;
#22381=DIRECTION ( 'NONE',  ( 0.000000000000000000, 0.000000000000000000, 1.000000000000000000 ) ) ;
#22395=CARTESIAN_POINT ( 'NONE',  ( 46.28203251265257023, 8.876941422008853166, -55.58930854417799594 ) ) ;
#22397=CARTESIAN_POINT ( 'NONE',  ( 10.07635536168542245, -54.02136955896584425, -34.82441657595373385 ) ) ;
#22404=DIRECTION ( 'NONE',  ( -1.031008731411319881E-16, 1.000000000000000000, 0.000000000000000000 ) ) ;
#22411=B_SPLINE_CURVE_WITH_KNOTS ( 'NONE', 3,
 ( #43912, #44166, #16637, #36288, #48625, #44683, #40489, #48359, #16382, #31574 ),
 .UNSPECIFIED., .F., .F.,
 ( 4, 2, 2, 2, 4 ),
 ( -0.0004107207312076359960, 0.000000000000000000, 0.01419180571516310066, 0.04450164637011760210, 0.05031563485841133304 ),
 .UNSPECIFIED. ) ;
#22412=CARTESIAN_POINT ( 'NONE',  ( 16.13393739769620083, -29.47259540523039689, -35.14999999999999858 ) ) ;
#22418=CARTESIAN_POINT ( 'NONE',  ( 2.422196078461530178, -5.407548561780520124, -35.02873218748179340 ) ) ;
#22428=CARTESIAN_POINT ( 'NONE',  ( 44.39055831136107599, -39.98592374925685533, -64.76712992094270760 ) ) ;
#22430=AXIS2_PLACEMENT_3D ( 'NONE', #34791, #42682, #50797 ) ;
#22449=DIRECTION ( 'NONE',  ( 0.6918010270571969267, 0.3994115091971329190, 0.6015661104845219098 ) ) ;
#22464=EDGE_CURVE ( 'NONE', #38344, #6571, #28695, .T. ) ;
#22468=EDGE_CURVE ( 'NONE', #49938, #14025, #19104, .T. ) ;
#22476=DIRECTION ( 'NONE',  ( -0.8660254037844387076, -0.4999999999999998890, 0.000000000000000000 ) ) ;
#22489=CARTESIAN_POINT ( 'NONE',  ( -7.298084762738758613, -16.21081643554488494, 4.943674098299959851 ) ) ;
#22496=CARTESIAN_POINT ( 'NONE',  ( 29.04782745927229826, -4.524248062580669583, -34.86734588637909837 ) ) ;
#22497=CARTESIAN_POINT ( 'NONE',  ( 34.13393739769599478, 17.88381105532079829, -35.14999999999999858 ) ) ;
#22501=CARTESIAN_POINT ( 'NONE',  ( 46.70905700370144586, -39.31695218441910100, -57.02994487585867489 ) ) ;
#22505=VERTEX_POINT ( 'NONE', #4700 ) ;
#22508=ORIENTED_EDGE ( 'NONE', *, *, #4979, .F. ) ;
#22509=AXIS2_PLACEMENT_3D ( 'NONE', #46180, #18888, #30675 ) ;
#22517=CARTESIAN_POINT ( 'NONE',  ( 28.84982806847620296, -26.63452174666150185, -34.69901084462020435 ) ) ;
#22531=EDGE_LOOP ( 'NONE', ( #14817, #17247, #43129, #40996, #27425, #28451, #11723 ) ) ;
#22547=CARTESIAN_POINT ( 'NONE',  ( 44.32161486965532049, -37.95901749436502826, -68.71160878878293943 ) ) ;
#22562=ORIENTED_EDGE ( 'NONE', *, *, #12550, .T. ) ;
#22566=CARTESIAN_POINT ( 'NONE',  ( 42.22528920520127826, -39.78856913145678220, -75.24368859111383756 ) ) ;
#22571=CARTESIAN_POINT ( 'NONE',  ( 38.67452568954060155, 1.883811055320659955, -81.65000000000000568 ) ) ;
#22572=EDGE_CURVE ( 'NONE', #15955, #34773, #25114, .T. ) ;
#22584=DIRECTION ( 'NONE',  ( 0.000000000000000000, 1.000000000000000000, 0.000000000000000000 ) ) ;
#22587=CYLINDRICAL_SURFACE ( 'NONE', #9375, 0.4999999999999980571 ) ;
#22597=CARTESIAN_POINT ( 'NONE',  ( 14.13393739769640156, 10.38381105532060111, -54.64999999999999858 ) ) ;
#22599=ORIENTED_EDGE ( 'NONE', *, *, #9038, .F. ) ;
#22607=CARTESIAN_POINT ( 'NONE',  ( 46.27121035923033077, 6.948460380232488021, -58.96360570400401713 ) ) ;
#22611=CARTESIAN_POINT ( 'NONE',  ( 0.3209249304026170480, -15.61618894467929941, -35.14999999999999858 ) ) ;
#22624=DIRECTION ( 'NONE',  ( 0.05643417272666774454, -0.04100182651872442269, -0.9975640502598241977 ) ) ;
#22631=LINE ( 'NONE', #25776, #51449 ) ;
#22636=FACE_OUTER_BOUND ( 'NONE', #18854, .T. ) ;
#22642=CARTESIAN_POINT ( 'NONE',  ( 9.894687805641389389, -53.60726374558549878, -34.64999999999999858 ) ) ;
#22651=CARTESIAN_POINT ( 'NONE',  ( 2.404741263826560171, -25.85214510508460251, -35.14999999999999858 ) ) ;
#22654=CARTESIAN_POINT ( 'NONE',  ( 45.81506188687751546, 8.850597565810659262, -57.85721284573491374 ) ) ;
#22659=VERTEX_POINT ( 'NONE', #44799 ) ;
#22660=DIRECTION ( 'NONE',  ( 0.06889765579810419593, 0.01091231665325485996, -0.9975640502598241977 ) ) ;
#22663=AXIS2_PLACEMENT_3D ( 'NONE', #46830, #3049, #42104 ) ;
#22665=CIRCLE ( 'NONE', #40228, 2.999999999999994227 ) ;
#22667=ORIENTED_EDGE ( 'NONE', *, *, #29431, .T. ) ;
#22669=CARTESIAN_POINT ( 'NONE',  ( 45.14919548887390022, -33.29386571476810275, -35.12503119152809461 ) ) ;
#22670=EDGE_LOOP ( 'NONE', ( #47062, #15966, #39502, #31317 ) ) ;
#22678=EDGE_CURVE ( 'NONE', #7583, #47128, #5491, .T. ) ;
#22690=CARTESIAN_POINT ( 'NONE',  ( 45.46288062967357746, -40.06128974838797774, -59.56694921511265761 ) ) ;
#22692=VECTOR ( 'NONE', #28245, 1000.000000000000000 ) ;
#22699=DIRECTION ( 'NONE',  ( -0.5516667872527389882, -0.8340645993220436871, 8.326672684688667890E-17 ) ) ;
#22706=DIRECTION ( 'NONE',  ( 0.000000000000000000, 1.000000000000000000, 0.000000000000000000 ) ) ;
#22723=CARTESIAN_POINT ( 'NONE',  ( 22.13393739769619728, -54.15188668067469990, -35.14999999999999858 ) ) ;
#22732=CARTESIAN_POINT ( 'NONE',  ( -6.866062602303790285, -15.61618894467929941, -59.64999999999999147 ) ) ;
#22733=ORIENTED_EDGE ( 'NONE', *, *, #43387, .F. ) ;
#22734=CARTESIAN_POINT ( 'NONE',  ( 29.13393466042962032, -26.74790781212725221, -35.10904485683931142 ) ) ;
#22735=DIRECTION ( 'NONE',  ( 0.4999999999999998890, 0.8660254037844387076, 0.000000000000000000 ) ) ;
#22753=CARTESIAN_POINT ( 'NONE',  ( 8.787528872100399013, -49.03431820457670653, -34.71551406240349280 ) ) ;
#22754=CARTESIAN_POINT ( 'NONE',  ( 14.63393739769620083, -32.15793020853440254, -34.64999999999999858 ) ) ;
#22755=ADVANCED_FACE ( 'NONE', ( #17785 ), #33758, .T. ) ;
#22757=CARTESIAN_POINT ( 'NONE',  ( -18.31222503402669943, 3.035017555580589832, -50.71178994223060243 ) ) ;
#22766=ORIENTED_EDGE ( 'NONE', *, *, #17451, .F. ) ;
#22767=CARTESIAN_POINT ( 'NONE',  ( 47.23800599814349255, 8.041507069165529487, -54.67567028232367932 ) ) ;
#22782=LINE ( 'NONE', #6309, #13767 ) ;
#22783=FACE_OUTER_BOUND ( 'NONE', #18621, .T. ) ;
#22792=DIRECTION ( 'NONE',  ( 0.000000000000000000, 0.000000000000000000, -1.000000000000000000 ) ) ;
#22804=CARTESIAN_POINT ( 'NONE',  ( 46.77958021070534045, -38.22981356621252758, -56.42173487551926314 ) ) ;
#22805=ORIENTED_EDGE ( 'NONE', *, *, #24807, .T. ) ;
#22806=B_SPLINE_CURVE_WITH_KNOTS ( 'NONE', 3,
 ( #42585, #9832, #6681, #41794, #1966, #14281, #17943, #29979, #10616, #22642 ),
 .UNSPECIFIED., .F., .F.,
 ( 4, 2, 2, 2, 4 ),
 ( 0.1272047750358668849, 0.1420319546175010106, 0.1570382458081870103, 0.1723372614084489884, 0.1727139781544710095 ),
 .UNSPECIFIED. ) ;
#22808=DIRECTION ( 'NONE',  ( 0.000000000000000000, 1.000000000000000000, 0.000000000000000000 ) ) ;
#22814=CARTESIAN_POINT ( 'NONE',  ( -0.007164427059776000244, 14.47565373231149977, -34.77269723891829756 ) ) ;
#22815=DIRECTION ( 'NONE',  ( -1.000000000000000000, 0.000000000000000000, 0.000000000000000000 ) ) ;
#22816=DIRECTION ( 'NONE',  ( 0.8660254037844383745, -0.5000000000000003331, -2.775557561562891844E-16 ) ) ;
#22830=CARTESIAN_POINT ( 'NONE',  ( 14.13393739769619906, -45.61618894467940066, -62.64999999999999858 ) ) ;
#22835=DIRECTION ( 'NONE',  ( 1.882763000000000063E-17, 1.367908000000000040E-17, -1.000000000000000000 ) ) ;
#22845=CIRCLE ( 'NONE', #17851, 2.500000000000000000 ) ;
#22858=EDGE_LOOP ( 'NONE', ( #26855, #7795, #8307, #44017 ) ) ;
#22860=CARTESIAN_POINT ( 'NONE',  ( 42.72578186200144756, 6.504558357780759970, -76.69071525042791393 ) ) ;
#22864=VECTOR ( 'NONE', #608, 1000.000000000000114 ) ;
#22865=ADVANCED_FACE ( 'NONE', ( #18561 ), #11228, .T. ) ;
#22866=FACE_OUTER_BOUND ( 'NONE', #20390, .T. ) ;
#22871=ADVANCED_FACE ( 'NONE', ( #51318 ), #6517, .T. ) ;
#22876=B_SPLINE_CURVE_WITH_KNOTS ( 'NONE', 3,
 ( #39255, #47390, #48866, #31108 ),
 .UNSPECIFIED., .F., .F.,
 ( 4, 4 ),
 ( 0.000000000000000000, 1.000000000000000000 ),
 .UNSPECIFIED. ) ;
#22884=CARTESIAN_POINT ( 'NONE',  ( 3.987490788289478783, -8.603434725040944642, -34.79644660940672907 ) ) ;
#22889=CARTESIAN_POINT ( 'NONE',  ( 0.5469381754224795777, -4.307629671082502831, -43.67210485792230656 ) ) ;
#22896=LINE ( 'NONE', #42324, #25830 ) ;
#22905=DIRECTION ( 'NONE',  ( 0.6933752452815367118, 0.7071067811865475727, -0.1386750490563054827 ) ) ;
#22909=DIRECTION ( 'NONE',  ( 0.000000000000000000, -1.000000000000000000, 0.000000000000000000 ) ) ;
#22918=CARTESIAN_POINT ( 'NONE',  ( 0.1155611319282749960, -51.17475502668380472, -35.14999999933320396 ) ) ;
#22924=VERTEX_POINT ( 'NONE', #47900 ) ;
#22929=EDGE_CURVE ( 'NONE', #45896, #677, #31143, .T. ) ;
#22937=DIRECTION ( 'NONE',  ( -1.000000000000000000, 0.000000000000000000, 0.000000000000000000 ) ) ;
#22945=CARTESIAN_POINT ( 'NONE',  ( 44.36160194340284590, -39.98360157410301952, -64.90776822339829266 ) ) ;
#22946=AXIS2_PLACEMENT_3D ( 'NONE', #42533, #22584, #39115 ) ;
#22960=FACE_OUTER_BOUND ( 'NONE', #22670, .T. ) ;
#22962=CARTESIAN_POINT ( 'NONE',  ( 44.58553514073535951, -33.15021188507264327, -46.23822836818835924 ) ) ;
#22963=EDGE_CURVE ( 'NONE', #25181, #34982, #36334, .T. ) ;
#22965=LINE ( 'NONE', #10686, #46870 ) ;
#22966=CARTESIAN_POINT ( 'NONE',  ( 9.026390854479029002, -47.84168788784550230, -54.64999999999999858 ) ) ;
#22969=EDGE_CURVE ( 'NONE', #46894, #13682, #2780, .T. ) ;
#22971=ORIENTED_EDGE ( 'NONE', *, *, #18636, .F. ) ;
#22977=ORIENTED_EDGE ( 'NONE', *, *, #12683, .T. ) ;
#22987=ORIENTED_EDGE ( 'NONE', *, *, #22032, .F. ) ;
#22989=DIRECTION ( 'NONE',  ( 1.000000000000000000, 0.000000000000000000, 0.000000000000000000 ) ) ;
#22995=B_SPLINE_CURVE_WITH_KNOTS ( 'NONE', 3,
 ( #45446, #45961, #6128, #34137 ),
 .UNSPECIFIED., .F., .F.,
 ( 4, 4 ),
 ( 0.000000000000000000, 1.000000000000000000 ),
 .UNSPECIFIED. ) ;
#23002=VERTEX_POINT ( 'NONE', #32387 ) ;
#23009=CARTESIAN_POINT ( 'NONE',  ( 22.20417850065061671, 22.76024865223504889, -34.79644414665609986 ) ) ;
#23010=CARTESIAN_POINT ( 'NONE',  ( 8.943569970476740849, -49.33365190531349498, -34.64999999999999858 ) ) ;
#23013=CARTESIAN_POINT ( 'NONE',  ( 0.2715958990298489861, 19.60531400798089763, -34.53033264416539794 ) ) ;
#23014=DIRECTION ( 'NONE',  ( 0.000000000000000000, 0.000000000000000000, 1.000000000000000000 ) ) ;
#23021=ORIENTED_EDGE ( 'NONE', *, *, #28683, .F. ) ;
#23022=CARTESIAN_POINT ( 'NONE',  ( 45.37168861558401289, 7.906016184253609858, -63.92127268888761193 ) ) ;
#23029=DIRECTION ( 'NONE',  ( 0.000000000000000000, 0.000000000000000000, 1.000000000000000000 ) ) ;
#23041=DIRECTION ( 'NONE',  ( 0.000000000000000000, 0.000000000000000000, 1.000000000000000000 ) ) ;
#23042=AXIS2_PLACEMENT_3D ( 'NONE', #32729, #12086, #4208 ) ;
#23050=CARTESIAN_POINT ( 'NONE',  ( 18.63393739769619728, -45.61618894467940066, -34.64999999999999858 ) ) ;
#23057=DIRECTION ( 'NONE',  ( 0.000000000000000000, 0.000000000000000000, 1.000000000000000000 ) ) ;
#23058=EDGE_CURVE ( 'NONE', #27937, #13523, #13674, .T. ) ;
#23062=CARTESIAN_POINT ( 'NONE',  ( 46.76953110038879657, -38.22888952695009124, -56.47198051342422787 ) ) ;
#23065=LINE ( 'NONE', #39085, #26695 ) ;
#23078=VECTOR ( 'NONE', #6802, 1000.000000000000114 ) ;
#23094=CARTESIAN_POINT ( 'NONE',  ( -0.2043949983302396078, -45.45597504765002839, -34.94418884479945575 ) ) ;
#23104=VECTOR ( 'NONE', #45588, 1000.000000000000000 ) ;
#23109=ORIENTED_EDGE ( 'NONE', *, *, #50652, .T. ) ;
#23114=CARTESIAN_POINT ( 'NONE',  ( 0.6045892726184427524, -8.790618991491967904, -34.79644291222913921 ) ) ;
#23118=CARTESIAN_POINT ( 'NONE',  ( 44.73832203227348003, 6.778932900174915233, -66.62801705372713457 ) ) ;
#23121=ORIENTED_EDGE ( 'NONE', *, *, #49271, .F. ) ;
#23124=AXIS2_PLACEMENT_3D ( 'NONE', #38915, #34438, #3527 ) ;
#23151=LINE ( 'NONE', #47046, #43205 ) ;
#23152=EDGE_CURVE ( 'NONE', #5655, #48924, #33695, .T. ) ;
#23158=EDGE_LOOP ( 'NONE', ( #24888, #31940, #37570, #36481 ) ) ;
#23162=CARTESIAN_POINT ( 'NONE',  ( 45.39782597164072797, 8.824816061999294803, -59.88240093257450525 ) ) ;
#23170=DIRECTION ( 'NONE',  ( -0.01091231665325478710, 0.06889765579810418206, -0.9975640502598241977 ) ) ;
#23172=CARTESIAN_POINT ( 'NONE',  ( 44.07452568954059302, 1.883811055320659955, -54.64999999999999858 ) ) ;
#23177=EDGE_CURVE ( 'NONE', #4162, #39703, #10301, .T. ) ;
#23178=CARTESIAN_POINT ( 'NONE',  ( 2.558369240368420172, -25.18609768228349921, -34.64999999999999858 ) ) ;
#23179=ORIENTED_EDGE ( 'NONE', *, *, #30916, .T. ) ;
#23185=CARTESIAN_POINT ( 'NONE',  ( -3.839728563314020349, -6.393788602144800493, -54.64999999999999858 ) ) ;
#23190=ORIENTED_EDGE ( 'NONE', *, *, #37084, .F. ) ;
#23195=CARTESIAN_POINT ( 'NONE',  ( 45.18678546796069639, -40.04353233429138470, -60.90568228453756205 ) ) ;
#23215=CARTESIAN_POINT ( 'NONE',  ( 40.79482532997379707, 8.392676044869128660, -82.14319696191608955 ) ) ;
#23216=CARTESIAN_POINT ( 'NONE',  ( 14.43662147174979893, 1.104866772713560152, -34.68801049095919353 ) ) ;
#23217=CARTESIAN_POINT ( 'NONE',  ( -0.2067785137990631461, -10.69301208835099537, -34.94627313319775652 ) ) ;
#23219=CARTESIAN_POINT ( 'NONE',  ( 0.4644698840366340287, -22.39564254398910137, -34.95504743437659556 ) ) ;
#23222=CARTESIAN_POINT ( 'NONE',  ( -0.1437508118502728860, -22.76409625575194795, -34.89146800830128825 ) ) ;
#23226=CARTESIAN_POINT ( 'NONE',  ( 0.2019507440921958497, -26.68395609241781585, -34.66067286864802099 ) ) ;
#23242=DIRECTION ( 'NONE',  ( 0.000000000000000000, 0.000000000000000000, -1.000000000000000000 ) ) ;
#23253=EDGE_CURVE ( 'NONE', #19286, #46894, #49663, .T. ) ;
#23259=CARTESIAN_POINT ( 'NONE',  ( 0.1605025566177880891, 19.59002818087794040, -34.67617345845554411 ) ) ;
#23264=FACE_OUTER_BOUND ( 'NONE', #49056, .T. ) ;
#23269=EDGE_CURVE ( 'NONE', #43625, #41459, #4840, .T. ) ;
#23272=CARTESIAN_POINT ( 'NONE',  ( 47.77173862087886391, 6.796530529533522547, -51.39044986337782461 ) ) ;
#23273=CARTESIAN_POINT ( 'NONE',  ( 19.13393739769600188, 18.38381105532069881, -83.01107220193038927 ) ) ;
#23289=DIRECTION ( 'NONE',  ( -1.000000000000000000, -5.465567116091310088E-15, 0.000000000000000000 ) ) ;
#23312=EDGE_CURVE ( 'NONE', #19286, #26463, #22845, .T. ) ;
#23313=CARTESIAN_POINT ( 'NONE',  ( 47.13393739769622215, 7.715342668379952862, -54.35302931744276833 ) ) ;
#23319=CARTESIAN_POINT ( 'NONE',  ( 10.13393739769619906, -54.15188668067469990, -54.64999999999999858 ) ) ;
#23322=AXIS2_PLACEMENT_3D ( 'NONE', #14795, #10353, #6423 ) ;
#23324=CIRCLE ( 'NONE', #4079, 3.000000000000005773 ) ;
#23328=CARTESIAN_POINT ( 'NONE',  ( 31.06510394192407887, -35.76182709040440955, -84.62926581869410825 ) ) ;
#23330=DIRECTION ( 'NONE',  ( 0.000000000000000000, 0.000000000000000000, -1.000000000000000000 ) ) ;
#23333=( BOUNDED_CURVE ( )  B_SPLINE_CURVE ( 2, ( #51046, #42932, #33567 ),
 .UNSPECIFIED., .F., .T. ) 
 B_SPLINE_CURVE_WITH_KNOTS ( ( 3, 3 ),
 ( 0.1321855491534549842, 2.139356573199050260 ),
 .UNSPECIFIED. ) 
 CURVE ( )  GEOMETRIC_REPRESENTATION_ITEM ( )  RATIONAL_B_SPLINE_CURVE ( ( 1.001093714210619989, 1.008874108804550085, 1.000760730680250177 ) ) 
 REPRESENTATION_ITEM ( '' )  );
#23348=DIRECTION ( 'NONE',  ( -1.000000000000000000, 0.000000000000000000, 0.000000000000000000 ) ) ;
#23354=ORIENTED_EDGE ( 'NONE', *, *, #51371, .F. ) ;
#23356=LINE ( 'NONE', #38345, #45505 ) ;
#23357=CARTESIAN_POINT ( 'NONE',  ( 11.88511791769057346, -35.52924089863758184, -59.64999999999999147 ) ) ;
#23363=DIRECTION ( 'NONE',  ( 0.000000000000000000, 0.000000000000000000, -1.000000000000000000 ) ) ;
#23365=CARTESIAN_POINT ( 'NONE',  ( 44.72938784791404743, 6.777849755104416118, -66.67268761791444831 ) ) ;
#23380=ADVANCED_FACE ( 'NONE', ( #43337 ), #32717, .T. ) ;
#23386=VERTEX_POINT ( 'NONE', #11368 ) ;
#23390=CARTESIAN_POINT ( 'NONE',  ( 8.943569970476740849, -49.33365190531349498, -34.64999999999999858 ) ) ;
#23397=CARTESIAN_POINT ( 'NONE',  ( 17.58210831189408552, 18.38379234151610930, -83.19397497661219631 ) ) ;
#23404=CARTESIAN_POINT ( 'NONE',  ( 59.13393739769620083, 1.883811055320659955, -34.64999999999999858 ) ) ;
#23410=EDGE_CURVE ( 'NONE', #13264, #50203, #28396, .T. ) ;
#23413=CARTESIAN_POINT ( 'NONE',  ( 47.13393739769619373, 8.048130187719129580, -35.14999999999999858 ) ) ;
#23419=CARTESIAN_POINT ( 'NONE',  ( 45.98741248406297899, 8.860759954654445991, -57.01957150137892683 ) ) ;
#23421=VERTEX_POINT ( 'NONE', #27075 ) ;
#23423=ORIENTED_EDGE ( 'NONE', *, *, #28704, .F. ) ;
#23435=ORIENTED_EDGE ( 'NONE', *, *, #16186, .F. ) ;
#23438=AXIS2_PLACEMENT_3D ( 'NONE', #11719, #51291, #51797 ) ;
#23441=ADVANCED_FACE ( 'NONE', ( #15796 ), #16763, .T. ) ;
#23445=DIRECTION ( 'NONE',  ( 0.000000000000000000, 0.000000000000000000, -1.000000000000000000 ) ) ;
#23448=DIRECTION ( 'NONE',  ( 0.6933752452815368228, -0.7071067811865473507, -0.1386750490563055105 ) ) ;
#23451=CARTESIAN_POINT ( 'NONE',  ( 46.13897661844973186, -40.10140556276615342, -56.28420545448003054 ) ) ;
#23453=CARTESIAN_POINT ( 'NONE',  ( 22.29130106582129756, 22.56200410046560023, -34.67842804303189297 ) ) ;
#23454=CYLINDRICAL_SURFACE ( 'NONE', #48174, 0.4999999999999994449 ) ;
#23477=ORIENTED_EDGE ( 'NONE', *, *, #24976, .T. ) ;
#23481=DIRECTION ( 'NONE',  ( -0.9304380493636926763, 0.3664492274467048283, 0.000000000000000000 ) ) ;
#23485=VERTEX_POINT ( 'NONE', #40868 ) ;
#23487=CARTESIAN_POINT ( 'NONE',  ( -20.24088394071658570, -1.549377950793656034, -52.62430360528765050 ) ) ;
#23492=DIRECTION ( 'NONE',  ( 0.000000000000000000, -1.000000000000000000, 0.000000000000000000 ) ) ;
#23497=DIRECTION ( 'NONE',  ( 0.000000000000000000, 0.000000000000000000, 1.000000000000000000 ) ) ;
#23499=CARTESIAN_POINT ( 'NONE',  ( 30.13393739769619728, -38.61618894467930119, -84.65000000000000568 ) ) ;
#23508=VECTOR ( 'NONE', #27568, 1000.000000000000000 ) ;
#23511=AXIS2_PLACEMENT_3D ( 'NONE', #18101, #26467, #42482 ) ;
#23513=ORIENTED_EDGE ( 'NONE', *, *, #5080, .F. ) ;
#23517=CARTESIAN_POINT ( 'NONE',  ( 16.13393739769620083, -15.61618894467929941, -34.64999999999999858 ) ) ;
#23519=EDGE_CURVE ( 'NONE', #9584, #16231, #7300, .T. ) ;
#23526=CARTESIAN_POINT ( 'NONE',  ( 17.63393739769629676, -7.616188944679219475, -35.14999999999999858 ) ) ;
#23532=CARTESIAN_POINT ( 'NONE',  ( 47.10950441794090437, 6.750887858598658475, -54.70666253679335966 ) ) ;
#23547=FACE_OUTER_BOUND ( 'NONE', #12337, .T. ) ;
#23564=CARTESIAN_POINT ( 'NONE',  ( 4.820228898711410359, -36.82939238027569928, -59.64999999999999147 ) ) ;
#23573=CARTESIAN_POINT ( 'NONE',  ( 13.05521822061487214, -49.46974233527257780, -34.79644660940672907 ) ) ;
#23578=DIRECTION ( 'NONE',  ( 0.000000000000000000, 0.000000000000000000, -1.000000000000000000 ) ) ;
#23580=VECTOR ( 'NONE', #41550, 1000.000000000000000 ) ;
#23586=CARTESIAN_POINT ( 'NONE',  ( 44.07452568954059302, -33.11618894467940066, -54.64999999999999858 ) ) ;
#23591=VERTEX_POINT ( 'NONE', #33952 ) ;
#23602=ORIENTED_EDGE ( 'NONE', *, *, #11370, .F. ) ;
#23612=FACE_OUTER_BOUND ( 'NONE', #33997, .T. ) ;
#23623=CARTESIAN_POINT ( 'NONE',  ( 29.13393739769619728, -33.11618894467940066, -53.85091742636659973 ) ) ;
#23627=CARTESIAN_POINT ( 'NONE',  ( 44.80920505379729235, 6.787426711885585995, -66.27361051051437357 ) ) ;
#23646=ORIENTED_EDGE ( 'NONE', *, *, #48367, .F. ) ;
#23666=DIRECTION ( 'NONE',  ( 0.000000000000000000, 0.000000000000000000, -1.000000000000000000 ) ) ;
#23677=ORIENTED_EDGE ( 'NONE', *, *, #16521, .T. ) ;
#23680=EDGE_LOOP ( 'NONE', ( #48600, #10969, #45962, #17340 ) ) ;
#23693=EDGE_LOOP ( 'NONE', ( #51501, #45947, #10688, #4295 ) ) ;
#23695=ORIENTED_EDGE ( 'NONE', *, *, #26740, .T. ) ;
#23707=VERTEX_POINT ( 'NONE', #18758 ) ;
#23713=CARTESIAN_POINT ( 'NONE',  ( 44.07301638960753820, -39.96058317689758610, -66.30624784718879994 ) ) ;
#23720=AXIS2_PLACEMENT_3D ( 'NONE', #48845, #40967, #5084 ) ;
#23723=EDGE_LOOP ( 'NONE', ( #25547, #13839, #42216, #1861, #24700 ) ) ;
#23731=CARTESIAN_POINT ( 'NONE',  ( 41.50533919090486279, 8.477239747926573088, -78.71846675104687563 ) ) ;
#23736=CARTESIAN_POINT ( 'NONE',  ( 0.07087462514320330698, 19.88569008439129959, -34.96641315697679175 ) ) ;
#23737=EDGE_LOOP ( 'NONE', ( #17878, #26038, #38062, #9597 ) ) ;
#23742=CARTESIAN_POINT ( 'NONE',  ( 29.11900864776890074, -4.497910611074960485, -35.02873218748179340 ) ) ;
#23747=CARTESIAN_POINT ( 'NONE',  ( 23.24148394091319858, 16.60930999848680401, -54.64999999999999858 ) ) ;
#23748=DIRECTION ( 'NONE',  ( 0.8660254037844387076, 0.4999999999999998890, 2.775557561562889194E-17 ) ) ;
#23749=AXIS2_PLACEMENT_3D ( 'NONE', #49148, #37582, #40745 ) ;
#23764=AXIS2_PLACEMENT_3D ( 'NONE', #29202, #45213, #45728 ) ;
#23769=CARTESIAN_POINT ( 'NONE',  ( 17.63393739769639978, 10.88381105532070059, -34.64999999999999858 ) ) ;
#23771=CARTESIAN_POINT ( 'NONE',  ( -0.01592648613902455240, -22.81930388578409463, -34.78031642072629381 ) ) ;
#23782=CARTESIAN_POINT ( 'NONE',  ( 0.4937122138109050762, -8.827062753033800391, -34.90839531524139971 ) ) ;
#23783=CARTESIAN_POINT ( 'NONE',  ( 47.11197453701439741, -38.11534973524540248, -54.74201631774479182 ) ) ;
#23785=ORIENTED_EDGE ( 'NONE', *, *, #25127, .F. ) ;
#23788=CARTESIAN_POINT ( 'NONE',  ( 46.65361620740416981, 6.724962863903830801, -56.99320044726326984 ) ) ;
#23794=CARTESIAN_POINT ( 'NONE',  ( 26.13393739769619728, -28.89524513604070322, -39.64999999999999858 ) ) ;
#23804=LINE ( 'NONE', #43500, #1735 ) ;
#23806=CARTESIAN_POINT ( 'NONE',  ( 13.13393739769619906, -49.61618894467939356, -83.01107220193038927 ) ) ;
#23817=FACE_OUTER_BOUND ( 'NONE', #48130, .T. ) ;
#23819=CARTESIAN_POINT ( 'NONE',  ( 46.25525774125586054, 2.762490711761019568, -54.56299356781535437 ) ) ;
#23823=CARTESIAN_POINT ( 'NONE',  ( 47.13393739769619373, -38.26167638829240047, -54.64999999999999858 ) ) ;
#23841=CARTESIAN_POINT ( 'NONE',  ( 22.33082320214399985, 22.47179399159420043, -34.65604926186119172 ) ) ;
#23842=LINE ( 'NONE', #43035, #43999 ) ;
#23853=CARTESIAN_POINT ( 'NONE',  ( 13.05521822061467319, 18.23736444591386174, -34.79644660940673617 ) ) ;
#23855=EDGE_LOOP ( 'NONE', ( #36766, #47327, #15381, #47567 ) ) ;
#23874=ORIENTED_EDGE ( 'NONE', *, *, #29496, .F. ) ;
#23877=CARTESIAN_POINT ( 'NONE',  ( 29.13393739769620083, -29.55841766305462315, -42.42700139135359194 ) ) ;
#23907=CARTESIAN_POINT ( 'NONE',  ( -0.1295185695944109927, -31.87964491196989414, -84.65000000000000568 ) ) ;
#23912=CARTESIAN_POINT ( 'NONE',  ( 0.3209249304026040028, 15.01904124785189865, -34.64999999999999858 ) ) ;
#23914=AXIS2_PLACEMENT_3D ( 'NONE', #46977, #22310, #30434 ) ;
#23915=CARTESIAN_POINT ( 'NONE',  ( -0.007164427059776000244, -20.74946784552680157, -34.77269723891829756 ) ) ;
#23919=EDGE_CURVE ( 'NONE', #37366, #45283, #1951, .T. ) ;
#23924=CARTESIAN_POINT ( 'NONE',  ( 22.19151943370638591, -54.02136955896735770, -34.82441657595545337 ) ) ;
#23925=DIRECTION ( 'NONE',  ( 0.6933752452815368228, -0.7071067811865473507, -0.1386750490563055105 ) ) ;
#23928=EDGE_CURVE ( 'NONE', #8545, #29423, #49014, .T. ) ;
#23939=VERTEX_POINT ( 'NONE', #17656 ) ;
#23944=( BOUNDED_CURVE ( )  B_SPLINE_CURVE ( 2, ( #12567, #1283, #13103 ),
 .UNSPECIFIED., .F., .T. ) 
 B_SPLINE_CURVE_WITH_KNOTS ( ( 3, 3 ),
 ( 0.1321855492373369967, 2.139356573274270090 ),
 .UNSPECIFIED. ) 
 CURVE ( )  GEOMETRIC_REPRESENTATION_ITEM ( )  RATIONAL_B_SPLINE_CURVE ( ( 1.001093714235619991, 1.008874109002009911, 1.000760730696570011 ) ) 
 REPRESENTATION_ITEM ( '' )  );
#23957=VERTEX_POINT ( 'NONE', #22597 ) ;
#23961=CARTESIAN_POINT ( 'NONE',  ( 12.95491128060869990, -49.88685839599860117, -82.14319696191608955 ) ) ;
#23964=EDGE_CURVE ( 'NONE', #32183, #30264, #37935, .T. ) ;
#23965=CARTESIAN_POINT ( 'NONE',  ( 44.00576040509109532, -39.95514525231072156, -66.63177681307838895 ) ) ;
#23970=DIRECTION ( 'NONE',  ( 0.000000000000000000, 0.000000000000000000, -1.000000000000000000 ) ) ;
#23978=AXIS2_PLACEMENT_3D ( 'NONE', #48559, #5060, #17367 ) ;
#23980=CARTESIAN_POINT ( 'NONE',  ( -6.866062602303790285, -15.61618894467929941, 4.943674098299959851 ) ) ;
#23981=CARTESIAN_POINT ( 'NONE',  ( 41.13211650194840274, 8.433633102539264570, -80.51793142025734085 ) ) ;
#23982=CARTESIAN_POINT ( 'NONE',  ( 44.64648917221038715, -33.16028773000454066, -45.09461220786214142 ) ) ;
#23984=FACE_OUTER_BOUND ( 'NONE', #30087, .T. ) ;
#23991=ORIENTED_EDGE ( 'NONE', *, *, #21078, .F. ) ;
#23998=ORIENTED_EDGE ( 'NONE', *, *, #17509, .F. ) ;
#24001=CARTESIAN_POINT ( 'NONE',  ( 18.13393739769620083, -37.52509124488599923, -54.64999999999999858 ) ) ;
#24006=VERTEX_POINT ( 'NONE', #18677 ) ;
#24008=CARTESIAN_POINT ( 'NONE',  ( 8.643744238043749917, -48.75525398023999912, -35.14999999999999858 ) ) ;
#24016=CARTESIAN_POINT ( 'NONE',  ( 0.5964323607431272212, 0.7622463544159004956, 4.943674098299870145 ) ) ;
#24022=EDGE_CURVE ( 'NONE', #5342, #23957, #23356, .T. ) ;
#24030=CARTESIAN_POINT ( 'NONE',  ( 16.13393739769620083, -15.61618894467929941, -54.64999999999999858 ) ) ;
#24039=CARTESIAN_POINT ( 'NONE',  ( 40.94097710274119351, 6.580928486660690524, -85.72111169200137226 ) ) ;
#24060=ORIENTED_EDGE ( 'NONE', *, *, #4519, .T. ) ;
#24065=CARTESIAN_POINT ( 'NONE',  ( 23.55667557762257758, -48.88697541251522694, -34.82978046822304918 ) ) ;
#24071=CARTESIAN_POINT ( 'NONE',  ( 18.00872666787282839, -32.49681002921883533, -34.81767276520689336 ) ) ;
#24076=FACE_OUTER_BOUND ( 'NONE', #47845, .T. ) ;
#24081=CARTESIAN_POINT ( 'NONE',  ( 0.1457841021255935343, -8.319710351909083812, -34.68167779225149161 ) ) ;
#24091=CYLINDRICAL_SURFACE ( 'NONE', #49992, 0.4999999999999986677 ) ;
#24092=CARTESIAN_POINT ( 'NONE',  ( 61.00258867160625442, -28.71632116457892181, -42.47246584482020637 ) ) ;
#24099=CIRCLE ( 'NONE', #14939, 31.45861873485090143 ) ;
#24116=CARTESIAN_POINT ( 'NONE',  ( 2.464092196720385708, -25.62390951037214037, -34.77490583097451804 ) ) ;
#24120=ORIENTED_EDGE ( 'NONE', *, *, #49422, .T. ) ;
#24127=B_SPLINE_CURVE_WITH_KNOTS ( 'NONE', 3,
 ( #39100, #50113, #46717, #3193 ),
 .UNSPECIFIED., .F., .F.,
 ( 4, 4 ),
 ( 0.000000000000000000, 1.000000000000000000 ),
 .UNSPECIFIED. ) ;
#24130=CARTESIAN_POINT ( 'NONE',  ( 42.43208337334868929, 6.460128661955979013, -78.15925233081755152 ) ) ;
#24132=B_SPLINE_CURVE_WITH_KNOTS ( 'NONE', 3,
 ( #13266, #29222, #20575, #48378, #25284, #21355, #4349, #48913, #28443, #12220 ),
 .UNSPECIFIED., .F., .F.,
 ( 4, 2, 2, 2, 4 ),
 ( -0.1799215976184830035, -0.1795414484421369861, -0.1664059944892330167, -0.1383522341548960033, -0.1329710036333066059 ),
 .UNSPECIFIED. ) ;
#24134=CARTESIAN_POINT ( 'NONE',  ( 45.34397758664299971, 2.696163290909390220, -34.64999999999999858 ) ) ;
#24142=AXIS2_PLACEMENT_3D ( 'NONE', #17593, #48272, #8443 ) ;
#24151=VERTEX_POINT ( 'NONE', #12117 ) ;
#24162=CARTESIAN_POINT ( 'NONE',  ( 17.40001803049475981, 18.38378339404363970, -83.20618638369494136 ) ) ;
#24166=DIRECTION ( 'NONE',  ( 0.8660254037844387076, 0.4999999999999998890, 2.775557561562889194E-17 ) ) ;
#24172=EDGE_CURVE ( 'NONE', #29814, #29423, #3639, .T. ) ;
#24177=ORIENTED_EDGE ( 'NONE', *, *, #23253, .F. ) ;
#24178=FACE_OUTER_BOUND ( 'NONE', #41297, .T. ) ;
#24179=CARTESIAN_POINT ( 'NONE',  ( 22.13393739769589885, 22.91950879131610108, -35.14999999999999858 ) ) ;
#24182=AXIS2_PLACEMENT_3D ( 'NONE', #33858, #25215, #41220 ) ;
#24198=VERTEX_POINT ( 'NONE', #11867 ) ;
#24207=DIRECTION ( 'NONE',  ( 0.000000000000000000, 0.000000000000000000, -1.000000000000000000 ) ) ;
#24217=CARTESIAN_POINT ( 'NONE',  ( 42.61000615344636344, -39.82798686284615997, -73.38501703869289372 ) ) ;
#24219=B_SPLINE_CURVE_WITH_KNOTS ( 'NONE', 3,
 ( #10430, #14352, #1781, #2041, #41876, #42139, #2300, #41610 ),
 .UNSPECIFIED., .F., .F.,
 ( 4, 2, 2, 4 ),
 ( -0.1329710036334196266, -0.1164701438936319999, -0.09932952752696240506, -0.09339196852981200558 ),
 .UNSPECIFIED. ) ;
#24226=EDGE_LOOP ( 'NONE', ( #41813, #21372, #13004, #30749, #41023 ) ) ;
#24232=CARTESIAN_POINT ( 'NONE',  ( 17.98749448546710994, -32.47778390180250341, -34.79644291222910368 ) ) ;
#24233=DIRECTION ( 'NONE',  ( -1.451273000000000212E-17, 7.532081000000000189E-18, -1.000000000000000000 ) ) ;
#24234=CARTESIAN_POINT ( 'NONE',  ( 42.21481387295106913, 8.555122854874271709, -75.29414714603025516 ) ) ;
#24236=CARTESIAN_POINT ( 'NONE',  ( 30.26439304108700412, 4.386381194870886624, -84.60847545484261900 ) ) ;
#24241=ORIENTED_EDGE ( 'NONE', *, *, #48396, .T. ) ;
#24242=EDGE_LOOP ( 'NONE', ( #48860, #45248, #22733, #31286, #955, #23021 ) ) ;
#24244=AXIS2_PLACEMENT_3D ( 'NONE', #21313, #21054, #9548 ) ;
#24246=AXIS2_PLACEMENT_3D ( 'NONE', #39793, #11511, #31644 ) ;
#24251=ADVANCED_FACE ( 'NONE', ( #48269 ), #40399, .T. ) ;
#24252=ORIENTED_EDGE ( 'NONE', *, *, #19220, .T. ) ;
#24255=CARTESIAN_POINT ( 'NONE',  ( -0.05020173012252868855, 14.40722748145230980, -34.80983693937416490 ) ) ;
#24271=CARTESIAN_POINT ( 'NONE',  ( -3.779114556262074487, -11.36736946467367204, -59.64999999999999147 ) ) ;
#24288=AXIS2_PLACEMENT_3D ( 'NONE', #13790, #36850, #29747 ) ;
#24291=AXIS2_PLACEMENT_3D ( 'NONE', #14360, #41616, #29300 ) ;
#24293=CARTESIAN_POINT ( 'NONE',  ( 16.13393739769620083, -15.61618894467929941, -643.2998782751060389 ) ) ;
#24295=CARTESIAN_POINT ( 'NONE',  ( 46.13393739769619373, 4.883811055320659733, -81.65000000000000568 ) ) ;
#24311=ORIENTED_EDGE ( 'NONE', *, *, #620, .F. ) ;
#24328=ORIENTED_EDGE ( 'NONE', *, *, #13669, .F. ) ;
#24341=CARTESIAN_POINT ( 'NONE',  ( 12.93740664656274397, -49.25056949571164466, -34.64999999999999858 ) ) ;
#24346=ADVANCED_FACE ( 'NONE', ( #13597 ), #2814, .T. ) ;
#24359=AXIS2_PLACEMENT_3D ( 'NONE', #39884, #23348, #3729 ) ;
#24374=FACE_BOUND ( 'NONE', #10175, .T. ) ;
#24387=VERTEX_POINT ( 'NONE', #32965 ) ;
#24391=ORIENTED_EDGE ( 'NONE', *, *, #27594, .F. ) ;
#24394=CARTESIAN_POINT ( 'NONE',  ( 42.32037652162321706, 6.442361943507792787, -78.71780434772890089 ) ) ;
#24415=CARTESIAN_POINT ( 'NONE',  ( 23.53669455186048864, 17.69319178430572137, -34.79644561402099612 ) ) ;
#24418=CARTESIAN_POINT ( 'NONE',  ( 44.13393739769620083, -36.11618894467930119, -44.64999999999999858 ) ) ;
#24422=CARTESIAN_POINT ( 'NONE',  ( 17.55180121426148077, 18.38379139978320609, -83.19610070254232426 ) ) ;
#24433=DIRECTION ( 'NONE',  ( 0.000000000000000000, 0.000000000000000000, 1.000000000000000000 ) ) ;
#24435=ORIENTED_EDGE ( 'NONE', *, *, #28201, .T. ) ;
#24441=ORIENTED_EDGE ( 'NONE', *, *, #43882, .F. ) ;
#24445=ADVANCED_FACE ( 'NONE', ( #20923 ), #40477, .F. ) ;
#24450=EDGE_CURVE ( 'NONE', #41828, #43880, #17880, .T. ) ;
#24479=CARTESIAN_POINT ( 'NONE',  ( 42.34736991110049331, -39.80156373499493583, -74.65291150510742568 ) ) ;
#24485=AXIS2_PLACEMENT_3D ( 'NONE', #9827, #33394, #6154 ) ;
#24486=DIRECTION ( 'NONE',  ( -0.8090169943749478954, -0.5877852522924724710, 0.000000000000000000 ) ) ;
#24487=CARTESIAN_POINT ( 'NONE',  ( 18.13393739769630031, 1.391621760993470014, -35.14999999999999858 ) ) ;
#24496=CARTESIAN_POINT ( 'NONE',  ( 41.08545287463531537, 8.428089156136307381, -80.74272105195825588 ) ) ;
#24499=DIRECTION ( 'NONE',  ( 1.000000000000000000, 0.000000000000000000, 0.000000000000000000 ) ) ;
#24500=ORIENTED_EDGE ( 'NONE', *, *, #12374, .T. ) ;
#24503=VERTEX_POINT ( 'NONE', #29051 ) ;
#24506=CIRCLE ( 'NONE', #38771, 38.99999999999998579 ) ;
#24511=EDGE_LOOP ( 'NONE', ( #21890, #30905, #33428, #35787, #15586 ) ) ;
#24515=CARTESIAN_POINT ( 'NONE',  ( -15.39330862682666101, 7.341020780706740467, -48.46231058698690219 ) ) ;
#24516=CARTESIAN_POINT ( 'NONE',  ( 14.42149519498352106, 18.38378315315731371, -83.17357193473726795 ) ) ;
#24525=ADVANCED_FACE ( 'NONE', ( #15144 ), #3098, .T. ) ;
#24527=CARTESIAN_POINT ( 'NONE',  ( -0.4410626023037880206, -3.737207156102679839, -35.14999999999999858 ) ) ;
#24528=CIRCLE ( 'NONE', #1968, 6.999999999999999112 ) ;
#24533=CARTESIAN_POINT ( 'NONE',  ( 11.63393739769619906, -41.61618894467930119, -35.14999999999999858 ) ) ;
#24539=B_SPLINE_CURVE_WITH_KNOTS ( 'NONE', 3,
 ( #15721, #24065, #5, #18873, #3936, #7349, #19649, #7610 ),
 .UNSPECIFIED., .F., .F.,
 ( 4, 2, 2, 4 ),
 ( 0.05031563485841133304, 0.06814349192364040075, 0.08666255477330790657, 0.09307761161196949351 ),
 .UNSPECIFIED. ) ;
#24541=AXIS2_PLACEMENT_3D ( 'NONE', #2289, #42389, #2031 ) ;
#24549=CARTESIAN_POINT ( 'NONE',  ( 0.4371248283888460318, -8.845792823550640449, -35.02873218748179340 ) ) ;
#24566=TOROIDAL_SURFACE ( 'NONE', #12910, 34.47562460986249988, 0.5000000000000000000 ) ;
#24575=VERTEX_POINT ( 'NONE', #5987 ) ;
#24577=FACE_OUTER_BOUND ( 'NONE', #35611, .T. ) ;
#24587=CARTESIAN_POINT ( 'NONE',  ( 10.07635536168570489, 22.78899166960868072, -34.82441657595547468 ) ) ;
#24596=CARTESIAN_POINT ( 'NONE',  ( 46.63393739769619373, -15.61618894467929941, -35.14999999999999858 ) ) ;
#24608=CARTESIAN_POINT ( 'NONE',  ( 16.97276188636960015, -43.80059717415329601, -59.64999999999999147 ) ) ;
#24634=FACE_OUTER_BOUND ( 'NONE', #28070, .T. ) ;
#24639=CARTESIAN_POINT ( 'NONE',  ( 12.95491128060869990, -49.88685839599860117, -82.14319696191608955 ) ) ;
#24641=DIRECTION ( 'NONE',  ( 0.000000000000000000, 0.7071067811865475727, 0.7071067811865475727 ) ) ;
#24642=EDGE_CURVE ( 'NONE', #27249, #7182, #15658, .T. ) ;
#24645=ORIENTED_EDGE ( 'NONE', *, *, #21391, .F. ) ;
#24650=FACE_OUTER_BOUND ( 'NONE', #31334, .T. ) ;
#24655=LINE ( 'NONE', #40407, #9141 ) ;
#24659=CARTESIAN_POINT ( 'NONE',  ( 45.15345886371729733, 2.073553906859470164, -35.03944707979399453 ) ) ;
#24661=CARTESIAN_POINT ( 'NONE',  ( 42.99085965337582138, -37.77634669025830050, -75.36538833490237721 ) ) ;
#24673=EDGE_CURVE ( 'NONE', #37859, #31098, #28717, .T. ) ;
#24679=VERTEX_POINT ( 'NONE', #23747 ) ;
#24682=CARTESIAN_POINT ( 'NONE',  ( 16.13393739769620083, -15.61618894467929941, -35.14999999999999858 ) ) ;
#24684=CARTESIAN_POINT ( 'NONE',  ( 16.13393739769620083, -29.47259540523039689, -47.64999999999999858 ) ) ;
#24686=DIRECTION ( 'NONE',  ( -0.000000000000000000, 1.000000000000000000, 0.000000000000000000 ) ) ;
#24695=VERTEX_POINT ( 'NONE', #16424 ) ;
#24700=ORIENTED_EDGE ( 'NONE', *, *, #7637, .T. ) ;
#24701=EDGE_CURVE ( 'NONE', #8526, #37113, #27944, .T. ) ;
#24705=EDGE_CURVE ( 'NONE', #11240, #35016, #30406, .T. ) ;
#24714=VECTOR ( 'NONE', #33454, 1000.000000000000000 ) ;
#24719=LINE ( 'NONE', #47135, #12078 ) ;
#24722=ORIENTED_EDGE ( 'NONE', *, *, #45697, .F. ) ;
#24724=CARTESIAN_POINT ( 'NONE',  ( 0.1457840918200039859, -10.50670027737364620, -34.68167776469301344 ) ) ;
#24730=DIRECTION ( 'NONE',  ( -1.000000000000000000, 0.000000000000000000, 0.000000000000000000 ) ) ;
#24738=EDGE_CURVE ( 'NONE', #32778, #32833, #29581, .T. ) ;
#24743=CARTESIAN_POINT ( 'NONE',  ( 42.75619885378542051, -39.84230250343536284, -72.67917449632909666 ) ) ;
#24745=AXIS2_PLACEMENT_3D ( 'NONE', #18582, #23014, #39036 ) ;
#24751=CARTESIAN_POINT ( 'NONE',  ( 14.53139780415550142, -32.25138633525569531, -34.65800258959610147 ) ) ;
#24761=CARTESIAN_POINT ( 'NONE',  ( 40.91633283741396809, 8.407571910465815535, -81.55800397143316616 ) ) ;
#24767=VERTEX_POINT ( 'NONE', #44723 ) ;
#24768=VERTEX_POINT ( 'NONE', #44464 ) ;
#24769=ADVANCED_FACE ( 'NONE', ( #8570 ), #21375, .T. ) ;
#24779=CARTESIAN_POINT ( 'NONE',  ( -10.06254952539740799, 13.27891273067756828, -43.88582999887075431 ) ) ;
#24780=CARTESIAN_POINT ( 'NONE',  ( 14.58828788332387383, 18.38379252020285648, -83.18681078541726492 ) ) ;
#24783=DIRECTION ( 'NONE',  ( -1.224646799147353207E-16, 1.000000000000000000, 0.000000000000000000 ) ) ;
#24797=CARTESIAN_POINT ( 'NONE',  ( 4.133937397696209715, -22.54439217495480108, -35.14999999999999858 ) ) ;
#24799=CARTESIAN_POINT ( 'NONE',  ( 16.13393739769620083, -15.61618894467929941, -54.64999999999999858 ) ) ;
#24803=ADVANCED_FACE ( 'NONE', ( #9357 ), #16956, .T. ) ;
#24807=EDGE_CURVE ( 'NONE', #50655, #46482, #21198, .T. ) ;
#24814=CARTESIAN_POINT ( 'NONE',  ( 0.5522155295079101966, -8.807798953772319805, -34.84133294386911928 ) ) ;
#24823=CIRCLE ( 'NONE', #36543, 2.999999999999999112 ) ;
#24850=CARTESIAN_POINT ( 'NONE',  ( 10.09871813756530123, 22.83973475445539947, -34.88336916441300417 ) ) ;
#24851=ORIENTED_EDGE ( 'NONE', *, *, #21261, .F. ) ;
#24852=CARTESIAN_POINT ( 'NONE',  ( 23.13393739769620083, -28.89524513604070322, -62.14999999999999858 ) ) ;
#24868=CARTESIAN_POINT ( 'NONE',  ( 28.67375133668729958, -4.663717383496379654, -34.65024193067809222 ) ) ;
#24869=CARTESIAN_POINT ( 'NONE',  ( 16.13393739769639623, 7.383811055320659733, 4.943674098299959851 ) ) ;
#24872=CARTESIAN_POINT ( 'NONE',  ( 16.13393739769620083, -15.61618894467929941, -34.64999999999999858 ) ) ;
#24873=CARTESIAN_POINT ( 'NONE',  ( 43.09923138757430650, -39.96440645322047658, -70.65236649871883401 ) ) ;
#24888=ORIENTED_EDGE ( 'NONE', *, *, #14542, .F. ) ;
#24896=CARTESIAN_POINT ( 'NONE',  ( 46.89857864678853616, 7.968436783889276676, -34.72191413131643145 ) ) ;
#24898=AXIS2_PLACEMENT_3D ( 'NONE', #17560, #25911, #9695 ) ;
#24906=ORIENTED_EDGE ( 'NONE', *, *, #1070, .T. ) ;
#24913=CARTESIAN_POINT ( 'NONE',  ( 42.65279859904871529, 6.493598508889044219, -77.05562690612859456 ) ) ;
#24919=CARTESIAN_POINT ( 'NONE',  ( 42.28978442694865691, -37.66980104272789731, -78.87076310448497907 ) ) ;
#24921=EDGE_CURVE ( 'NONE', #51503, #29628, #17076, .T. ) ;
#24928=DIRECTION ( 'NONE',  ( 0.000000000000000000, 0.000000000000000000, 1.000000000000000000 ) ) ;
#24935=CARTESIAN_POINT ( 'NONE',  ( 45.14919548887390022, 2.061487825409429764, -35.12503119152809461 ) ) ;
#24937=DIRECTION ( 'NONE',  ( 0.000000000000000000, 0.000000000000000000, 1.000000000000000000 ) ) ;
#24938=ORIENTED_EDGE ( 'NONE', *, *, #38639, .T. ) ;
#24941=CARTESIAN_POINT ( 'NONE',  ( 22.13393739769589885, 22.91950879131610108, -35.14999999999999858 ) ) ;
#24951=DIRECTION ( 'NONE',  ( 0.000000000000000000, -1.000000000000000000, 0.000000000000000000 ) ) ;
#24958=DIRECTION ( 'NONE',  ( -1.000000000000000000, 0.000000000000000000, 0.000000000000000000 ) ) ;
#24971=CARTESIAN_POINT ( 'NONE',  ( -20.36606260230379917, -15.61618894467949836, -69.65000000000000568 ) ) ;
#24976=EDGE_CURVE ( 'NONE', #11158, #15142, #44222, .T. ) ;
#24988=CARTESIAN_POINT ( 'NONE',  ( 45.42616726031420882, 2.762490711761018236, -58.70844597252361297 ) ) ;
#24992=ORIENTED_EDGE ( 'NONE', *, *, #37996, .T. ) ;
#24996=EDGE_CURVE ( 'NONE', #7027, #35178, #32933, .T. ) ;
#25002=AXIS2_PLACEMENT_3D ( 'NONE', #44332, #37253, #40402 ) ;
#25006=CARTESIAN_POINT ( 'NONE',  ( 14.58123197128150039, -32.20606442350140242, -34.65032322548079691 ) ) ;
#25017=CARTESIAN_POINT ( 'NONE',  ( 45.00717534271083053, 8.798628770718870840, -61.77800503858115633 ) ) ;
#25030=CARTESIAN_POINT ( 'NONE',  ( 23.08073416742070094, -9.873403152104399894, -35.14999999999999858 ) ) ;
#25031=EDGE_LOOP ( 'NONE', ( #19114, #28225 ) ) ;
#25049=CARTESIAN_POINT ( 'NONE',  ( 8.711199217769639347, 17.65459752315663877, -34.82978046822305629 ) ) ;
#25068=DIRECTION ( 'NONE',  ( 0.000000000000000000, 1.000000000000000000, 0.000000000000000000 ) ) ;
#25071=CARTESIAN_POINT ( 'NONE',  ( 16.13393739769620083, -38.61618894467930119, -62.64999999999999858 ) ) ;
#25082=DIRECTION ( 'NONE',  ( -1.224646799147353207E-16, 1.000000000000000000, 0.000000000000000000 ) ) ;
#25114=LINE ( 'NONE', #50023, #42927 ) ;
#25121=VECTOR ( 'NONE', #39195, 1000.000000000000000 ) ;
#25127=EDGE_CURVE ( 'NONE', #12629, #50723, #8071, .T. ) ;
#25137=DIRECTION ( 'NONE',  ( -0.8090169943749471182, 0.5877852522924732481, 0.000000000000000000 ) ) ;
#25139=CARTESIAN_POINT ( 'NONE',  ( 14.13393739769630031, 1.391621760993509982, -35.14999999999999858 ) ) ;
#25140=CARTESIAN_POINT ( 'NONE',  ( 29.35282966121437553, -35.71037171799162735, -84.62344484690784441 ) ) ;
#25155=VERTEX_POINT ( 'NONE', #2504 ) ;
#25171=VERTEX_POINT ( 'NONE', #39446 ) ;
#25172=ORIENTED_EDGE ( 'NONE', *, *, #36175, .F. ) ;
#25181=VERTEX_POINT ( 'NONE', #11153 ) ;
#25182=CARTESIAN_POINT ( 'NONE',  ( 14.63393739769630031, 0.9255523191757060175, -34.64999999999999858 ) ) ;
#25188=CARTESIAN_POINT ( 'NONE',  ( 42.29796674348754948, -37.67109563684581985, -78.82985224857310413 ) ) ;
#25189=ORIENTED_EDGE ( 'NONE', *, *, #48803, .F. ) ;
#25192=ADVANCED_FACE ( 'NONE', ( #38933 ), #16839, .T. ) ;
#25195=EDGE_CURVE ( 'NONE', #7027, #9837, #43379, .T. ) ;
#25197=DIRECTION ( 'NONE',  ( -1.000000000000000000, 0.000000000000000000, 0.000000000000000000 ) ) ;
#25212=CARTESIAN_POINT ( 'NONE',  ( 17.98749078828947745, -41.76263555408611694, -34.79644660940672907 ) ) ;
#25215=DIRECTION ( 'NONE',  ( 0.000000000000000000, -1.000000000000000000, 0.000000000000000000 ) ) ;
#25219=ADVANCED_FACE ( 'NONE', ( #7476 ), #937, .F. ) ;
#25223=ORIENTED_EDGE ( 'NONE', *, *, #2851, .T. ) ;
#25224=LINE ( 'NONE', #33353, #12919 ) ;
#25227=CARTESIAN_POINT ( 'NONE',  ( 33.38393739769599478, 10.53025766472752522, -34.79644660940672907 ) ) ;
#25238=EDGE_CURVE ( 'NONE', #39742, #50075, #14329, .T. ) ;
#25239=AXIS2_PLACEMENT_3D ( 'NONE', #12221, #44186, #19565 ) ;
#25242=ORIENTED_EDGE ( 'NONE', *, *, #20221, .F. ) ;
#25247=ORIENTED_EDGE ( 'NONE', *, *, #35323, .F. ) ;
#25250=CARTESIAN_POINT ( 'NONE',  ( 11.73137203405248385, 10.53025766472752522, -34.79644660940672907 ) ) ;
#25254=CARTESIAN_POINT ( 'NONE',  ( 47.13393739769619373, 4.883811055320659733, -54.64999999999999858 ) ) ;
#25264=CARTESIAN_POINT ( 'NONE',  ( 46.82538613462318722, -34.56499699448699658, -54.61944740401202125 ) ) ;
#25269=CARTESIAN_POINT ( 'NONE',  ( 14.63393739769640156, 10.88381105532070059, -34.64999999999999858 ) ) ;
#25274=EDGE_CURVE ( 'NONE', #35178, #18174, #6963, .T. ) ;
#25276=DIRECTION ( 'NONE',  ( 1.000000000000000000, 0.000000000000000000, 0.000000000000000000 ) ) ;
#25277=EDGE_CURVE ( 'NONE', #12905, #41446, #20159, .T. ) ;
#25284=CARTESIAN_POINT ( 'NONE',  ( 23.37006864188870026, 18.01372606128889942, -34.65445009297679491 ) ) ;
#25286=CARTESIAN_POINT ( 'NONE',  ( 45.24585991142964048, 8.815101637006968360, -60.61901997089581329 ) ) ;
#25288=DIRECTION ( 'NONE',  ( -0.3863301728269175062, -0.9223605572462019175, 3.330669073875470114E-16 ) ) ;
#25290=VERTEX_POINT ( 'NONE', #19776 ) ;
#25292=ORIENTED_EDGE ( 'NONE', *, *, #17794, .F. ) ;
#25298=ORIENTED_EDGE ( 'NONE', *, *, #8877, .T. ) ;
#25304=DIRECTION ( 'NONE',  ( 0.000000000000000000, 0.000000000000000000, 1.000000000000000000 ) ) ;
#25309=DIRECTION ( 'NONE',  ( 0.000000000000000000, 0.7071067811865463515, -0.7071067811865487940 ) ) ;
#25323=ORIENTED_EDGE ( 'NONE', *, *, #51511, .T. ) ;
#25325=AXIS2_PLACEMENT_3D ( 'NONE', #46669, #50331, #26455 ) ;
#25331=LINE ( 'NONE', #4654, #25580 ) ;
#25333=CARTESIAN_POINT ( 'NONE',  ( 4.133937397696209715, -22.54439217495480108, -47.64999999999999858 ) ) ;
#25337=CARTESIAN_POINT ( 'NONE',  ( 20.63393739769620083, -41.61618894467930119, -54.64999999999999858 ) ) ;
#25339=ORIENTED_EDGE ( 'NONE', *, *, #4107, .T. ) ;
#25340=AXIS2_PLACEMENT_3D ( 'NONE', #16681, #28988, #33172 ) ;
#25352=CARTESIAN_POINT ( 'NONE',  ( 44.13393739769620083, -33.11618894467930829, -54.27132075603720551 ) ) ;
#25353=ORIENTED_EDGE ( 'NONE', *, *, #22572, .F. ) ;
#25358=CARTESIAN_POINT ( 'NONE',  ( -11.39236625349550103, 2.585530954890270294, -54.64999999999999858 ) ) ;
#25363=CARTESIAN_POINT ( 'NONE',  ( -22.72534110410520114, -11.79254667875349938, -54.70989275527219320 ) ) ;
#25368=DIRECTION ( 'NONE',  ( 0.5516667872527449834, -0.8340645993220396903, -3.885780586188043947E-16 ) ) ;
#25386=DIRECTION ( 'NONE',  ( 0.8660254037844384856, -0.5000000000000003331, -2.775557561562892337E-16 ) ) ;
#25387=ORIENTED_EDGE ( 'NONE', *, *, #6371, .F. ) ;
#25396=CARTESIAN_POINT ( 'NONE',  ( 47.17883912218999853, -39.34270251064258161, -54.71052591825291245 ) ) ;
#25401=ORIENTED_EDGE ( 'NONE', *, *, #14274, .T. ) ;
#25403=ORIENTED_EDGE ( 'NONE', *, *, #37018, .T. ) ;
#25415=AXIS2_PLACEMENT_3D ( 'NONE', #49795, #42189, #34563 ) ;
#25422=DIRECTION ( 'NONE',  ( 0.000000000000000000, 0.000000000000000000, 1.000000000000000000 ) ) ;
#25427=VERTEX_POINT ( 'NONE', #16608 ) ;
#25436=ORIENTED_EDGE ( 'NONE', *, *, #9593, .F. ) ;
#25437=DIRECTION ( 'NONE',  ( 1.000000000000000000, 0.000000000000000000, 0.000000000000000000 ) ) ;
#25438=DIRECTION ( 'NONE',  ( -1.000000000000000000, 0.000000000000000000, 0.000000000000000000 ) ) ;
#25441=AXIS2_PLACEMENT_3D ( 'NONE', #22611, #38627, #34666 ) ;
#25443=CARTESIAN_POINT ( 'NONE',  ( 41.94238982860078835, -37.61441522663087511, -80.60767011578155916 ) ) ;
#25445=ORIENTED_EDGE ( 'NONE', *, *, #39873, .F. ) ;
#25453=CARTESIAN_POINT ( 'NONE',  ( -9.953010648345507860, -19.86500842468492323, -59.64999999999999147 ) ) ;
#25455=ORIENTED_EDGE ( 'NONE', *, *, #38498, .T. ) ;
#25466=CARTESIAN_POINT ( 'NONE',  ( 22.20417850065061671, 22.76024865223504889, -34.79644414665609986 ) ) ;
#25470=EDGE_CURVE ( 'NONE', #36729, #36007, #11607, .T. ) ;
#25483=CARTESIAN_POINT ( 'NONE',  ( 14.13393739769619906, -31.61618894467930474, -34.64999999999999858 ) ) ;
#25490=ORIENTED_EDGE ( 'NONE', *, *, #47734, .F. ) ;
#25501=CARTESIAN_POINT ( 'NONE',  ( 45.95394279055306441, 6.916571454256072116, -60.54993553558288255 ) ) ;
#25502=ORIENTED_EDGE ( 'NONE', *, *, #33851, .F. ) ;
#25513=DIRECTION ( 'NONE',  ( 1.000000000000000000, 0.000000000000000000, 0.000000000000000000 ) ) ;
#25519=VECTOR ( 'NONE', #22937, 1000.000000000000000 ) ;
#25527=DIRECTION ( 'NONE',  ( 1.000000000000000000, 0.000000000000000000, 0.000000000000000000 ) ) ;
#25534=FACE_OUTER_BOUND ( 'NONE', #20328, .T. ) ;
#25541=DIRECTION ( 'NONE',  ( -1.000000000000000000, 0.000000000000000000, 0.000000000000000000 ) ) ;
#25543=CARTESIAN_POINT ( 'NONE',  ( 43.97715045787865762, 8.720472785296667695, -66.77010945423391775 ) ) ;
#25547=ORIENTED_EDGE ( 'NONE', *, *, #40612, .F. ) ;
#25551=ORIENTED_EDGE ( 'NONE', *, *, #10432, .T. ) ;
#25553=DIRECTION ( 'NONE',  ( 1.000000000000000000, 0.000000000000000000, 0.000000000000000000 ) ) ;
#25554=AXIS2_PLACEMENT_3D ( 'NONE', #6736, #51525, #47598 ) ;
#25561=CARTESIAN_POINT ( 'NONE',  ( 16.13393739769620083, -15.61618894467929941, -35.14999999999999858 ) ) ;
#25576=CIRCLE ( 'NONE', #20558, 0.4934525379635912867 ) ;
#25577=CARTESIAN_POINT ( 'NONE',  ( 47.08272461591150204, 8.115112359209708970, -53.89515469992119989 ) ) ;
#25580=VECTOR ( 'NONE', #17492, 999.9999999999998863 ) ;
#25584=CARTESIAN_POINT ( 'NONE',  ( 46.98749078828947034, -36.11618894467930119, -34.79644660940672907 ) ) ;
#25586=DIRECTION ( 'NONE',  ( 0.8660254037844380415, -0.5000000000000012212, -2.498001805406606160E-16 ) ) ;
#25592=ORIENTED_EDGE ( 'NONE', *, *, #627, .F. ) ;
#25604=DIRECTION ( 'NONE',  ( 0.000000000000000000, 0.000000000000000000, -1.000000000000000000 ) ) ;
#25610=DIRECTION ( 'NONE',  ( 0.000000000000000000, -1.000000000000000000, 0.000000000000000000 ) ) ;
#25616=CARTESIAN_POINT ( 'NONE',  ( -13.76961861560299916, -41.00297359184299495, -46.76611145355789745 ) ) ;
#25617=AXIS2_PLACEMENT_3D ( 'NONE', #41759, #3489, #43065 ) ;
#25629=DIRECTION ( 'NONE',  ( -0.8660254037844379305, 0.5000000000000011102, -1.387778780781449373E-16 ) ) ;
#25631=EDGE_CURVE ( 'NONE', #47003, #10013, #50337, .T. ) ;
#25635=ORIENTED_EDGE ( 'NONE', *, *, #33157, .F. ) ;
#25639=( BOUNDED_CURVE ( )  B_SPLINE_CURVE ( 3, ( #18617, #50600, #26728, #5800 ),
 .UNSPECIFIED., .F., .T. ) 
 B_SPLINE_CURVE_WITH_KNOTS ( ( 4, 4 ),
 ( 4.712388980384694115, 5.070260775219138871 ),
 .UNSPECIFIED. ) 
 CURVE ( )  GEOMETRIC_REPRESENTATION_ITEM ( )  RATIONAL_B_SPLINE_CURVE ( ( 1.000000000000000000, 0.9893557610490356646, 0.9893557610490356646, 1.000000000000000000 ) ) 
 REPRESENTATION_ITEM ( '' )  );
#25651=CARTESIAN_POINT ( 'NONE',  ( 17.72982031756377808, -49.61616882370213943, -83.18296600389349749 ) ) ;
#25654=LINE ( 'NONE', #40623, #39478 ) ;
#25656=CARTESIAN_POINT ( 'NONE',  ( 47.18678629383617107, -39.34334098796522738, -54.67089428642063353 ) ) ;
#25668=CARTESIAN_POINT ( 'NONE',  ( 28.81656660489900190, -26.62211590400339745, -34.68308842254609914 ) ) ;
#25670=CARTESIAN_POINT ( 'NONE',  ( 47.13393739769619373, 4.883811055320659733, -54.64999999999999858 ) ) ;
#25690=CARTESIAN_POINT ( 'NONE',  ( 33.13393739769620083, -38.61618894467930119, -84.65000000000000568 ) ) ;
#25694=ORIENTED_EDGE ( 'NONE', *, *, #33968, .F. ) ;
#25696=DIRECTION ( 'NONE',  ( 0.000000000000000000, -1.000000000000000000, 0.000000000000000000 ) ) ;
#25701=CARTESIAN_POINT ( 'NONE',  ( 45.63740510567983932, -38.11460057359725795, -62.13264583676811981 ) ) ;
#25710=LINE ( 'NONE', #6342, #20590 ) ;
#25716=CARTESIAN_POINT ( 'NONE',  ( 46.63499162694400724, -39.11122816143360126, -34.64999999999999858 ) ) ;
#25733=VECTOR ( 'NONE', #7518, 1000.000000000000000 ) ;
#25737=CARTESIAN_POINT ( 'NONE',  ( -11.36606260230380094, -15.61618894467929941, -54.64999999999999858 ) ) ;
#25751=CARTESIAN_POINT ( 'NONE',  ( 9.124990099443129665, -48.86424491586210195, -35.14566363178129649 ) ) ;
#25753=CARTESIAN_POINT ( 'NONE',  ( 45.42810023600526392, 6.859503157004126273, -63.17912806148366656 ) ) ;
#25765=CARTESIAN_POINT ( 'NONE',  ( 14.14886614762370165, 1.362847559348080217, -35.02873218748179340 ) ) ;
#25776=CARTESIAN_POINT ( 'NONE',  ( 25.72499013618932651, -0.9180541517691319653, -34.79644660940672907 ) ) ;
#25792=ORIENTED_EDGE ( 'NONE', *, *, #24450, .T. ) ;
#25798=CARTESIAN_POINT ( 'NONE',  ( 44.67293909344935798, 8.774802390190076906, -63.39842665425204871 ) ) ;
#25800=ADVANCED_FACE ( 'NONE', ( #38413 ), #50212, .F. ) ;
#25805=EDGE_LOOP ( 'NONE', ( #2835, #6245, #40385, #10829 ) ) ;
#25807=CARTESIAN_POINT ( 'NONE',  ( -22.75970726311355108, -18.37500023713087671, -54.70196997798354488 ) ) ;
#25830=VECTOR ( 'NONE', #38129, 1000.000000000000000 ) ;
#25833=ORIENTED_EDGE ( 'NONE', *, *, #30670, .T. ) ;
#25836=EDGE_CURVE ( 'NONE', #8281, #45496, #5930, .T. ) ;
#25837=DIRECTION ( 'NONE',  ( 0.000000000000000000, 0.000000000000000000, -1.000000000000000000 ) ) ;
#25857=CARTESIAN_POINT ( 'NONE',  ( 0.5774960717374452157, -22.43288435223359656, -34.81767276520686494 ) ) ;
#25862=ORIENTED_EDGE ( 'NONE', *, *, #30093, .T. ) ;
#25871=AXIS2_PLACEMENT_3D ( 'NONE', #17955, #38923, #30772 ) ;
#25874=CARTESIAN_POINT ( 'NONE',  ( -1.431265392021220162, -50.53043258612900246, -36.47998747206590053 ) ) ;
#25876=AXIS2_PLACEMENT_3D ( 'NONE', #414, #19303, #28441 ) ;
#25882=VERTEX_POINT ( 'NONE', #18748 ) ;
#25893=ORIENTED_EDGE ( 'NONE', *, *, #4979, .T. ) ;
#25900=DIRECTION ( 'NONE',  ( 0.8660254037844390407, -0.4999999999999995004, 0.000000000000000000 ) ) ;
#25905=CARTESIAN_POINT ( 'NONE',  ( 29.10811623682189975, -4.501937149316799669, -34.99013415954829753 ) ) ;
#25906=VECTOR ( 'NONE', #2729, 1000.000000000000000 ) ;
#25910=CARTESIAN_POINT ( 'NONE',  ( -15.83221208767410282, 6.858269193346590242, -48.53302639233909588 ) ) ;
#25911=DIRECTION ( 'NONE',  ( 0.000000000000000000, 0.000000000000000000, 1.000000000000000000 ) ) ;
#25912=CARTESIAN_POINT ( 'NONE',  ( 46.38067733160732331, -40.25943396676748876, -54.53019052586303417 ) ) ;
#25918=VERTEX_POINT ( 'NONE', #35515 ) ;
#25919=CARTESIAN_POINT ( 'NONE',  ( 44.05838509154141036, 8.810486217098942419, -66.03926413344439084 ) ) ;
#25923=CARTESIAN_POINT ( 'NONE',  ( 28.71032976354209865, -26.58237652039480281, -34.65450330891889763 ) ) ;
#25944=ORIENTED_EDGE ( 'NONE', *, *, #26854, .T. ) ;
#25945=CARTESIAN_POINT ( 'NONE',  ( 10.13393739769589885, 22.91950879131600161, -34.64999999999999858 ) ) ;
#25953=CARTESIAN_POINT ( 'NONE',  ( 44.07452568954059302, 1.883811055320659955, -54.64999999999999858 ) ) ;
#25958=EDGE_CURVE ( 'NONE', #11224, #29423, #49515, .T. ) ;
#25963=CARTESIAN_POINT ( 'NONE',  ( 44.35481541144333306, -37.96333356703264883, -68.54560956798736981 ) ) ;
#25964=ADVANCED_FACE ( 'NONE', ( #47580 ), #27385, .T. ) ;
#25979=CARTESIAN_POINT ( 'NONE',  ( 41.87382049790848271, -39.75083843982427112, -76.94057980257345264 ) ) ;
#25994=DIRECTION ( 'NONE',  ( 0.000000000000000000, -1.000000000000000000, 0.000000000000000000 ) ) ;
#26009=ORIENTED_EDGE ( 'NONE', *, *, #24921, .F. ) ;
#26013=ORIENTED_EDGE ( 'NONE', *, *, #48371, .T. ) ;
#26019=CARTESIAN_POINT ( 'NONE',  ( 46.47824713337531932, 6.969044071021170517, -57.92844982156870515 ) ) ;
#26020=VERTEX_POINT ( 'NONE', #31049 ) ;
#26026=FACE_OUTER_BOUND ( 'NONE', #825, .T. ) ;
#26028=CARTESIAN_POINT ( 'NONE',  ( 13.63393739769599833, 14.38381105532070059, -34.64999999999999858 ) ) ;
#26034=LINE ( 'NONE', #38638, #25906 ) ;
#26038=ORIENTED_EDGE ( 'NONE', *, *, #845, .F. ) ;
#26049=DIRECTION ( 'NONE',  ( -0.7071067811865511255, -0.7071067811865440200, 0.000000000000000000 ) ) ;
#26052=CARTESIAN_POINT ( 'NONE',  ( 26.13393739769619728, -2.337132753317950229, -39.64999999999999858 ) ) ;
#26063=CARTESIAN_POINT ( 'NONE',  ( 29.13393739769619728, -33.11618894467940066, -34.64999999999999858 ) ) ;
#26066=CARTESIAN_POINT ( 'NONE',  ( 44.29800273259771615, 8.746227658329765120, -65.21609057545674659 ) ) ;
#26072=ORIENTED_EDGE ( 'NONE', *, *, #35822, .F. ) ;
#26078=ORIENTED_EDGE ( 'NONE', *, *, #41164, .F. ) ;
#26081=CARTESIAN_POINT ( 'NONE',  ( 28.13393739769619728, -8.687985714403843929, -35.01561944896766221 ) ) ;
#26083=CARTESIAN_POINT ( 'NONE',  ( -6.866062602303790285, -15.61618894467929941, -59.64999999999999147 ) ) ;
#26099=FACE_OUTER_BOUND ( 'NONE', #47654, .T. ) ;
#26109=CARTESIAN_POINT ( 'NONE',  ( 17.20688454841970128, 14.56395709402249850, -35.14999999999999858 ) ) ;
#26118=SPHERICAL_SURFACE ( 'NONE', #24541, 0.5000000000000000000 ) ;
#26120=CARTESIAN_POINT ( 'NONE',  ( 47.04404845359650267, 8.017726918288019533, -34.85732842610089932 ) ) ;
#26137=ORIENTED_EDGE ( 'NONE', *, *, #29900, .F. ) ;
#26139=CARTESIAN_POINT ( 'NONE',  ( -22.46120355510790034, -21.45481835963710182, -54.31569267914190391 ) ) ;
#26164=ORIENTED_EDGE ( 'NONE', *, *, #38268, .F. ) ;
#26174=CARTESIAN_POINT ( 'NONE',  ( -9.374724833670061486, 14.33830887257789932, -43.22289157268509996 ) ) ;
#26176=CARTESIAN_POINT ( 'NONE',  ( 40.88670949972279089, -39.06981162304028032, -85.10457558764954911 ) ) ;
#26178=PLANE ( 'NONE',  #25415 ) ;
#26181=ADVANCED_FACE ( 'NONE', ( #14742 ), #22587, .T. ) ;
#26183=ORIENTED_EDGE ( 'NONE', *, *, #7969, .F. ) ;
#26184=CARTESIAN_POINT ( 'NONE',  ( 47.22257521636639410, 8.040674068322497092, -54.75197889428296349 ) ) ;
#26193=DIRECTION ( 'NONE',  ( -1.000000000000000000, 0.000000000000000000, 0.000000000000000000 ) ) ;
#26194=EDGE_LOOP ( 'NONE', ( #8388, #20729, #6499, #1770 ) ) ;
#26209=ORIENTED_EDGE ( 'NONE', *, *, #3266, .F. ) ;
#26217=DIRECTION ( 'NONE',  ( 0.000000000000000000, 1.000000000000000000, 0.000000000000000000 ) ) ;
#26218=DIRECTION ( 'NONE',  ( -0.8660254037844387076, -0.4999999999999998890, 1.110223024625155678E-16 ) ) ;
#26222=CARTESIAN_POINT ( 'NONE',  ( 45.83898684223488829, -38.13670450189240313, -61.12474413365445969 ) ) ;
#26223=B_SPLINE_CURVE_WITH_KNOTS ( 'NONE', 3,
 ( #28524, #32962, #490, #44261, #16226, #241 ),
 .UNSPECIFIED., .F., .F.,
 ( 4, 2, 4 ),
 ( -0.1400863131347609980, -0.1374219544292619999, -0.1219760492225880066 ),
 .UNSPECIFIED. ) ;
#26231=CIRCLE ( 'NONE', #30419, 39.00000000000001421 ) ;
#26243=CARTESIAN_POINT ( 'NONE',  ( 41.53258628612942971, -39.71279169438616918, -78.58678531550816615 ) ) ;
#26273=AXIS2_PLACEMENT_3D ( 'NONE', #39007, #7548, #44664 ) ;
#26276=VERTEX_POINT ( 'NONE', #26518 ) ;
#26284=CARTESIAN_POINT ( 'NONE',  ( 0.1155610841158959956, 19.94237700917059897, -35.14999985728680088 ) ) ;
#26292=FACE_OUTER_BOUND ( 'NONE', #5669, .T. ) ;
#26299=VERTEX_POINT ( 'NONE', #35693 ) ;
#26305=CARTESIAN_POINT ( 'NONE',  ( 16.13393739769620083, -15.61618894467929941, -69.65000000000000568 ) ) ;
#26315=CIRCLE ( 'NONE', #18805, 2.999999999999998224 ) ;
#26316=DIRECTION ( 'NONE',  ( 0.000000000000000000, 0.000000000000000000, -1.000000000000000000 ) ) ;
#26319=LINE ( 'NONE', #45481, #45724 ) ;
#26326=FACE_OUTER_BOUND ( 'NONE', #19773, .T. ) ;
#26328=CARTESIAN_POINT ( 'NONE',  ( 45.95638572195198179, 8.859046655822801597, -57.17003146777447142 ) ) ;
#26331=ORIENTED_EDGE ( 'NONE', *, *, #28953, .T. ) ;
#26334=CARTESIAN_POINT ( 'NONE',  ( -22.65176864815480329, -19.69794255023575857, -54.65770472193846530 ) ) ;
#26347=EDGE_CURVE ( 'NONE', #44397, #27321, #11336, .T. ) ;
#26357=CARTESIAN_POINT ( 'NONE',  ( 44.47540486623933020, -39.99256076608075716, -64.35539580940769611 ) ) ;
#26373=CARTESIAN_POINT ( 'NONE',  ( 16.13393739769620083, -15.61618894467929941, 36.77166666666649775 ) ) ;
#26374=CARTESIAN_POINT ( 'NONE',  ( 44.13393739769620083, 1.883811055320659955, -54.27132075603810080 ) ) ;
#26382=VERTEX_POINT ( 'NONE', #12353 ) ;
#26383=DIRECTION ( 'NONE',  ( 0.000000000000000000, 0.000000000000000000, 1.000000000000000000 ) ) ;
#26392=ORIENTED_EDGE ( 'NONE', *, *, #28864, .F. ) ;
#26393=CARTESIAN_POINT ( 'NONE',  ( -22.86606125915950116, -18.55922616655630009, -54.87897021767069106 ) ) ;
#26401=ORIENTED_EDGE ( 'NONE', *, *, #4383, .F. ) ;
#26416=EDGE_CURVE ( 'NONE', #51495, #32888, #39479, .T. ) ;
#26427=CARTESIAN_POINT ( 'NONE',  ( 29.06532888865359965, -4.517767789041739590, -34.89721277419619838 ) ) ;
#26431=CARTESIAN_POINT ( 'NONE',  ( 0.3560139052572889873, 20.05003001002749841, -34.85296064851209508 ) ) ;
#26433=CARTESIAN_POINT ( 'NONE',  ( 41.43972917658179256, -38.75047512967100971, -83.14010518295869190 ) ) ;
#26436=EDGE_CURVE ( 'NONE', #48656, #43880, #48156, .T. ) ;
#26441=CARTESIAN_POINT ( 'NONE',  ( 43.11186292497671246, 8.718372030718779087, -70.65452844614090111 ) ) ;
#26452=EDGE_LOOP ( 'NONE', ( #44454, #38415, #5707, #49060, #11982 ) ) ;
#26455=DIRECTION ( 'NONE',  ( 0.7071067811865475727, 0.000000000000000000, 0.7071067811865475727 ) ) ;
#26458=CARTESIAN_POINT ( 'NONE',  ( -0.4410626023037880206, -27.49517073325580085, -35.14999999999999858 ) ) ;
#26463=VERTEX_POINT ( 'NONE', #27554 ) ;
#26467=DIRECTION ( 'NONE',  ( 0.000000000000000000, -1.000000000000000000, 0.000000000000000000 ) ) ;
#26481=CARTESIAN_POINT ( 'NONE',  ( 45.10181048658294145, -38.05446154858772445, -64.81063413519126470 ) ) ;
#26483=CARTESIAN_POINT ( 'NONE',  ( 47.13393649688870113, -39.28050833195659663, -53.76790015415899404 ) ) ;
#26500=CARTESIAN_POINT ( 'NONE',  ( 41.51070890355069309, -39.71021112747065729, -78.69265187567246755 ) ) ;
#26516=FACE_OUTER_BOUND ( 'NONE', #34598, .T. ) ;
#26518=CARTESIAN_POINT ( 'NONE',  ( 20.13393739769620083, -28.89524513604070322, -84.65000000000000568 ) ) ;
#26527=ORIENTED_EDGE ( 'NONE', *, *, #23410, .T. ) ;
#26529=VERTEX_POINT ( 'NONE', #13373 ) ;
#26536=EDGE_CURVE ( 'NONE', #40950, #41446, #27759, .T. ) ;
#26538=ORIENTED_EDGE ( 'NONE', *, *, #22249, .F. ) ;
#26540=CARTESIAN_POINT ( 'NONE',  ( 45.66610078067787981, 6.885504573898759695, -61.98917487139547688 ) ) ;
#26544=FACE_OUTER_BOUND ( 'NONE', #30979, .T. ) ;
#26546=CARTESIAN_POINT ( 'NONE',  ( 0.000000000000000000, 0.000000000000000000, 0.000000000000000000 ) ) ;
#26548=DIRECTION ( 'NONE',  ( 0.000000000000000000, 0.000000000000000000, -1.000000000000000000 ) ) ;
#26558=ORIENTED_EDGE ( 'NONE', *, *, #26608, .F. ) ;
#26562=DIRECTION ( 'NONE',  ( 0.3863301728269261659, 0.9223605572461982538, 0.000000000000000000 ) ) ;
#26563=DIRECTION ( 'NONE',  ( 0.000000000000000000, 0.000000000000000000, 1.000000000000000000 ) ) ;
#26583=CARTESIAN_POINT ( 'NONE',  ( 16.13393739769620083, -30.04994567442000175, -34.64999999999999858 ) ) ;
#26585=CARTESIAN_POINT ( 'NONE',  ( 10.06369629473941352, -53.99262654158863484, -34.79644414665150975 ) ) ;
#26589=EDGE_LOOP ( 'NONE', ( #45115, #29769, #40069 ) ) ;
#26594=FACE_OUTER_BOUND ( 'NONE', #23158, .T. ) ;
#26608=EDGE_CURVE ( 'NONE', #40328, #51786, #48754, .T. ) ;
#26614=CARTESIAN_POINT ( 'NONE',  ( 27.13393739769620083, -38.61618894467930119, -72.14999999999999147 ) ) ;
#26617=ORIENTED_EDGE ( 'NONE', *, *, #50464, .T. ) ;
#26621=CARTESIAN_POINT ( 'NONE',  ( 46.12376833368420392, -40.10057103694796155, -56.35806153124856621 ) ) ;
#26623=CIRCLE ( 'NONE', #10761, 151.6440921975380434 ) ;
#26644=EDGE_CURVE ( 'NONE', #12924, #37859, #46968, .T. ) ;
#26653=LINE ( 'NONE', #31101, #47718 ) ;
#26676=ORIENTED_EDGE ( 'NONE', *, *, #13964, .F. ) ;
#26683=CARTESIAN_POINT ( 'NONE',  ( 38.67452568954060155, -33.11618894467940066, -81.65000000000000568 ) ) ;
#26687=CARTESIAN_POINT ( 'NONE',  ( 47.13264866673830511, -38.11667935645279925, -54.63852466879949787 ) ) ;
#26692=VERTEX_POINT ( 'NONE', #46125 ) ;
#26694=ORIENTED_EDGE ( 'NONE', *, *, #10663, .T. ) ;
#26695=VECTOR ( 'NONE', #3177, 1000.000000000000000 ) ;
#26696=CARTESIAN_POINT ( 'NONE',  ( 40.57483056633861196, 8.377405199161493954, -83.15256529792165452 ) ) ;
#26699=CARTESIAN_POINT ( 'NONE',  ( 46.98749101202549383, -39.23094825485602399, -34.79644638567071269 ) ) ;
#26708=AXIS2_PLACEMENT_3D ( 'NONE', #43045, #43303, #19438 ) ;
#26718=CARTESIAN_POINT ( 'NONE',  ( 16.13393739769620083, -29.47259540523039689, -35.14999999999999858 ) ) ;
#26723=DIRECTION ( 'NONE',  ( 0.000000000000000000, -1.000000000000000000, 0.000000000000000000 ) ) ;
#26728=CARTESIAN_POINT ( 'NONE',  ( 0.2019507440921954611, -8.287282526050189446, -34.66067286864802099 ) ) ;
#26733=CARTESIAN_POINT ( 'NONE',  ( 44.09915591415798275, 1.883883970182539835, -54.64999999999999858 ) ) ;
#26738=CARTESIAN_POINT ( 'NONE',  ( 46.93999483510361870, -38.24462483669982049, -55.61966498947037252 ) ) ;
#26740=EDGE_CURVE ( 'NONE', #7036, #1146, #1564, .T. ) ;
#26742=AXIS2_PLACEMENT_3D ( 'NONE', #4145, #15953, #36115 ) ;
#26744=CARTESIAN_POINT ( 'NONE',  ( -22.79130321220790378, -13.38297325766516011, -54.71749000676463481 ) ) ;
#26752=FACE_OUTER_BOUND ( 'NONE', #20572, .T. ) ;
#26776=AXIS2_PLACEMENT_3D ( 'NONE', #8833, #24783, #40792 ) ;
#26779=AXIS2_PLACEMENT_3D ( 'NONE', #20541, #19785, #48610 ) ;
#26780=CARTESIAN_POINT ( 'NONE',  ( 40.00893739769619373, -16.26570799751769769, -35.14999999999999858 ) ) ;
#26786=VECTOR ( 'NONE', #33571, 1000.000000000000000 ) ;
#26791=ORIENTED_EDGE ( 'NONE', *, *, #7799, .F. ) ;
#26799=CARTESIAN_POINT ( 'NONE',  ( 31.13393739769620083, -36.11618894467930119, -81.65000000000000568 ) ) ;
#26800=CARTESIAN_POINT ( 'NONE',  ( 42.76911844754650360, -36.11618894467930119, -61.17703620997009750 ) ) ;
#26803=CARTESIAN_POINT ( 'NONE',  ( 43.77342226960121252, 6.654908062603587915, -71.45256550439793841 ) ) ;
#26810=AXIS2_PLACEMENT_3D ( 'NONE', #3374, #7562, #18823 ) ;
#26816=VECTOR ( 'NONE', #40472, 1000.000000000000114 ) ;
#26821=CIRCLE ( 'NONE', #3386, 3.000000000000001776 ) ;
#26838=CYLINDRICAL_SURFACE ( 'NONE', #23322, 0.4999999999999982236 ) ;
#26854=EDGE_CURVE ( 'NONE', #36140, #50419, #27465, .T. ) ;
#26855=ORIENTED_EDGE ( 'NONE', *, *, #45563, .T. ) ;
#26870=LINE ( 'NONE', #6973, #38398 ) ;
#26873=B_SPLINE_CURVE_WITH_KNOTS ( 'NONE', 3,
 ( #170, #11466, #15388, #8556, #15899, #8288, #16407, #39497, #11978, #15644, #24236, #20070, #31598, #36063, #32364, #7783, #48383, #44189 ),
 .UNSPECIFIED., .F., .F.,
 ( 4, 2, 2, 2, 2, 2, 2, 2, 4 ),
 ( 0.000000000000000000, 0.1250000000000077993, 0.1875000000000098532, 0.2500000000000119349, 0.3750000000000123790, 0.4375000000000107692, 0.4687500000000119349, 0.5000000000000131006, 1.000000000000000000 ),
 .UNSPECIFIED. ) ;
#26884=EDGE_CURVE ( 'NONE', #21889, #13277, #13161, .T. ) ;
#26888=CARTESIAN_POINT ( 'NONE',  ( 45.81018332226489065, -40.08279255246922190, -57.88043798612723378 ) ) ;
#26891=AXIS2_PLACEMENT_3D ( 'NONE', #51753, #19006, #3810 ) ;
#26906=PLANE ( 'NONE',  #17733 ) ;
#26908=CARTESIAN_POINT ( 'NONE',  ( 44.30395658100767520, -33.11967951199632409, -51.34838756301716955 ) ) ;
#26921=AXIS2_PLACEMENT_3D ( 'NONE', #24799, #4909, #36878 ) ;
#26932=ORIENTED_EDGE ( 'NONE', *, *, #51511, .F. ) ;
#26934=VECTOR ( 'NONE', #38987, 1000.000000000000000 ) ;
#26935=CARTESIAN_POINT ( 'NONE',  ( 47.13393739769619373, -36.11618894467930119, -54.64999999999999858 ) ) ;
#26942=CYLINDRICAL_SURFACE ( 'NONE', #9228, 3.000000000000000444 ) ;
#26947=CARTESIAN_POINT ( 'NONE',  ( 47.08181966212730174, -39.34878172615530190, -53.90061828279809930 ) ) ;
#26957=CARTESIAN_POINT ( 'NONE',  ( -0.2606685752331820427, 19.44500263626499859, -34.99215748765989531 ) ) ;
#26959=CARTESIAN_POINT ( 'NONE',  ( 45.52271482667700297, -37.98968692785550161, -62.69526427244640132 ) ) ;
#26966=AXIS2_PLACEMENT_3D ( 'NONE', #37945, #2298, #10687 ) ;
#26980=B_SPLINE_CURVE_WITH_KNOTS ( 'NONE', 3,
 ( #48323, #20777, #1137, #19311, #44389, #36767, #23217, #12949, #35292, #48069, #8490, #7266 ),
 .UNSPECIFIED., .F., .F.,
 ( 4, 1, 2, 2, 1, 2, 4 ),
 ( 0.000000000000000000, 0.2500000000000280886, 0.3750000000000361933, 0.4062500000000416334, 0.4375000000000470735, 0.5000000000000446310, 1.000000000000000000 ),
 .UNSPECIFIED. ) ;
#26981=VERTEX_POINT ( 'NONE', #48694 ) ;
#26990=ORIENTED_EDGE ( 'NONE', *, *, #40051, .T. ) ;
#27006=CARTESIAN_POINT ( 'NONE',  ( 46.24251708701347496, -38.17788423405144727, -59.10706492824460412 ) ) ;
#27015=LINE ( 'NONE', #31185, #6961 ) ;
#27018=CYLINDRICAL_SURFACE ( 'NONE', #33182, 2.999999999999999112 ) ;
#27028=ORIENTED_EDGE ( 'NONE', *, *, #18404, .F. ) ;
#27040=FACE_OUTER_BOUND ( 'NONE', #16445, .T. ) ;
#27041=CARTESIAN_POINT ( 'NONE',  ( -0.2905447780693382609, -45.37728495500358861, -35.01965454424513524 ) ) ;
#27043=CARTESIAN_POINT ( 'NONE',  ( 47.13393739769619373, -38.26167638829240047, -54.64999999999999858 ) ) ;
#27053=CARTESIAN_POINT ( 'NONE',  ( 16.13393739769620083, -45.61618894467940066, -62.64999999999999858 ) ) ;
#27063=CARTESIAN_POINT ( 'NONE',  ( -8.923813801541088608, 7.426280886100511403, -42.52630539064124093 ) ) ;
#27064=CARTESIAN_POINT ( 'NONE',  ( 43.00594420470828538, 6.546349551758413376, -75.28996588853145511 ) ) ;
#27066=VERTEX_POINT ( 'NONE', #14785 ) ;
#27071=( NAMED_UNIT ( * ) SI_UNIT ( $, .STERADIAN. ) SOLID_ANGLE_UNIT ( ) );
#27075=CARTESIAN_POINT ( 'NONE',  ( 46.47536507427530239, -40.11920440292289669, -54.64999999999999858 ) ) ;
#27081=AXIS2_PLACEMENT_3D ( 'NONE', #41239, #5351, #21305 ) ;
#27113=CARTESIAN_POINT ( 'NONE',  ( 45.41100509400894936, 8.825660103508100818, -59.81845664609551250 ) ) ;
#27116=ORIENTED_EDGE ( 'NONE', *, *, #6563, .T. ) ;
#27124=DIRECTION ( 'NONE',  ( -0.3502816565540429750, 0.000000000000000000, 0.9366444154970205993 ) ) ;
#27125=ADVANCED_FACE ( 'NONE', ( #42839 ), #29018, .T. ) ;
#27127=CARTESIAN_POINT ( 'NONE',  ( 19.31296351478369999, -49.88685839599860117, -82.14319696191608955 ) ) ;
#27130=DIRECTION ( 'NONE',  ( 0.7071067811865475727, 0.000000000000000000, 0.7071067811865475727 ) ) ;
#27137=DIRECTION ( 'NONE',  ( 0.000000000000000000, 1.000000000000000000, 0.000000000000000000 ) ) ;
#27140=CARTESIAN_POINT ( 'NONE',  ( 0.6614253361915112261, -22.46035056599116686, -34.75586992539663100 ) ) ;
#27148=CARTESIAN_POINT ( 'NONE',  ( 45.06052948167663175, -40.03471377011139509, -61.51912326202059234 ) ) ;
#27167=ORIENTED_EDGE ( 'NONE', *, *, #49145, .T. ) ;
#27168=CARTESIAN_POINT ( 'NONE',  ( -0.2865249686165991516, -22.78714623532964723, -35.01561944896766931 ) ) ;
#27178=EDGE_CURVE ( 'NONE', #9877, #32504, #3314, .T. ) ;
#27181=EDGE_CURVE ( 'NONE', #3105, #37975, #16453, .T. ) ;
#27187=DIRECTION ( 'NONE',  ( -1.000000000000000000, 0.000000000000000000, 0.000000000000000000 ) ) ;
#27189=CARTESIAN_POINT ( 'NONE',  ( 13.13393739769600010, 18.38381105532060289, -34.64999999999999858 ) ) ;
#27201=ORIENTED_EDGE ( 'NONE', *, *, #7158, .T. ) ;
#27202=CIRCLE ( 'NONE', #30560, 17.09468304687048956 ) ;
#27220=CARTESIAN_POINT ( 'NONE',  ( 46.31133434054406450, 7.971624601050109504, -59.28131743592275171 ) ) ;
#27235=CARTESIAN_POINT ( 'NONE',  ( -0.007164427059776000244, -4.186223695871990280, -34.77269723891829756 ) ) ;
#27241=EDGE_CURVE ( 'NONE', #18727, #50035, #11384, .T. ) ;
#27243=B_SPLINE_CURVE_WITH_KNOTS ( 'NONE', 3,
 ( #45261, #25049, #33183, #21636, #9368, #37391, #17476, #37135 ),
 .UNSPECIFIED., .F., .F.,
 ( 4, 2, 2, 4 ),
 ( 0.05031563485850510525, 0.06814349192389300425, 0.08666255477376220984, 0.09307761161249389348 ),
 .UNSPECIFIED. ) ;
#27247=EDGE_CURVE ( 'NONE', #40660, #32504, #32494, .T. ) ;
#27248=CARTESIAN_POINT ( 'NONE',  ( 0.6045892726184427524, -8.790618991491967904, -34.79644291222913921 ) ) ;
#27249=VERTEX_POINT ( 'NONE', #15567 ) ;
#27259=EDGE_LOOP ( 'NONE', ( #15280, #37936, #36145, #10765, #42140 ) ) ;
#27268=CIRCLE ( 'NONE', #50698, 33.97624844042369574 ) ;
#27281=CARTESIAN_POINT ( 'NONE',  ( 31.79224979287389985, -36.11618894467930119, -84.65000000000000568 ) ) ;
#27282=CARTESIAN_POINT ( 'NONE',  ( 16.13393739769620083, -45.61618894467940066, -35.14999999999999858 ) ) ;
#27294=CARTESIAN_POINT ( 'NONE',  ( 16.13393739769620083, -38.61618894467930119, 4.943674098299959851 ) ) ;
#27295=CARTESIAN_POINT ( 'NONE',  ( 13.13393739769596102, 18.38381105532059934, -35.01561944896766221 ) ) ;
#27296=COLOUR_RGB ( '', 0.31764706, 0.68627451, 0.89019608) ;
#27307=CIRCLE ( 'NONE', #4713, 1.999999999999998224 ) ;
#27316=ORIENTED_EDGE ( 'NONE', *, *, #43651, .T. ) ;
#27318=CARTESIAN_POINT ( 'NONE',  ( 42.74343314659522264, 6.507180287579836353, -76.60246204020066330 ) ) ;
#27321=VERTEX_POINT ( 'NONE', #39927 ) ;
#27331=CARTESIAN_POINT ( 'NONE',  ( -0.3016046179078940015, -20.31737465961040101, -35.02873218748179340 ) ) ;
#27334=EDGE_CURVE ( 'NONE', #23591, #25918, #19226, .T. ) ;
#27346=DIRECTION ( 'NONE',  ( 0.5516667872527503125, 0.8340645993220362486, 0.000000000000000000 ) ) ;
#27356=CARTESIAN_POINT ( 'NONE',  ( 44.11147024075970080, -33.11640768660669920, -54.64999999999999858 ) ) ;
#27362=ORIENTED_EDGE ( 'NONE', *, *, #8933, .T. ) ;
#27366=CARTESIAN_POINT ( 'NONE',  ( 46.11276164393227361, 8.867600659815479958, -56.41146322270898139 ) ) ;
#27368=EDGE_LOOP ( 'NONE', ( #18071, #12612, #29112, #45051, #34053 ) ) ;
#27372=VECTOR ( 'NONE', #13299, 1000.000000000000000 ) ;
#27380=ADVANCED_FACE ( 'NONE', ( #31773 ), #3517, .T. ) ;
#27383=CARTESIAN_POINT ( 'NONE',  ( 18.13393739769620083, -41.61618894467930119, -35.14999999999999858 ) ) ;
#27385=PLANE ( 'NONE',  #26891 ) ;
#27398=ORIENTED_EDGE ( 'NONE', *, *, #28958, .F. ) ;
#27402=CARTESIAN_POINT ( 'NONE',  ( 45.77359740143206324, -40.08047819383660482, -58.05860318629369488 ) ) ;
#27425=ORIENTED_EDGE ( 'NONE', *, *, #13626, .T. ) ;
#27428=EDGE_LOOP ( 'NONE', ( #737, #9905, #35029, #25944, #44337 ) ) ;
#27437=CARTESIAN_POINT ( 'NONE',  ( -22.60067283610179700, -11.07416626356550005, -54.64998264227110525 ) ) ;
#27445=LINE ( 'NONE', #39009, #15758 ) ;
#27465=LINE ( 'NONE', #39538, #32328 ) ;
#27472=CARTESIAN_POINT ( 'NONE',  ( 43.68604305009880306, -37.81292632501880036, -71.88615322025499665 ) ) ;
#27480=CARTESIAN_POINT ( 'NONE',  ( 43.75706346978401484, 7.740046907999022174, -71.93205349775588786 ) ) ;
#27493=EDGE_CURVE ( 'NONE', #45223, #7747, #41591, .T. ) ;
#27511=CARTESIAN_POINT ( 'NONE',  ( 19.31296351478369999, -49.88685839599860117, -82.14319696191608955 ) ) ;
#27538=CARTESIAN_POINT ( 'NONE',  ( 22.37318698975099807, -53.60726374558549878, -34.64999999999999858 ) ) ;
#27549=DIRECTION ( 'NONE',  ( 0.6339889056055360017, 0.000000000000000000, -0.7733421413379041320 ) ) ;
#27554=CARTESIAN_POINT ( 'NONE',  ( 45.34397758664299971, 2.696163290909390220, -34.64999999999999858 ) ) ;
#27562=ORIENTED_EDGE ( 'NONE', *, *, #33968, .T. ) ;
#27566=CARTESIAN_POINT ( 'NONE',  ( 0.1416488651360897633, -45.95570562466429010, -34.68322412398369892 ) ) ;
#27568=DIRECTION ( 'NONE',  ( 0.000000000000000000, 0.000000000000000000, 1.000000000000000000 ) ) ;
#27575=CARTESIAN_POINT ( 'NONE',  ( 43.51419838157591613, 6.618822493252672245, -72.74866027328177154 ) ) ;
#27580=CARTESIAN_POINT ( 'NONE',  ( 45.25840371050470168, 2.392299703521869603, -34.70497375832189846 ) ) ;
#27592=EDGE_LOOP ( 'NONE', ( #46552, #49638, #21694, #22599 ) ) ;
#27594=EDGE_CURVE ( 'NONE', #46163, #51177, #44102, .T. ) ;
#27617=CARTESIAN_POINT ( 'NONE',  ( 47.07753517504149698, 8.029056321811339103, -34.91082242604309727 ) ) ;
#27620=DIRECTION ( 'NONE',  ( -0.5516667872527302174, -0.8340645993220495713, 0.000000000000000000 ) ) ;
#27631=DIRECTION ( 'NONE',  ( -1.000000000000000000, 0.000000000000000000, 0.000000000000000000 ) ) ;
#27640=VECTOR ( 'NONE', #9031, 1000.000000000000000 ) ;
#27642=( BOUNDED_CURVE ( )  B_SPLINE_CURVE ( 3, ( #39804, #32165, #15960, #48181 ),
 .UNSPECIFIED., .F., .T. ) 
 B_SPLINE_CURVE_WITH_KNOTS ( ( 4, 4 ),
 ( 5.497787143782128183, 6.283185307179577350 ),
 .UNSPECIFIED. ) 
 CURVE ( )  GEOMETRIC_REPRESENTATION_ITEM ( )  RATIONAL_B_SPLINE_CURVE ( ( 1.000000000000000000, 0.9492530216741897897, 0.9492530216741897897, 1.000000000000000000 ) ) 
 REPRESENTATION_ITEM ( '' )  );
#27644=DIRECTION ( 'NONE',  ( 0.000000000000000000, 5.418249000000000090E-13, 1.000000000000000000 ) ) ;
#27646=CIRCLE ( 'NONE', #906, 0.5000000000000028866 ) ;
#27648=DIRECTION ( 'NONE',  ( -0.5516667872527557526, 0.8340645993220324739, 0.000000000000000000 ) ) ;
#27651=CYLINDRICAL_SURFACE ( 'NONE', #31241, 0.4999999999999967248 ) ;
#27654=ORIENTED_EDGE ( 'NONE', *, *, #13957, .F. ) ;
#27659=CARTESIAN_POINT ( 'NONE',  ( 43.66028230008726041, -39.92605316001158400, -68.30461377173425319 ) ) ;
#27678=CARTESIAN_POINT ( 'NONE',  ( 27.50893739769620083, -36.61730498645199816, -35.14999999999999858 ) ) ;
#27680=CARTESIAN_POINT ( 'NONE',  ( 41.77940164082745156, 8.508192307914475450, -77.39573496664088736 ) ) ;
#27681=LINE ( 'NONE', #51289, #33959 ) ;
#27686=CARTESIAN_POINT ( 'NONE',  ( 0.06064750360406240270, 19.78548888128160144, -34.82147232542479998 ) ) ;
#27694=ORIENTED_EDGE ( 'NONE', *, *, #11492, .F. ) ;
#27708=CARTESIAN_POINT ( 'NONE',  ( 17.76831794872855141, -41.98180839364705008, -34.64999999999999858 ) ) ;
#27721=DIRECTION ( 'NONE',  ( 0.000000000000000000, 0.000000000000000000, 1.000000000000000000 ) ) ;
#27722=CARTESIAN_POINT ( 'NONE',  ( 0.1457841021255935343, -4.451138319363987073, -34.68167779225149161 ) ) ;
#27726=CARTESIAN_POINT ( 'NONE',  ( 8.737696419500725398, -48.93815596428014203, -34.78557451168259007 ) ) ;
#27727=CARTESIAN_POINT ( 'NONE',  ( 0.02075511821175915136, 19.53788625088298048, -34.74841884006161052 ) ) ;
#27734=CYLINDRICAL_SURFACE ( 'NONE', #38846, 0.4999999999999982236 ) ;
#27739=CARTESIAN_POINT ( 'NONE',  ( 44.14073854797647556, 6.492434696291280893, -69.57759189706122527 ) ) ;
#27742=EDGE_CURVE ( 'NONE', #12820, #26692, #36464, .T. ) ;
#27759=CIRCLE ( 'NONE', #19386, 31.45861873485090143 ) ;
#27760=VECTOR ( 'NONE', #1127, 1000.000000000000114 ) ;
#27761=ORIENTED_EDGE ( 'NONE', *, *, #32152, .F. ) ;
#27765=VERTEX_POINT ( 'NONE', #38318 ) ;
#27771=CARTESIAN_POINT ( 'NONE',  ( 19.28172483834616457, -49.83962866466755059, -82.44267625234891739 ) ) ;
#27778=CARTESIAN_POINT ( 'NONE',  ( 46.69599177284572988, -38.22215067635794128, -56.83968353337930068 ) ) ;
#27795=CYLINDRICAL_SURFACE ( 'NONE', #36428, 0.4999999999999982236 ) ;
#27809=ORIENTED_EDGE ( 'NONE', *, *, #37329, .F. ) ;
#27810=CARTESIAN_POINT ( 'NONE',  ( 23.32430482491550094, 18.10127401595489971, -34.64999999999999858 ) ) ;
#27812=DIRECTION ( 'NONE',  ( 0.000000000000000000, -1.000000000000000000, 0.000000000000000000 ) ) ;
#27816=CARTESIAN_POINT ( 'NONE',  ( 16.13393739769620083, -1.759782484128330049, -35.14999999999999858 ) ) ;
#27819=CARTESIAN_POINT ( 'NONE',  ( 17.63393739769629676, 0.9255523191756780399, -34.64999999999999858 ) ) ;
#27828=B_SPLINE_CURVE_WITH_KNOTS ( 'NONE', 3,
 ( #34863, #42754, #19139, #7108, #30410, #30667, #38558, #50864, #46951, #50354 ),
 .UNSPECIFIED., .F., .F.,
 ( 4, 2, 2, 2, 4 ),
 ( -0.1857717838173399971, -0.1853436703578560107, -0.1652145016253949994, -0.1459149143061169995, -0.1350635247397783956 ),
 .UNSPECIFIED. ) ;
#27832=CARTESIAN_POINT ( 'NONE',  ( 43.95317894857520002, 6.678920976524271857, -70.55372978514877502 ) ) ;
#27834=EDGE_CURVE ( 'NONE', #37056, #14308, #23842, .T. ) ;
#27849=EDGE_CURVE ( 'NONE', #35594, #43797, #27268, .T. ) ;
#27860=CARTESIAN_POINT ( 'NONE',  ( 28.13393739769619728, -8.687985714403851034, -47.64999999999999858 ) ) ;
#27873=ORIENTED_EDGE ( 'NONE', *, *, #36610, .F. ) ;
#27879=ORIENTED_EDGE ( 'NONE', *, *, #29900, .T. ) ;
#27882=ORIENTED_EDGE ( 'NONE', *, *, #6084, .T. ) ;
#27891=CARTESIAN_POINT ( 'NONE',  ( -0.007164427059776000244, -10.48291004383190028, -34.77269723891829756 ) ) ;
#27894=EDGE_LOOP ( 'NONE', ( #51807, #32172, #19713, #11255, #1784 ) ) ;
#27903=LINE ( 'NONE', #47085, #20388 ) ;
#27909=CONICAL_SURFACE ( 'NONE', #37136, 19.50000000000000000, 0.2449786631268651149 ) ;
#27911=CARTESIAN_POINT ( 'NONE',  ( 11.96660005458890019, -42.11618894467939356, -34.64999999999999858 ) ) ;
#27912=ADVANCED_FACE ( 'NONE', ( #51662 ), #41491, .F. ) ;
#27914=CARTESIAN_POINT ( 'NONE',  ( 42.23111299307110045, -39.78919581839614494, -75.21549960612240682 ) ) ;
#27931=CARTESIAN_POINT ( 'NONE',  ( 42.01616251554107606, 8.533769718121346770, -76.25424629209925342 ) ) ;
#27936=LINE ( 'NONE', #43938, #32284 ) ;
#27937=VERTEX_POINT ( 'NONE', #282 ) ;
#27942=VERTEX_POINT ( 'NONE', #27538 ) ;
#27944=LINE ( 'NONE', #35307, #5327 ) ;
#27948=CARTESIAN_POINT ( 'NONE',  ( 20.63541822830159589, 20.65389878999348738, -69.46507341768980837 ) ) ;
#27955=CARTESIAN_POINT ( 'NONE',  ( 47.13393739769619373, 8.048130187719129580, -35.14999999999999858 ) ) ;
#27958=DIRECTION ( 'NONE',  ( 0.000000000000000000, -1.000000000000000000, 0.000000000000000000 ) ) ;
#27987=CARTESIAN_POINT ( 'NONE',  ( 43.45629245243522121, 6.417003004502526586, -73.00576010489325540 ) ) ;
#27995=CARTESIAN_POINT ( 'NONE',  ( 0.1457841021255935343, -15.61618894467929941, -34.68167779225149161 ) ) ;
#28010=ORIENTED_EDGE ( 'NONE', *, *, #8160, .T. ) ;
#28017=CARTESIAN_POINT ( 'NONE',  ( 44.13393739769620083, -33.11618894467940066, -54.35294145922159714 ) ) ;
#28033=CARTESIAN_POINT ( 'NONE',  ( 47.13393739769619373, -38.60474673416580060, -54.64997574802373492 ) ) ;
#28040=CARTESIAN_POINT ( 'NONE',  ( 41.70634816843200809, -39.79356890906309729, -77.49277520938784392 ) ) ;
#28057=AXIS2_PLACEMENT_3D ( 'NONE', #20171, #4711, #35905 ) ;
#28065=CARTESIAN_POINT ( 'NONE',  ( 2.558062577110330249, -25.18749138766609974, -34.64999999999999858 ) ) ;
#28070=EDGE_LOOP ( 'NONE', ( #29871, #6449, #18416, #43600, #22805, #24328, #9334, #35295, #45614, #49649, #2600, #11270, #34980 ) ) ;
#28079=AXIS2_PLACEMENT_3D ( 'NONE', #6496, #26383, #9902 ) ;
#28080=CARTESIAN_POINT ( 'NONE',  ( 17.94297559678599185, 1.205480371600828438, -34.75586992539665943 ) ) ;
#28085=CARTESIAN_POINT ( 'NONE',  ( 45.20441673098799384, 2.222700185736389944, -34.80570975016329527 ) ) ;
#28088=SHAPE_REPRESENTATION ( 'Foot Base', ( #20940 ), #50248 ) ;
#28106=DIRECTION ( 'NONE',  ( 0.5897727341282554825, -0.3900873262218120252, 0.7071067811865473507 ) ) ;
#28108=VECTOR ( 'NONE', #24928, 1000.000000000000000 ) ;
#28120=CARTESIAN_POINT ( 'NONE',  ( 20.39068152308574966, -41.98180839364705008, -34.64999999999999147 ) ) ;
#28134=VERTEX_POINT ( 'NONE', #36561 ) ;
#28137=CARTESIAN_POINT ( 'NONE',  ( 18.47369125467839979, -4.651823196201450017, -35.14999999999999858 ) ) ;
#28138=CARTESIAN_POINT ( 'NONE',  ( 0.4047412638266219553, -8.844334399411719616, -35.14999999999999858 ) ) ;
#28139=DIRECTION ( 'NONE',  ( -0.1643989873053569861, -8.962268658296950507E-16, 0.9863939238321438596 ) ) ;
#28147=ORIENTED_EDGE ( 'NONE', *, *, #10118, .T. ) ;
#28152=CARTESIAN_POINT ( 'NONE',  ( 30.13393739769619728, 7.383811055320659733, -59.64999999999999147 ) ) ;
#28160=CIRCLE ( 'NONE', #5606, 3.000000000000001332 ) ;
#28162=CARTESIAN_POINT ( 'NONE',  ( 28.37540540599746919, -8.548574094810419410, -34.70142521051217699 ) ) ;
#28165=CARTESIAN_POINT ( 'NONE',  ( 44.09118259309181553, -39.96203129707259905, -66.21835677545064414 ) ) ;
#28175=ADVANCED_FACE ( 'NONE', ( #32352 ), #930, .T. ) ;
#28184=FACE_OUTER_BOUND ( 'NONE', #30341, .T. ) ;
#28185=CARTESIAN_POINT ( 'NONE',  ( 41.05890600732872286, 8.424924847782378379, -80.87056964938905423 ) ) ;
#28186=CARTESIAN_POINT ( 'NONE',  ( 19.33046814882933973, 18.01819160635306716, -34.64999999999999858 ) ) ;
#28201=EDGE_CURVE ( 'NONE', #23386, #20265, #9059, .T. ) ;
#28206=EDGE_CURVE ( 'NONE', #40830, #33379, #36298, .T. ) ;
#28208=FACE_OUTER_BOUND ( 'NONE', #22531, .T. ) ;
#28213=DIRECTION ( 'NONE',  ( -0.4999999999999985012, 0.8660254037844394848, 0.000000000000000000 ) ) ;
#28217=CARTESIAN_POINT ( 'NONE',  ( -22.66047177492978548, -11.61221224052196455, -54.65944424064918650 ) ) ;
#28220=CARTESIAN_POINT ( 'NONE',  ( 14.63393739769640156, 10.88381105532070059, -34.64999999999999858 ) ) ;
#28225=ORIENTED_EDGE ( 'NONE', *, *, #47034, .T. ) ;
#28228=DIRECTION ( 'NONE',  ( 0.000000000000000000, 0.000000000000000000, -1.000000000000000000 ) ) ;
#28241=ORIENTED_EDGE ( 'NONE', *, *, #9121, .F. ) ;
#28244=CARTESIAN_POINT ( 'NONE',  ( 53.58923637029294440, -18.19535155712478414, -15.94606409914099210 ) ) ;
#28245=DIRECTION ( 'NONE',  ( 0.000000000000000000, -1.000000000000000000, 0.000000000000000000 ) ) ;
#28265=DIRECTION ( 'NONE',  ( -0.8660254037844387076, -0.4999999999999998890, 1.110223024625155678E-16 ) ) ;
#28266=ORIENTED_EDGE ( 'NONE', *, *, #7799, .T. ) ;
#28271=DIRECTION ( 'NONE',  ( -1.000000000000000000, 0.000000000000000000, 0.000000000000000000 ) ) ;
#28275=DIRECTION ( 'NONE',  ( 1.000000000000000000, 0.000000000000000000, 0.000000000000000000 ) ) ;
#28293=CARTESIAN_POINT ( 'NONE',  ( 30.72739985827759313, -35.67572234546251764, -84.61750747199793921 ) ) ;
#28302=EDGE_CURVE ( 'NONE', #2651, #2348, #51591, .T. ) ;
#28309=EDGE_CURVE ( 'NONE', #41238, #23939, #42824, .T. ) ;
#28315=LINE ( 'NONE', #4223, #42888 ) ;
#28317=CARTESIAN_POINT ( 'NONE',  ( 0.3209249304026170480, -46.25141913721060405, -34.64999999999999858 ) ) ;
#28321=CYLINDRICAL_SURFACE ( 'NONE', #40894, 0.4999999999999982236 ) ;
#28330=ORIENTED_EDGE ( 'NONE', *, *, #6889, .T. ) ;
#28331=ADVANCED_FACE ( 'NONE', ( #25534 ), #41281, .T. ) ;
#28339=LINE ( 'NONE', #40412, #21290 ) ;
#28340=CARTESIAN_POINT ( 'NONE',  ( 41.67047660715986979, -37.56944021528936872, -81.96730251586943439 ) ) ;
#28349=CIRCLE ( 'NONE', #9150, 0.5000000000000004441 ) ;
#28352=CARTESIAN_POINT ( 'NONE',  ( 13.63393739769619906, -45.61618894467940066, -34.64999999999999858 ) ) ;
#28366=CARTESIAN_POINT ( 'NONE',  ( 17.00276768726040899, 18.38376088500272587, -83.22678919096382799 ) ) ;
#28368=CARTESIAN_POINT ( 'NONE',  ( -0.007164427059776000244, -22.82436266295209748, -34.77269723891829756 ) ) ;
#28370=EDGE_CURVE ( 'NONE', #46428, #21893, #26319, .T. ) ;
#28382=DIRECTION ( 'NONE',  ( 1.000000000000000000, 0.000000000000000000, 0.000000000000000000 ) ) ;
#28391=AXIS2_PLACEMENT_3D ( 'NONE', #35754, #19507, #116 ) ;
#28392=ORIENTED_EDGE ( 'NONE', *, *, #12854, .T. ) ;
#28396=( BOUNDED_CURVE ( )  B_SPLINE_CURVE ( 3, ( #27331, #36939, #7429, #11111 ),
 .UNSPECIFIED., .F., .T. ) 
 B_SPLINE_CURVE_WITH_KNOTS ( ( 4, 4 ),
 ( 2.795354856560299694, 3.141592653589793116 ),
 .UNSPECIFIED. ) 
 CURVE ( )  GEOMETRIC_REPRESENTATION_ITEM ( )  RATIONAL_B_SPLINE_CURVE ( ( 1.000000000000000000, 0.9900348743600091428, 0.9900348743600091428, 1.000000000000000000 ) ) 
 REPRESENTATION_ITEM ( '' )  );
#28401=ORIENTED_EDGE ( 'NONE', *, *, #7933, .T. ) ;
#28403=CARTESIAN_POINT ( 'NONE',  ( 14.13393739769619906, -37.52509124488599923, -54.64999999999999858 ) ) ;
#28406=CARTESIAN_POINT ( 'NONE',  ( 0.3188076311095650595, -10.53374720320550040, -34.65000336222090027 ) ) ;
#28412=DIRECTION ( 'NONE',  ( -1.000000000000000000, 0.000000000000000000, 0.000000000000000000 ) ) ;
#28414=AXIS2_PLACEMENT_3D ( 'NONE', #49254, #8376, #45049 ) ;
#28416=CIRCLE ( 'NONE', #17555, 6.999999999999999112 ) ;
#28427=CARTESIAN_POINT ( 'NONE',  ( 42.58520944582495815, -39.82551429970306600, -73.50479774005893319 ) ) ;
#28435=CARTESIAN_POINT ( 'NONE',  ( 18.11900864776900022, 1.362847559348050019, -35.02873218748179340 ) ) ;
#28436=CARTESIAN_POINT ( 'NONE',  ( 17.98749078828947745, -32.58675169315650066, -34.79644660940672907 ) ) ;
#28441=DIRECTION ( 'NONE',  ( 0.000000000000000000, 0.7071067811865463515, -0.7071067811865487940 ) ) ;
#28443=CARTESIAN_POINT ( 'NONE',  ( 23.53017837589144889, 17.70577807492161071, -34.78557451168261849 ) ) ;
#28444=LINE ( 'NONE', #5399, #19381 ) ;
#28445=CARTESIAN_POINT ( 'NONE',  ( 42.31769135335058252, 8.566187770374650512, -74.79605566854385756 ) ) ;
#28446=CARTESIAN_POINT ( 'NONE',  ( 19.26373325286755644, 18.14234304701946243, -34.70142521051218409 ) ) ;
#28448=DIRECTION ( 'NONE',  ( 0.000000000000000000, -1.000000000000000000, 0.000000000000000000 ) ) ;
#28451=ORIENTED_EDGE ( 'NONE', *, *, #29453, .T. ) ;
#28454=FACE_BOUND ( 'NONE', #31421, .T. ) ;
#28466=CARTESIAN_POINT ( 'NONE',  ( -15.36168286337127853, 7.384389844490065080, -48.43517473143955243 ) ) ;
#28467=CARTESIAN_POINT ( 'NONE',  ( 14.32270318449056035, 18.38377289504289180, -83.16479114466771705 ) ) ;
#28469=DIRECTION ( 'NONE',  ( 0.000000000000000000, -0.7071067811865466846, -0.7071067811865483499 ) ) ;
#28470=DIRECTION ( 'NONE',  ( -1.000000000000000000, 0.000000000000000000, 0.000000000000000000 ) ) ;
#28477=EDGE_CURVE ( 'NONE', #26529, #33379, #40806, .T. ) ;
#28488=ORIENTED_EDGE ( 'NONE', *, *, #44655, .T. ) ;
#28497=VECTOR ( 'NONE', #49769, 1000.000000000000000 ) ;
#28499=DIRECTION ( 'NONE',  ( 1.000000000000000000, 0.000000000000000000, 0.000000000000000000 ) ) ;
#28508=CARTESIAN_POINT ( 'NONE',  ( 2.488944341170579833, -5.725871553929439806, -34.70985242058479514 ) ) ;
#28518=ORIENTED_EDGE ( 'NONE', *, *, #41560, .F. ) ;
#28524=CARTESIAN_POINT ( 'NONE',  ( 0.1457840918200039859, -10.50670027737364620, -34.68167776469301344 ) ) ;
#28525=ORIENTED_EDGE ( 'NONE', *, *, #29715, .F. ) ;
#28547=CARTESIAN_POINT ( 'NONE',  ( 11.79459217608825483, 10.62527906362197605, -34.70142521051213436 ) ) ;
#28554=CARTESIAN_POINT ( 'NONE',  ( 14.86785676567460079, -49.61616128341084675, -83.20618638372945952 ) ) ;
#28566=LINE ( 'NONE', #44566, #29362 ) ;
#28578=FACE_BOUND ( 'NONE', #4997, .T. ) ;
#28583=CARTESIAN_POINT ( 'NONE',  ( 46.81384049422970151, 7.939671762211538919, -34.68207991959079806 ) ) ;
#28590=CARTESIAN_POINT ( 'NONE',  ( 15.53930990683081070, 7.815833215755628061, 4.943674098299959851 ) ) ;
#28600=EDGE_CURVE ( 'NONE', #42649, #14039, #44968, .T. ) ;
#28602=CARTESIAN_POINT ( 'NONE',  ( 42.30137742020378511, -37.67163298317260001, -78.81279910741842798 ) ) ;
#28606=B_SPLINE_CURVE_WITH_KNOTS ( 'NONE', 3,
 ( #24941, #5587, #41215, #13708, #37286, #5068, #21025, #25466 ),
 .UNSPECIFIED., .F., .F.,
 ( 4, 2, 2, 4 ),
 ( 0.08616863070364449984, 0.1028498217467809922, 0.1208689123369260099, 0.1272047750342873151 ),
 .UNSPECIFIED. ) ;
#28608=VECTOR ( 'NONE', #29793, 1000.000000000000000 ) ;
#28613=CARTESIAN_POINT ( 'NONE',  ( 45.34397758664299971, -33.92854118026809829, -34.64999999999999858 ) ) ;
#28628=CARTESIAN_POINT ( 'NONE',  ( 18.47369125467839979, -4.651823196201450017, -35.14999999999999858 ) ) ;
#28631=CARTESIAN_POINT ( 'NONE',  ( 21.50893739769619728, 1.920825481955539926, -35.14999999999999858 ) ) ;
#28639=EDGE_LOOP ( 'NONE', ( #369, #38085, #3814, #12601, #46459 ) ) ;
#28640=DIRECTION ( 'NONE',  ( 0.000000000000000000, 0.7071067811865475727, 0.7071067811865475727 ) ) ;
#28645=ORIENTED_EDGE ( 'NONE', *, *, #51530, .F. ) ;
#28658=ORIENTED_EDGE ( 'NONE', *, *, #9758, .F. ) ;
#28678=ORIENTED_EDGE ( 'NONE', *, *, #21347, .F. ) ;
#28679=CARTESIAN_POINT ( 'NONE',  ( 18.00872666787291365, 1.264432139860217852, -34.81767276520689336 ) ) ;
#28680=CARTESIAN_POINT ( 'NONE',  ( 28.63393739769619728, -8.399310579809030841, -34.64999999999999858 ) ) ;
#28683=EDGE_CURVE ( 'NONE', #24767, #46747, #3040, .T. ) ;
#28684=CARTESIAN_POINT ( 'NONE',  ( 43.02789550845886168, -39.86892128716395689, -71.36382768978903357 ) ) ;
#28685=CARTESIAN_POINT ( 'NONE',  ( 14.49955684666403144, 10.74943050428832869, -34.64999999999999858 ) ) ;
#28693=ORIENTED_EDGE ( 'NONE', *, *, #23919, .F. ) ;
#28695=( BOUNDED_CURVE ( )  B_SPLINE_CURVE ( 3, ( #761, #12069, #16757, #23819 ),
 .UNSPECIFIED., .F., .T. ) 
 B_SPLINE_CURVE_WITH_KNOTS ( ( 4, 4 ),
 ( 4.712388980384691450, 5.497787143782140618 ),
 .UNSPECIFIED. ) 
 CURVE ( )  GEOMETRIC_REPRESENTATION_ITEM ( )  RATIONAL_B_SPLINE_CURVE ( ( 1.000000000000000000, 0.9492530216741910110, 0.9492530216741910110, 1.000000000000000000 ) ) 
 REPRESENTATION_ITEM ( '' )  );
#28701=DIRECTION ( 'NONE',  ( 0.000000000000000000, 0.000000000000000000, -1.000000000000000000 ) ) ;
#28702=CARTESIAN_POINT ( 'NONE',  ( 42.92778368268686506, 8.626831504079211399, -71.84863307370312668 ) ) ;
#28704=EDGE_CURVE ( 'NONE', #33893, #38344, #10748, .T. ) ;
#28717=CIRCLE ( 'NONE', #46329, 17.09468304687040785 ) ;
#28721=CARTESIAN_POINT ( 'NONE',  ( -8.460328592820898663, 14.65132278408173860, -42.51048757408748457 ) ) ;
#28722=CARTESIAN_POINT ( 'NONE',  ( 14.53805447820786512, 18.38379093432319422, -83.18296600395719054 ) ) ;
#28729=CARTESIAN_POINT ( 'NONE',  ( -110.7194986169279929, 1.883811055205739882, -112.4763993716680091 ) ) ;
#28740=CYLINDRICAL_SURFACE ( 'NONE', #38552, 0.5000000000000014433 ) ;
#28755=CARTESIAN_POINT ( 'NONE',  ( 22.13393739769619728, -54.15188668067469990, -54.64999999999999858 ) ) ;
#28763=ORIENTED_EDGE ( 'NONE', *, *, #34538, .T. ) ;
#28765=CARTESIAN_POINT ( 'NONE',  ( 23.62413055734840128, 17.52287609088140030, -35.14999999999999858 ) ) ;
#28766=DIRECTION ( 'NONE',  ( 0.5112408204145768575, 0.8594375041513085955, 0.000000000000000000 ) ) ;
#28773=EDGE_CURVE ( 'NONE', #37113, #41542, #17296, .T. ) ;
#28775=ORIENTED_EDGE ( 'NONE', *, *, #34757, .T. ) ;
#28787=DIRECTION ( 'NONE',  ( 0.000000000000000000, 0.000000000000000000, -1.000000000000000000 ) ) ;
#28792=CIRCLE ( 'NONE', #2019, 33.00000000000000000 ) ;
#28793=ORIENTED_EDGE ( 'NONE', *, *, #12374, .F. ) ;
#28805=CARTESIAN_POINT ( 'NONE',  ( 22.13393739769619728, -54.15188668067469990, -34.64999999999999858 ) ) ;
#28807=CARTESIAN_POINT ( 'NONE',  ( 13.63393739769599833, 14.38381105532070059, -35.14999999999999858 ) ) ;
#28808=CARTESIAN_POINT ( 'NONE',  ( -13.39236625349549925, -0.8785706602474870897, -54.64999999999999858 ) ) ;
#28839=ADVANCED_FACE ( 'NONE', ( #7332 ), #40068, .T. ) ;
#28842=FACE_BOUND ( 'NONE', #2062, .T. ) ;
#28851=ORIENTED_EDGE ( 'NONE', *, *, #11370, .T. ) ;
#28864=EDGE_CURVE ( 'NONE', #49018, #1956, #3660, .T. ) ;
#28870=ORIENTED_EDGE ( 'NONE', *, *, #6384, .F. ) ;
#28885=CARTESIAN_POINT ( 'NONE',  ( 16.13393739769599833, 14.38381105532070059, -34.64999999999999858 ) ) ;
#28886=ORIENTED_EDGE ( 'NONE', *, *, #46861, .T. ) ;
#28904=FACE_OUTER_BOUND ( 'NONE', #49878, .T. ) ;
#28928=ORIENTED_EDGE ( 'NONE', *, *, #25195, .F. ) ;
#28930=CARTESIAN_POINT ( 'NONE',  ( 0.3209249304026170480, -10.53407907283069989, -34.64999999999999858 ) ) ;
#28940=EDGE_LOOP ( 'NONE', ( #23121, #2836, #3738, #22261, #8438, #48852, #37964, #10060 ) ) ;
#28949=CARTESIAN_POINT ( 'NONE',  ( -0.8602693046289622281, -12.42650008425934693, -35.51452756723926996 ) ) ;
#28951=CIRCLE ( 'NONE', #4689, 16.60961179679779676 ) ;
#28953=EDGE_CURVE ( 'NONE', #21893, #11156, #27307, .T. ) ;
#28958=EDGE_CURVE ( 'NONE', #37692, #23421, #33988, .T. ) ;
#28965=CARTESIAN_POINT ( 'NONE',  ( 17.63393739769620083, -42.11618894467939356, -34.64999999999999858 ) ) ;
#28967=CARTESIAN_POINT ( 'NONE',  ( 43.14635114408183370, 8.647671771403498298, -70.79083171591096857 ) ) ;
#28968=CARTESIAN_POINT ( 'NONE',  ( 19.21265657477716005, 18.23736444591407135, -34.79644660940672907 ) ) ;
#28974=ORIENTED_EDGE ( 'NONE', *, *, #22235, .F. ) ;
#28977=DIRECTION ( 'NONE',  ( 0.9805806756909202226, 0.000000000000000000, -0.1961161351381840445 ) ) ;
#28982=ORIENTED_EDGE ( 'NONE', *, *, #50752, .T. ) ;
#28984=FACE_OUTER_BOUND ( 'NONE', #26194, .T. ) ;
#28987=CARTESIAN_POINT ( 'NONE',  ( -9.252977670667002386, 13.99041838265985582, -43.19094538359154711 ) ) ;
#28988=DIRECTION ( 'NONE',  ( -0.5516667872527503125, 0.8340645993220362486, -1.942890293094025918E-16 ) ) ;
#28990=EDGE_CURVE ( 'NONE', #7271, #45182, #51355, .T. ) ;
#28992=ORIENTED_EDGE ( 'NONE', *, *, #4402, .F. ) ;
#28993=CYLINDRICAL_SURFACE ( 'NONE', #15797, 0.4999999999999994449 ) ;
#29001=B_SPLINE_CURVE_WITH_KNOTS ( 'NONE', 3,
 ( #10610, #34948, #39418, #42319 ),
 .UNSPECIFIED., .F., .F.,
 ( 4, 4 ),
 ( 0.000000000000000000, 1.000000000000000000 ),
 .UNSPECIFIED. ) ;
#29003=FACE_OUTER_BOUND ( 'NONE', #12043, .T. ) ;
#29010=ORIENTED_EDGE ( 'NONE', *, *, #46888, .T. ) ;
#29012=AXIS2_PLACEMENT_3D ( 'NONE', #47295, #31525, #35984 ) ;
#29016=( BOUNDED_CURVE ( )  B_SPLINE_CURVE ( 3, ( #29542, #45028, #13325, #37672 ),
 .UNSPECIFIED., .F., .T. ) 
 B_SPLINE_CURVE_WITH_KNOTS ( ( 4, 4 ),
 ( 2.356194490192332403, 3.141592653589799777 ),
 .UNSPECIFIED. ) 
 CURVE ( )  GEOMETRIC_REPRESENTATION_ITEM ( )  RATIONAL_B_SPLINE_CURVE ( ( 1.000000000000000000, 0.9492530216741885685, 0.9492530216741885685, 1.000000000000000000 ) ) 
 REPRESENTATION_ITEM ( '' )  );
#29018=CONICAL_SURFACE ( 'NONE', #50768, 36.50000000000000000, 0.1651486774146265213 ) ;
#29051=CARTESIAN_POINT ( 'NONE',  ( 0.1457841021255935343, -26.78123956999450428, -34.68167779225149161 ) ) ;
#29065=DIRECTION ( 'NONE',  ( -1.000000000000000000, 0.000000000000000000, 0.000000000000000000 ) ) ;
#29074=VERTEX_POINT ( 'NONE', #12551 ) ;
#29082=CARTESIAN_POINT ( 'NONE',  ( 30.52248363924751828, -35.64217098745972123, -84.61231660026447798 ) ) ;
#29083=DIRECTION ( 'NONE',  ( 0.000000000000000000, -1.000000000000000000, 0.000000000000000000 ) ) ;
#29085=EDGE_LOOP ( 'NONE', ( #31523, #7484, #1260, #382, #47011 ) ) ;
#29110=CARTESIAN_POINT ( 'NONE',  ( 37.88393739769619373, -42.11618894467939356, -35.14999999999999858 ) ) ;
#29112=ORIENTED_EDGE ( 'NONE', *, *, #32512, .F. ) ;
#29117=VERTEX_POINT ( 'NONE', #25352 ) ;
#29120=CARTESIAN_POINT ( 'NONE',  ( 13.24776434638835632, -17.71311640963744338, -643.2998782751060389 ) ) ;
#29128=CARTESIAN_POINT ( 'NONE',  ( 42.30441222516678579, -37.67211025355430110, -78.79762527759561408 ) ) ;
#29129=ORIENTED_EDGE ( 'NONE', *, *, #12294, .T. ) ;
#29146=ORIENTED_EDGE ( 'NONE', *, *, #33998, .F. ) ;
#29163=ORIENTED_EDGE ( 'NONE', *, *, #5638, .T. ) ;
#29168=ORIENTED_EDGE ( 'NONE', *, *, #48028, .F. ) ;
#29170=ORIENTED_EDGE ( 'NONE', *, *, #11528, .T. ) ;
#29178=DIRECTION ( 'NONE',  ( 0.2201791028319839971, 0.9741803703773870282, 0.04993764759657599861 ) ) ;
#29182=VECTOR ( 'NONE', #25368, 1000.000000000000000 ) ;
#29188=CARTESIAN_POINT ( 'NONE',  ( 0.2007819157892938577, -10.51527493241353994, -34.66110989977890000 ) ) ;
#29198=ORIENTED_EDGE ( 'NONE', *, *, #16834, .T. ) ;
#29202=CARTESIAN_POINT ( 'NONE',  ( 18.70688454841999970, -48.06418385137889970, -35.14999999999999858 ) ) ;
#29205=CIRCLE ( 'NONE', #32517, 39.00000000000000711 ) ;
#29222=CARTESIAN_POINT ( 'NONE',  ( 23.32493948456750132, 18.10006093832409491, -34.64999999999999858 ) ) ;
#29223=DIRECTION ( 'NONE',  ( 0.8204012560548800126, 0.5717882292104090602, 0.000000000000000000 ) ) ;
#29224=CARTESIAN_POINT ( 'NONE',  ( 43.63119145555815237, 8.691161901990289707, -68.44539823191810513 ) ) ;
#29233=CARTESIAN_POINT ( 'NONE',  ( -3.839728563314020349, -6.393788602144800493, -54.64999999999999858 ) ) ;
#29240=CARTESIAN_POINT ( 'NONE',  ( -11.60499810224809103, 11.81104071652318410, -45.20979172290213199 ) ) ;
#29241=FACE_OUTER_BOUND ( 'NONE', #7384, .T. ) ;
#29243=CARTESIAN_POINT ( 'NONE',  ( 16.13393739769620083, -29.47259540523037202, -35.01561944896766221 ) ) ;
#29246=ORIENTED_EDGE ( 'NONE', *, *, #15270, .T. ) ;
#29247=DIRECTION ( 'NONE',  ( 0.000000000000000000, -0.7071067811865492381, 0.7071067811865457964 ) ) ;
#29252=CIRCLE ( 'NONE', #35170, 2.999999999999999112 ) ;
#29253=VECTOR ( 'NONE', #50123, 1000.000000000000000 ) ;
#29255=DIRECTION ( 'NONE',  ( 0.000000000000000000, 0.000000000000000000, -1.000000000000000000 ) ) ;
#29257=EDGE_CURVE ( 'NONE', #27765, #5705, #21384, .T. ) ;
#29263=LINE ( 'NONE', #42365, #21784 ) ;
#29269=DIRECTION ( 'NONE',  ( 0.000000000000000000, 0.000000000000000000, 1.000000000000000000 ) ) ;
#29270=EDGE_CURVE ( 'NONE', #13277, #45223, #24219, .T. ) ;
#29284=VECTOR ( 'NONE', #22909, 1000.000000000000000 ) ;
#29300=DIRECTION ( 'NONE',  ( 0.000000000000000000, 0.7071067811865475727, 0.7071067811865475727 ) ) ;
#29303=CARTESIAN_POINT ( 'NONE',  ( 0.8105618841727830759, -51.44517397597059727, -34.28607352350360316 ) ) ;
#29304=CARTESIAN_POINT ( 'NONE',  ( 16.13393739769620083, -15.61618894467919816, -82.14319696191608955 ) ) ;
#29324=EDGE_CURVE ( 'NONE', #33273, #33944, #33734, .T. ) ;
#29325=VECTOR ( 'NONE', #13050, 1000.000000000000000 ) ;
#29333=ADVANCED_FACE ( 'NONE', ( #46083 ), #50778, .T. ) ;
#29337=CARTESIAN_POINT ( 'NONE',  ( 16.13393739769620083, -15.61618894467929941, -84.65000000000000568 ) ) ;
#29338=CARTESIAN_POINT ( 'NONE',  ( 13.60966998086417590, -49.61618894467943619, -83.09320499168605068 ) ) ;
#29341=CARTESIAN_POINT ( 'NONE',  ( 44.97440182180130108, -40.14835006695389552, -61.45165435098494555 ) ) ;
#29343=EDGE_CURVE ( 'NONE', #40171, #32200, #30054, .T. ) ;
#29356=EDGE_LOOP ( 'NONE', ( #9295, #46101, #4755, #29524 ) ) ;
#29362=VECTOR ( 'NONE', #8667, 1000.000000000000000 ) ;
#29365=CARTESIAN_POINT ( 'NONE',  ( 2.488944341170570063, -25.50650633542909773, -34.70985242058479514 ) ) ;
#29367=AXIS2_PLACEMENT_3D ( 'NONE', #46909, #6807, #14915 ) ;
#29369=AXIS2_PLACEMENT_3D ( 'NONE', #31114, #47394, #43199 ) ;
#29370=DIRECTION ( 'NONE',  ( 1.000000000000000000, 0.000000000000000000, 0.000000000000000000 ) ) ;
#29376=ORIENTED_EDGE ( 'NONE', *, *, #3179, .T. ) ;
#29383=CARTESIAN_POINT ( 'NONE',  ( 13.13393739769600010, 18.38381105532060289, -35.14999999999999858 ) ) ;
#29388=CARTESIAN_POINT ( 'NONE',  ( 42.97889992224431666, -37.77457641634045160, -75.42518632368958720 ) ) ;
#29408=DIRECTION ( 'NONE',  ( 1.000000000000000000, 0.000000000000000000, 0.000000000000000000 ) ) ;
#29416=CYLINDRICAL_SURFACE ( 'NONE', #13377, 0.4999999999999982236 ) ;
#29423=VERTEX_POINT ( 'NONE', #19571 ) ;
#29431=EDGE_CURVE ( 'NONE', #43147, #32833, #36675, .T. ) ;
#29432=EDGE_LOOP ( 'NONE', ( #46179, #40398, #13693, #14094, #26401, #15694 ) ) ;
#29434=ORIENTED_EDGE ( 'NONE', *, *, #34150, .F. ) ;
#29438=EDGE_CURVE ( 'NONE', #36069, #26276, #43220, .T. ) ;
#29453=EDGE_CURVE ( 'NONE', #49316, #38190, #31862, .T. ) ;
#29467=( BOUNDED_CURVE ( )  B_SPLINE_CURVE ( 3, ( #25212, #17120, #48309, #4278 ),
 .UNSPECIFIED., .F., .T. ) 
 B_SPLINE_CURVE_WITH_KNOTS ( ( 4, 4 ),
 ( 2.356194490192353719, 3.141592653589795781 ),
 .UNSPECIFIED. ) 
 CURVE ( )  GEOMETRIC_REPRESENTATION_ITEM ( )  RATIONAL_B_SPLINE_CURVE ( ( 1.000000000000000000, 0.9492530216741918991, 0.9492530216741918991, 1.000000000000000000 ) ) 
 REPRESENTATION_ITEM ( '' )  );
#29469=DIRECTION ( 'NONE',  ( -0.3535533905932738974, 0.6123724356957941373, 0.7071067811865477948 ) ) ;
#29470=DIRECTION ( 'NONE',  ( 0.000000000000000000, 0.000000000000000000, -1.000000000000000000 ) ) ;
#29474=CARTESIAN_POINT ( 'NONE',  ( 16.13393739769620083, -15.61618894467929941, -643.2998782751060389 ) ) ;
#29486=CARTESIAN_POINT ( 'NONE',  ( 44.26178562846939002, 8.743315224798376306, -65.39183186454530983 ) ) ;
#29496=EDGE_CURVE ( 'NONE', #27321, #27249, #21052, .T. ) ;
#29498=DIRECTION ( 'NONE',  ( 0.000000000000000000, 0.000000000000000000, 1.000000000000000000 ) ) ;
#29500=ORIENTED_EDGE ( 'NONE', *, *, #6568, .F. ) ;
#29502=ORIENTED_EDGE ( 'NONE', *, *, #51411, .F. ) ;
#29504=CARTESIAN_POINT ( 'NONE',  ( -15.55064706627671356, 7.123802962138601202, -48.59731086643836306 ) ) ;
#29505=CARTESIAN_POINT ( 'NONE',  ( 28.28038400710289935, -8.603434725040973063, -34.79644660940672907 ) ) ;
#29511=CARTESIAN_POINT ( 'NONE',  ( 14.23931515459916319, -32.51455091268737618, -34.84133294386910507 ) ) ;
#29513=EDGE_CURVE ( 'NONE', #38136, #51719, #27936, .T. ) ;
#29524=ORIENTED_EDGE ( 'NONE', *, *, #36610, .T. ) ;
#29540=EDGE_LOOP ( 'NONE', ( #17512, #5866, #16945, #7530 ) ) ;
#29541=CARTESIAN_POINT ( 'NONE',  ( 23.13393739769620083, -2.337132753317950229, -62.14999999999999858 ) ) ;
#29542=CARTESIAN_POINT ( 'NONE',  ( 19.21265657477752598, -49.46974233527256359, -34.79644660940672907 ) ) ;
#29543=DIRECTION ( 'NONE',  ( 0.000000000000000000, 0.000000000000000000, 1.000000000000000000 ) ) ;
#29549=CARTESIAN_POINT ( 'NONE',  ( 0.3209249304026170480, -15.61618894467929941, -35.14999999999999858 ) ) ;
#29550=EDGE_LOOP ( 'NONE', ( #20600, #31829, #3086, #43947 ) ) ;
#29559=CARTESIAN_POINT ( 'NONE',  ( -13.72343451011500015, -40.91412750062520587, -46.69925608350429513 ) ) ;
#29577=ORIENTED_EDGE ( 'NONE', *, *, #38270, .T. ) ;
#29581=B_SPLINE_CURVE_WITH_KNOTS ( 'NONE', 3,
 ( #27437, #8050, #3866, #20088, #43440, #36079, #16164, #7543, #47630, #23487, #3611, #32121, #19581, #31612, #34402, #38355, #33430, #8828, #13034, #29504, #36859, #24515, #28466, #40531, #10323, #9087, #29240, #6392, #24779, #5417, #28987, #13544, #37124, #40788, #20857, #28721, #1480, #33171, #4889, #46235, #41308, #690, #26284 ),
 .UNSPECIFIED., .F., .F.,
 ( 4, 2, 2, 1, 1, 1, 2, 2, 2, 2, 1, 1, 1, 1, 2, 2, 2, 2, 2, 1, 1, 1, 1, 2, 2, 2, 4 ),
 ( 0.000000000000000000, 0.1249999999999913958, 0.1874999999999870937, 0.2187499999999848455, 0.2343749999999837907, 0.2421874999999832079, 0.2460937499999829858, 0.2499999999999827360, 0.3749999999999771849, 0.4374999999999744094, 0.4687499999999731326, 0.4843749999999725220, 0.4921874999999722444, 0.4960937499999720779, 0.4980468749999720224, 0.4999999999999720224, 0.6249999999999749090, 0.6874999999999764633, 0.7187499999999771294, 0.7343749999999775735, 0.7421874999999777955, 0.7460937499999776845, 0.7480468749999776845, 0.7490234374999776845, 0.7499999999999775735, 0.8749999999999887867, 1.000000000000000000 ),
 .UNSPECIFIED. ) ;
#29589=CARTESIAN_POINT ( 'NONE',  ( 29.11414631625610028, -4.499707858305580288, -35.00928286143069812 ) ) ;
#29590=CARTESIAN_POINT ( 'NONE',  ( 18.27002738368036461, -49.61612325953908709, -83.13257468804646066 ) ) ;
#29594=CARTESIAN_POINT ( 'NONE',  ( 46.38238331322911279, -40.25953821574219660, -54.52185312847988286 ) ) ;
#29602=CARTESIAN_POINT ( 'NONE',  ( 16.13393739769620083, -30.04994567442000175, -34.64999999999999858 ) ) ;
#29610=VERTEX_POINT ( 'NONE', #3085 ) ;
#29611=EDGE_CURVE ( 'NONE', #36176, #40719, #1627, .T. ) ;
#29628=VERTEX_POINT ( 'NONE', #28352 ) ;
#29633=EDGE_LOOP ( 'NONE', ( #42483, #14581, #23991, #34065 ) ) ;
#29634=FACE_OUTER_BOUND ( 'NONE', #34305, .T. ) ;
#29635=CARTESIAN_POINT ( 'NONE',  ( 11.63393739769621682, -41.61618894467939356, -35.01561944896766221 ) ) ;
#29637=AXIS2_PLACEMENT_3D ( 'NONE', #7169, #30736, #34928 ) ;
#29639=CARTESIAN_POINT ( 'NONE',  ( 44.28551402523930847, -37.95431502561086035, -68.89210660893036220 ) ) ;
#29640=EDGE_CURVE ( 'NONE', #9028, #51719, #32789, .T. ) ;
#29641=EDGE_LOOP ( 'NONE', ( #29129, #35875, #8975, #40902, #48522, #36130 ) ) ;
#29646=B_SPLINE_CURVE_WITH_KNOTS ( 'NONE', 3,
 ( #46778, #43097, #38651, #19486, #2740, #51469, #50690, #15044 ),
 .UNSPECIFIED., .F., .F.,
 ( 4, 2, 2, 4 ),
 ( -0.1350635247393814631, -0.1243669311585589993, -0.1075965482633170073, -0.1052074838078570079 ),
 .UNSPECIFIED. ) ;
#29651=EDGE_CURVE ( 'NONE', #13682, #25181, #37272, .T. ) ;
#29660=ORIENTED_EDGE ( 'NONE', *, *, #23058, .F. ) ;
#29669=CARTESIAN_POINT ( 'NONE',  ( -10.98055936835113577, -21.27930790530396266, -84.65000000000000568 ) ) ;
#29680=EDGE_CURVE ( 'NONE', #40270, #51808, #49084, .T. ) ;
#29691=CARTESIAN_POINT ( 'NONE',  ( 23.62400244246340009, -48.75656286698960429, -35.12503119152809461 ) ) ;
#29692=VERTEX_POINT ( 'NONE', #25453 ) ;
#29693=CARTESIAN_POINT ( 'NONE',  ( 46.45338246003043992, 6.966592679198189586, -58.05277450657466431 ) ) ;
#29699=EDGE_CURVE ( 'NONE', #21348, #30264, #1373, .T. ) ;
#29706=DIRECTION ( 'NONE',  ( 0.000000000000000000, 0.000000000000000000, 1.000000000000000000 ) ) ;
#29715=EDGE_CURVE ( 'NONE', #23939, #38446, #5573, .T. ) ;
#29719=EDGE_CURVE ( 'NONE', #11933, #45450, #25710, .T. ) ;
#29735=CARTESIAN_POINT ( 'NONE',  ( 44.34764830394051671, 8.750173897780856080, -64.97525299307636715 ) ) ;
#29737=AXIS2_PLACEMENT_3D ( 'NONE', #4724, #12864, #41143 ) ;
#29738=LINE ( 'NONE', #4873, #30151 ) ;
#29742=AXIS2_PLACEMENT_3D ( 'NONE', #18314, #50309, #18579 ) ;
#29743=ORIENTED_EDGE ( 'NONE', *, *, #33998, .T. ) ;
#29746=CARTESIAN_POINT ( 'NONE',  ( -22.83415939270349782, -16.77728946961760670, -54.74109773066948037 ) ) ;
#29747=DIRECTION ( 'NONE',  ( 0.3535533905932799481, 0.6123724356957926940, 0.7071067811865460184 ) ) ;
#29750=DIRECTION ( 'NONE',  ( 0.000000000000000000, 0.000000000000000000, 1.000000000000000000 ) ) ;
#29752=CARTESIAN_POINT ( 'NONE',  ( 16.13393739769620083, -29.64169738395614218, -34.79644660940672907 ) ) ;
#29753=ORIENTED_EDGE ( 'NONE', *, *, #5581, .F. ) ;
#29754=CARTESIAN_POINT ( 'NONE',  ( 0.1457839871805953758, -45.96255801450852374, -34.68167748489142355 ) ) ;
#29756=CARTESIAN_POINT ( 'NONE',  ( 14.28038030992529528, -32.47778390180254604, -34.79644291222909658 ) ) ;
#29759=CARTESIAN_POINT ( 'NONE',  ( 2.434269054290310041, -5.465919710348150495, -34.90839531524139971 ) ) ;
#29769=ORIENTED_EDGE ( 'NONE', *, *, #38654, .F. ) ;
#29776=CARTESIAN_POINT ( 'NONE',  ( -1.839728563314010135, -2.929686987007059873, -54.64999999999999858 ) ) ;
#29780=DIRECTION ( 'NONE',  ( 1.000000000000000000, 0.000000000000000000, 0.000000000000000000 ) ) ;
#29785=CYLINDRICAL_SURFACE ( 'NONE', #9515, 0.4999999999999982236 ) ;
#29792=DIRECTION ( 'NONE',  ( -1.000000000000000000, 0.000000000000000000, 0.000000000000000000 ) ) ;
#29793=DIRECTION ( 'NONE',  ( 0.000000000000000000, 0.000000000000000000, -1.000000000000000000 ) ) ;
#29796=AXIS2_PLACEMENT_3D ( 'NONE', #23794, #43745, #39810 ) ;
#29799=EDGE_LOOP ( 'NONE', ( #49707, #6319, #30907, #38405, #16246 ) ) ;
#29805=VECTOR ( 'NONE', #25068, 1000.000000000000000 ) ;
#29807=CARTESIAN_POINT ( 'NONE',  ( -22.79226920359159791, -13.71770807034589978, -54.60327039117859727 ) ) ;
#29808=AXIS2_PLACEMENT_3D ( 'NONE', #10354, #31271, #30763 ) ;
#29814=VERTEX_POINT ( 'NONE', #10535 ) ;
#29822=CIRCLE ( 'NONE', #29012, 6.999999999999999112 ) ;
#29832=LINE ( 'NONE', #34277, #23104 ) ;
#29833=ORIENTED_EDGE ( 'NONE', *, *, #15270, .F. ) ;
#29840=CYLINDRICAL_SURFACE ( 'NONE', #14721, 0.4999999999999982236 ) ;
#29844=CARTESIAN_POINT ( 'NONE',  ( 47.18591479748049267, -39.34332397330658182, -54.67514754180037784 ) ) ;
#29850=CARTESIAN_POINT ( 'NONE',  ( 47.23550238413793068, 8.041347586024643945, -54.68809082614725980 ) ) ;
#29859=CARTESIAN_POINT ( 'NONE',  ( 16.13393739769620083, -15.61618894467929941, -54.64999999999999858 ) ) ;
#29871=ORIENTED_EDGE ( 'NONE', *, *, #39671, .F. ) ;
#29889=CARTESIAN_POINT ( 'NONE',  ( 0.1375711481827747995, -20.72695808371032200, -34.68474920830817609 ) ) ;
#29890=CARTESIAN_POINT ( 'NONE',  ( 44.10600500027882021, -37.93128479403036835, -69.78959966447122554 ) ) ;
#29892=CARTESIAN_POINT ( 'NONE',  ( 18.13393739769619728, -45.61618894467940066, -35.14999999999999858 ) ) ;
#29898=EDGE_CURVE ( 'NONE', #21076, #50035, #31758, .T. ) ;
#29900=EDGE_CURVE ( 'NONE', #15981, #46925, #29832, .T. ) ;
#29903=ADVANCED_FACE ( 'NONE', ( #21971 ), #50300, .T. ) ;
#29909=CARTESIAN_POINT ( 'NONE',  ( 46.63393739769619373, -39.11086919362080039, -34.64999999999999858 ) ) ;
#29915=AXIS2_PLACEMENT_3D ( 'NONE', #36105, #28228, #44230 ) ;
#29921=CARTESIAN_POINT ( 'NONE',  ( 4.133937397696209715, -8.687985714403829718, -35.14999999999999858 ) ) ;
#29922=SPHERICAL_SURFACE ( 'NONE', #20040, 3.000000000000000000 ) ;
#29924=CIRCLE ( 'NONE', #48351, 22.00000000000000000 ) ;
#29929=CARTESIAN_POINT ( 'NONE',  ( 18.13393739769620083, -32.61307204591476250, -35.10658870008960974 ) ) ;
#29935=ORIENTED_EDGE ( 'NONE', *, *, #47508, .F. ) ;
#29936=B_SPLINE_CURVE_WITH_KNOTS ( 'NONE', 3,
 ( #50150, #2445, #30217, #37569, #1677, #41763, #10059, #45964, #46494, #14247, #6645, #18428, #45448, #38354, #5867, #18173, #26019, #21834, #29693, #42032, #42291, #9550, #22607, #45703, #46234, #30473, #6390, #37841, #29951, #25501, #6131, #10322, #49897, #22088, #21572, #5618, #10583, #1934, #26540, #17664, #38101, #13992, #49648, #13739, #9805, #25753, #17916, #33886, #34140, #22350, #34401, #50417, #42554, #19719, #19200, #39388, #15788, #34924, #15539, #39136, #23627, #42815, #47265, #31491, #23118, #23365, #47516, #43069, #51694, #38881, #18687, #11101, #47770, #7931, #31746, #39643, #11353, #11876, #10839, #35710, #27832, #50667, #43831, #26803, #3749, #11611, #15020, #34661, #27575, #30987, #43579, #3228, #3492, #2970, #15283, #38623, #7680, #18944, #35185, #51188, #2714, #50923, #47013, #14762, #27064, #30731, #43325, #31237, #46757, #7165, #6911, #27318, #22860, #7419, #19460, #35445, #51443, #20736, #24913, #827, #8188, #24130, #36723, #20219, #40925, #8448, #24394, #33043, #40408, #4766, #16299, #4249, #39904, #74, #36460, #44866, #36996, #5037, #16047, #45121, #32255, #44599, #4502, #8704, #49068, #8969 ),
 .UNSPECIFIED., .F., .F.,
 ( 4, 2, 2, 2, 2, 2, 2, 2, 1, 2, 2, 2, 2, 2, 2, 2, 2, 1, 2, 2, 2, 2, 2, 2, 2, 2, 2, 1, 2, 2, 2, 2, 2, 2, 2, 2, 2, 2, 2, 2, 2, 2, 2, 2, 2, 2, 2, 2, 1, 2, 2, 2, 2, 1, 1, 2, 2, 2, 2, 2, 1, 1, 2, 2, 2, 2, 1, 2, 2, 2, 2, 2, 2, 2, 1, 2, 2, 4 ),
 ( 0.000000000000000000, 0.03125000000001593170, 0.04687500000002425837, 0.05468750000002842171, 0.05859375000003026746, 0.06250000000003211320, 0.09375000000004794776, 0.1093750000000559414, 0.1171875000000599382, 0.1210937500000619366, 0.1250000000000639211, 0.1562500000000854872, 0.1718750000000967004, 0.1796875000001026401, 0.1875000000001085521, 0.2187500000001322553, 0.2343750000001444678, 0.2421875000001501577, 0.2460937500001528777, 0.2500000000001555978, 0.2812500000001789124, 0.2968750000001905143, 0.3046875000001968981, 0.3085937500002001177, 0.3125000000002033373, 0.3437500000002295386, 0.3593750000002427503, 0.3671875000002494116, 0.3710937500002527423, 0.3750000000002560729, 0.4062500000002683964, 0.4218750000002753353, 0.4296875000002787215, 0.4335937500002811085, 0.4375000000002834954, 0.4687500000002967626, 0.4843750000003033684, 0.4921875000003056999, 0.5000000000003080869, 0.5312500000003175238, 0.5468750000003227418, 0.5625000000003280709, 0.5937500000003388401, 0.6093750000003441691, 0.6250000000003496092, 0.6562500000003629319, 0.6718750000003695932, 0.6796875000003735900, 0.6835937500003755884, 0.6855468750003766987, 0.6875000000003778089, 0.7187500000003954614, 0.7343750000004034550, 0.7421875000004075629, 0.7460937500004085621, 0.7480468750004091172, 0.7500000000004096723, 0.7812500000003940182, 0.7968750000003855805, 0.8046875000003813616, 0.8085937500003786971, 0.8105468750003768097, 0.8115234375003753664, 0.8125000000003738121, 0.8437500000003221867, 0.8593750000002956524, 0.8671875000002816636, 0.8710937500002746692, 0.8730468750002721157, 0.8740234375002708944, 0.8750000000002695622, 0.9062500000001992850, 0.9218750000001649791, 0.9296875000001472156, 0.9335937500001383338, 0.9355468750001344480, 0.9375000000001305622, 1.000000000000000000 ),
 .UNSPECIFIED. ) ;
#29951=CARTESIAN_POINT ( 'NONE',  ( 46.02161178372806916, 6.923385635729644605, -60.21157151071680858 ) ) ;
#29956=DIRECTION ( 'NONE',  ( 0.000000000000000000, 0.000000000000000000, -1.000000000000000000 ) ) ;
#29957=CARTESIAN_POINT ( 'NONE',  ( 16.13393739769620083, -15.61618894467929941, -54.64999999999999858 ) ) ;
#29960=AXIS2_PLACEMENT_3D ( 'NONE', #10775, #50351, #38291 ) ;
#29962=CARTESIAN_POINT ( 'NONE',  ( 30.13393739769619728, 7.383811055320659733, -84.65000000000000568 ) ) ;
#29967=ADVANCED_FACE ( 'NONE', ( #10720 ), #2079, .T. ) ;
#29969=ORIENTED_EDGE ( 'NONE', *, *, #17194, .F. ) ;
#29972=CYLINDRICAL_SURFACE ( 'NONE', #24485, 0.4999999999999980571 ) ;
#29979=CARTESIAN_POINT ( 'NONE',  ( 9.895693118437540292, -53.60956520270919867, -34.65000333313919612 ) ) ;
#29983=EDGE_CURVE ( 'NONE', #29692, #11865, #6527, .T. ) ;
#29987=VERTEX_POINT ( 'NONE', #17546 ) ;
#29991=VECTOR ( 'NONE', #48873, 1000.000000000000000 ) ;
#29993=CARTESIAN_POINT ( 'NONE',  ( 43.85570627947347333, 8.710526304754909077, -67.35765774891521573 ) ) ;
#29998=ORIENTED_EDGE ( 'NONE', *, *, #3366, .T. ) ;
#30003=CARTESIAN_POINT ( 'NONE',  ( 17.89246938939507103, 10.62527906362202756, -34.70142521051214857 ) ) ;
#30004=DIRECTION ( 'NONE',  ( -0.8660254037844390407, -0.4999999999999995004, -5.551115123125774074E-17 ) ) ;
#30006=EDGE_LOOP ( 'NONE', ( #49987, #48661, #33691, #28928 ) ) ;
#30009=ADVANCED_FACE ( 'NONE', ( #38239 ), #2332, .T. ) ;
#30026=AXIS2_PLACEMENT_3D ( 'NONE', #9730, #46683, #50347 ) ;
#30027=CARTESIAN_POINT ( 'NONE',  ( 11.63393739769600010, 10.38381105532060111, -35.14999999999999858 ) ) ;
#30028=EDGE_CURVE ( 'NONE', #40719, #42065, #16315, .T. ) ;
#30033=CARTESIAN_POINT ( 'NONE',  ( 29.13393739769619728, -33.11618894467940066, -53.85091742636659973 ) ) ;
#30034=FACE_OUTER_BOUND ( 'NONE', #28940, .T. ) ;
#30043=VERTEX_POINT ( 'NONE', #47149 ) ;
#30050=CARTESIAN_POINT ( 'NONE',  ( 19.26373325286787974, -49.37472093637801862, -34.70142521051216988 ) ) ;
#30054=LINE ( 'NONE', #34241, #21414 ) ;
#30056=EDGE_LOOP ( 'NONE', ( #48395, #619, #26013, #19774 ) ) ;
#30064=EDGE_CURVE ( 'NONE', #46545, #23421, #42366, .T. ) ;
#30067=CARTESIAN_POINT ( 'NONE',  ( -1.534588559015300113, -50.44432100765110505, -36.31182994165819622 ) ) ;
#30074=EDGE_CURVE ( 'NONE', #15142, #12924, #39397, .T. ) ;
#30076=( BOUNDED_CURVE ( )  B_SPLINE_CURVE ( 3, ( #12584, #3954, #28547, #8393 ),
 .UNSPECIFIED., .F., .T. ) 
 B_SPLINE_CURVE_WITH_KNOTS ( ( 4, 4 ),
 ( 1.570796326794903441, 2.356194490192073943 ),
 .UNSPECIFIED. ) 
 CURVE ( )  GEOMETRIC_REPRESENTATION_ITEM ( )  RATIONAL_B_SPLINE_CURVE ( ( 1.000000000000000000, 0.9492530216742265381, 0.9492530216742265381, 1.000000000000000000 ) ) 
 REPRESENTATION_ITEM ( '' )  );
#30087=EDGE_LOOP ( 'NONE', ( #49898, #1631, #9451, #23513, #51043, #44303, #33800, #9147, #50915, #49043, #13434, #5395, #34278, #38783, #6633, #14629, #39138, #10235, #4479, #3597, #48330, #21005, #23354 ) ) ;
#30093=EDGE_CURVE ( 'NONE', #48924, #336, #14900, .T. ) ;
#30097=AXIS2_PLACEMENT_3D ( 'NONE', #25561, #41567, #42089 ) ;
#30100=CIRCLE ( 'NONE', #26779, 3.000000000000000888 ) ;
#30102=CARTESIAN_POINT ( 'NONE',  ( 28.90964706005130225, -4.575559556054879629, -34.73148477628539865 ) ) ;
#30104=AXIS2_PLACEMENT_3D ( 'NONE', #36000, #117, #32049 ) ;
#30107=CARTESIAN_POINT ( 'NONE',  ( 0.01417123839112280001, 19.49180391766380183, -34.75417992180849325 ) ) ;
#30109=CARTESIAN_POINT ( 'NONE',  ( 42.10077372231668846, -38.84036518154631068, -79.87212092322644708 ) ) ;
#30111=CYLINDRICAL_SURFACE ( 'NONE', #6791, 0.4999999999999994449 ) ;
#30113=EDGE_LOOP ( 'NONE', ( #13422, #2770, #48322, #42866 ) ) ;
#30116=CARTESIAN_POINT ( 'NONE',  ( 72.07723754518156056, -8.533442488085691835, -19.87883576049206980 ) ) ;
#30125=B_SPLINE_CURVE_WITH_KNOTS ( 'NONE', 3,
 ( #31303, #47583, #34986, #46817, #50986, #35776, #11163, #3557, #43899, #7994, #39966, #47332, #4061, #43648, #20027, #3815, #3292 ),
 .UNSPECIFIED., .F., .F.,
 ( 4, 2, 1, 1, 1, 1, 1, 1, 1, 2, 2, 4 ),
 ( 0.000000000000000000, 0.2499999999999136246, 0.3749999999998709921, 0.4374999999998502309, 0.4687499999998397948, 0.4843749999998340217, 0.4921874999998305800, 0.4960937499998287481, 0.4980468749998278599, 0.4990234374998280265, 0.4999999999998281375, 1.000000000000000000 ),
 .UNSPECIFIED. ) ;
#30149=DIRECTION ( 'NONE',  ( 0.000000000000000000, 0.000000000000000000, -1.000000000000000000 ) ) ;
#30150=CARTESIAN_POINT ( 'NONE',  ( 29.13393739769619728, -33.11618894467940066, -34.64999999999999858 ) ) ;
#30151=VECTOR ( 'NONE', #41033, 1000.000000000000000 ) ;
#30158=CARTESIAN_POINT ( 'NONE',  ( 45.39015875754859053, -38.08747578716207727, -63.36883525997365041 ) ) ;
#30162=FACE_OUTER_BOUND ( 'NONE', #4060, .T. ) ;
#30177=CARTESIAN_POINT ( 'NONE',  ( 40.79482532997379707, -39.62505393422780031, -82.14319696191608955 ) ) ;
#30189=VECTOR ( 'NONE', #22476, 1000.000000000000000 ) ;
#30199=CARTESIAN_POINT ( 'NONE',  ( 18.12828521207214294, -32.60348064536626822, -35.06583844469491851 ) ) ;
#30202=CARTESIAN_POINT ( 'NONE',  ( 3.633937397696210159, -19.08029055981709732, -35.14999999999999858 ) ) ;
#30217=CARTESIAN_POINT ( 'NONE',  ( 47.04596872651796247, 7.021586061845817461, -55.08983903758259260 ) ) ;
#30222=CARTESIAN_POINT ( 'NONE',  ( 16.13393739769620083, -29.47259540523039689, -35.14999999999999858 ) ) ;
#30225=LINE ( 'NONE', #41772, #18294 ) ;
#30246=CARTESIAN_POINT ( 'NONE',  ( 17.25678305769729803, 12.72875286183739973, -62.64999999999999858 ) ) ;
#30254=EDGE_LOOP ( 'NONE', ( #2372, #42873, #37622, #18227 ) ) ;
#30257=DIRECTION ( 'NONE',  ( -0.000000000000000000, 1.000000000000000000, 0.000000000000000000 ) ) ;
#30264=VERTEX_POINT ( 'NONE', #456 ) ;
#30265=EDGE_LOOP ( 'NONE', ( #21317, #8962, #17282, #42647 ) ) ;
#30268=CARTESIAN_POINT ( 'NONE',  ( -22.62439110747796889, -19.95374504816285466, -54.65132778005098402 ) ) ;
#30269=CARTESIAN_POINT ( 'NONE',  ( -18.93711747768801956, -32.99710777797167083, -51.50532171058987529 ) ) ;
#30276=DIRECTION ( 'NONE',  ( 0.8660254037844387076, -0.4999999999999998890, 0.000000000000000000 ) ) ;
#30281=EDGE_CURVE ( 'NONE', #336, #24767, #15106, .T. ) ;
#30292=CARTESIAN_POINT ( 'NONE',  ( 46.60156948537970578, 8.729780378598791302, -54.61635207866100217 ) ) ;
#30293=CARTESIAN_POINT ( 'NONE',  ( 11.66815189201653347, 10.43523626583280617, -34.89146800830119588 ) ) ;
#30297=CARTESIAN_POINT ( 'NONE',  ( 44.75408132727028487, -40.01302229878363903, -63.00536423570013511 ) ) ;
#30299=DIRECTION ( 'NONE',  ( 1.000000000000000000, 0.000000000000000000, 0.000000000000000000 ) ) ;
#30312=DIRECTION ( 'NONE',  ( -0.4107275965530814421, -0.9117581046690669266, 0.000000000000000000 ) ) ;
#30313=CARTESIAN_POINT ( 'NONE',  ( 46.99244837402765285, 8.000249783914572532, -34.80140398659610668 ) ) ;
#30321=EDGE_LOOP ( 'NONE', ( #2028, #32716, #25635, #18512 ) ) ;
#30326=LINE ( 'NONE', #13342, #20824 ) ;
#30331=CARTESIAN_POINT ( 'NONE',  ( -1.533723836532590035, -50.07764524056720035, -36.10017410556069706 ) ) ;
#30341=EDGE_LOOP ( 'NONE', ( #41249, #1790, #14494, #6505 ) ) ;
#30342=CARTESIAN_POINT ( 'NONE',  ( 30.13393739769619728, -38.61618894467930119, -59.64999999999999147 ) ) ;
#30352=ORIENTED_EDGE ( 'NONE', *, *, #265, .T. ) ;
#30356=AXIS2_PLACEMENT_3D ( 'NONE', #19490, #47544, #4029 ) ;
#30358=AXIS2_PLACEMENT_3D ( 'NONE', #49397, #48876, #5368 ) ;
#30359=CARTESIAN_POINT ( 'NONE',  ( 28.78179405415149716, -4.623252633501089726, -34.67096478998279707 ) ) ;
#30360=EDGE_CURVE ( 'NONE', #218, #21076, #29263, .T. ) ;
#30364=CARTESIAN_POINT ( 'NONE',  ( 0.2860235532455480123, 19.98438480351800095, -34.73917836322149810 ) ) ;
#30366=CARTESIAN_POINT ( 'NONE',  ( 42.54838292251218235, -38.91056855093247435, -77.63407492224945372 ) ) ;
#30374=CARTESIAN_POINT ( 'NONE',  ( 44.13393739769620083, -33.11618894467940066, -54.35294145922159714 ) ) ;
#30381=CARTESIAN_POINT ( 'NONE',  ( 15.01109173769499883, -43.96113075119600211, -62.64999999999999858 ) ) ;
#30389=( BOUNDED_CURVE ( )  B_SPLINE_CURVE ( 3, ( #24081, #48225, #24, #51646 ),
 .UNSPECIFIED., .F., .T. ) 
 B_SPLINE_CURVE_WITH_KNOTS ( ( 4, 4 ),
 ( 5.070260775219138871, 5.428132570053650241 ),
 .UNSPECIFIED. ) 
 CURVE ( )  GEOMETRIC_REPRESENTATION_ITEM ( )  RATIONAL_B_SPLINE_CURVE ( ( 1.000000000000000000, 0.9893557610490316678, 0.9893557610490316678, 1.000000000000000000 ) ) 
 REPRESENTATION_ITEM ( '' )  );
#30398=ORIENTED_EDGE ( 'NONE', *, *, #16005, .T. ) ;
#30405=VERTEX_POINT ( 'NONE', #13809 ) ;
#30406=CIRCLE ( 'NONE', #37118, 2.999999999999999112 ) ;
#30410=CARTESIAN_POINT ( 'NONE',  ( 17.73647699123689847, -32.25138633525569531, -34.65800258959610147 ) ) ;
#30413=CARTESIAN_POINT ( 'NONE',  ( 45.02782540735238115, -38.04571132974656678, -65.18055859578058175 ) ) ;
#30415=CARTESIAN_POINT ( 'NONE',  ( -22.72558660355269566, -12.37859355894351410, -54.68545204612530597 ) ) ;
#30419=AXIS2_PLACEMENT_3D ( 'NONE', #48708, #29543, #28766 ) ;
#30431=CARTESIAN_POINT ( 'NONE',  ( 41.61216686777694918, -39.72206404522755463, -78.20190362087095082 ) ) ;
#30432=VECTOR ( 'NONE', #40201, 1000.000000000000000 ) ;
#30434=DIRECTION ( 'NONE',  ( 0.8204012560548787913, -0.5717882292104107256, 0.000000000000000000 ) ) ;
#30435=EDGE_CURVE ( 'NONE', #45483, #34982, #6906, .T. ) ;
#30447=LINE ( 'NONE', #46469, #49303 ) ;
#30453=CARTESIAN_POINT ( 'NONE',  ( 18.11900864776890074, -32.59522544870679894, -35.02873218748179340 ) ) ;
#30458=ORIENTED_EDGE ( 'NONE', *, *, #37214, .F. ) ;
#30463=CARTESIAN_POINT ( 'NONE',  ( 16.13393739769620083, -15.61618894467929941, -54.64999999999999858 ) ) ;
#30464=EDGE_CURVE ( 'NONE', #32888, #23485, #5902, .T. ) ;
#30473=CARTESIAN_POINT ( 'NONE',  ( 46.17257466001858290, 6.938700589869487345, -59.45676296270231376 ) ) ;
#30475=ORIENTED_EDGE ( 'NONE', *, *, #45140, .T. ) ;
#30499=DIRECTION ( 'NONE',  ( 0.8660254037844390407, 0.4999999999999995004, 2.775557561562887037E-17 ) ) ;
#30509=CARTESIAN_POINT ( 'NONE',  ( 20.59972290337569589, -41.66761415519157197, -34.89146800830128825 ) ) ;
#30521=ORIENTED_EDGE ( 'NONE', *, *, #42522, .T. ) ;
#30525=DIRECTION ( 'NONE',  ( -0.8090169943749471182, 0.5877852522924732481, 0.000000000000000000 ) ) ;
#30528=ORIENTED_EDGE ( 'NONE', *, *, #48396, .F. ) ;
#30531=AXIS2_PLACEMENT_3D ( 'NONE', #31688, #33508, #13866 ) ;
#30533=EDGE_LOOP ( 'NONE', ( #15345, #6876, #30770, #23602, #35237 ) ) ;
#30542=B_SPLINE_CURVE_WITH_KNOTS ( 'NONE', 3,
 ( #17572, #2625, #6550, #50324, #33795, #25923, #14410, #21738, #25668, #22517, #18597, #33541, #13897, #41670, #49559, #38526, #46140, #18079, #10231, #13646, #37745, #1843, #2103, #17821, #49804 ),
 .UNSPECIFIED., .F., .F.,
 ( 4, 3, 3, 3, 3, 3, 3, 3, 4 ),
 ( -0.1626565276727789944, -0.1623185391170249847, -0.1505729783072729810, -0.1388990119013250035, -0.1281439427408750109, -0.1186168937590759975, -0.1079791825846370124, -0.09959263459902399640, -0.09350866753172300261 ),
 .UNSPECIFIED. ) ;
#30552=CARTESIAN_POINT ( 'NONE',  ( 44.97387785896593471, -40.02856819528950183, -61.94005888394004700 ) ) ;
#30555=EDGE_CURVE ( 'NONE', #18232, #24151, #38701, .T. ) ;
#30560=AXIS2_PLACEMENT_3D ( 'NONE', #35659, #4194, #48481 ) ;
#30563=LINE ( 'NONE', #25337, #331 ) ;
#30567=ORIENTED_EDGE ( 'NONE', *, *, #19045, .F. ) ;
#30572=CARTESIAN_POINT ( 'NONE',  ( 14.32489919860654304, 1.205480371600849532, -34.75586992539665943 ) ) ;
#30575=CARTESIAN_POINT ( 'NONE',  ( 0.4420762188774020052, -22.38822566875639808, -35.01387690002259490 ) ) ;
#30583=ORIENTED_EDGE ( 'NONE', *, *, #32218, .F. ) ;
#30596=ORIENTED_EDGE ( 'NONE', *, *, #38281, .T. ) ;
#30602=EDGE_CURVE ( 'NONE', #32056, #16369, #35784, .T. ) ;
#30612=CARTESIAN_POINT ( 'NONE',  ( 13.05521822061487214, -49.46974233527257780, -34.79644660940672907 ) ) ;
#30624=CARTESIAN_POINT ( 'NONE',  ( -21.19111549538119732, -3.902638417377439772, -53.38966602606979706 ) ) ;
#30632=CARTESIAN_POINT ( 'NONE',  ( 46.37902371098480359, 9.012179193705595281, -54.60036856012990825 ) ) ;
#30653=CARTESIAN_POINT ( 'NONE',  ( 44.08684091409431005, -33.11618894467930119, -54.64999999999999858 ) ) ;
#30656=AXIS2_PLACEMENT_3D ( 'NONE', #37869, #50691, #25527 ) ;
#30658=VERTEX_POINT ( 'NONE', #42628 ) ;
#30659=DIRECTION ( 'NONE',  ( 0.6918010270571950393, -0.3994115091971360276, 0.6015661104845220208 ) ) ;
#30662=ORIENTED_EDGE ( 'NONE', *, *, #51047, .T. ) ;
#30665=VECTOR ( 'NONE', #45858, 1000.000000000000000 ) ;
#30667=CARTESIAN_POINT ( 'NONE',  ( 17.83125332364289761, -32.33724466207230108, -34.68801049095930011 ) ) ;
#30670=EDGE_CURVE ( 'NONE', #15778, #48656, #7494, .T. ) ;
#30672=CARTESIAN_POINT ( 'NONE',  ( 43.57164778298420060, -37.85903016011967281, -72.46142985655266955 ) ) ;
#30675=DIRECTION ( 'NONE',  ( 0.000000000000000000, -1.000000000000000000, 0.000000000000000000 ) ) ;
#30685=EDGE_CURVE ( 'NONE', #16602, #2647, #46829, .T. ) ;
#30694=CARTESIAN_POINT ( 'NONE',  ( 41.86875520594507094, -39.75028450918884459, -76.96502288003935632 ) ) ;
#30698=( BOUNDED_CURVE ( )  B_SPLINE_CURVE ( 3, ( #43805, #35930, #19694, #7905 ),
 .UNSPECIFIED., .F., .T. ) 
 B_SPLINE_CURVE_WITH_KNOTS ( ( 4, 4 ),
 ( 4.712388980384689674, 5.070260775219133542 ),
 .UNSPECIFIED. ) 
 CURVE ( )  GEOMETRIC_REPRESENTATION_ITEM ( )  RATIONAL_B_SPLINE_CURVE ( ( 1.000000000000000000, 0.9893557610490356646, 0.9893557610490356646, 1.000000000000000000 ) ) 
 REPRESENTATION_ITEM ( '' )  );
#30703=CARTESIAN_POINT ( 'NONE',  ( 20.59972290337550049, 10.43523626583286656, -34.89146800830130246 ) ) ;
#30730=DIRECTION ( 'NONE',  ( -1.000000000000000000, 0.000000000000000000, 0.000000000000000000 ) ) ;
#30731=CARTESIAN_POINT ( 'NONE',  ( 43.00066473404336165, 6.545556978096114698, -75.31636325171257340 ) ) ;
#30736=DIRECTION ( 'NONE',  ( 0.000000000000000000, 0.000000000000000000, -1.000000000000000000 ) ) ;
#30744=DIRECTION ( 'NONE',  ( 0.000000000000000000, 0.000000000000000000, -1.000000000000000000 ) ) ;
#30749=ORIENTED_EDGE ( 'NONE', *, *, #40241, .T. ) ;
#30753=AXIS2_PLACEMENT_3D ( 'NONE', #12216, #11710, #11970 ) ;
#30762=CARTESIAN_POINT ( 'NONE',  ( -0.1295185695942999982, 0.6472670226113349523, -84.65000000000000568 ) ) ;
#30763=DIRECTION ( 'NONE',  ( 0.5215975411497816294, -0.8522221556268643194, 0.04066205264374356254 ) ) ;
#30766=CARTESIAN_POINT ( 'NONE',  ( 20.53650276133985031, -41.76263555408612405, -34.79644660940672907 ) ) ;
#30767=ORIENTED_EDGE ( 'NONE', *, *, #10659, .T. ) ;
#30770=ORIENTED_EDGE ( 'NONE', *, *, #46447, .F. ) ;
#30771=CARTESIAN_POINT ( 'NONE',  ( -1.839728563314089849, -28.30269090235150031, -54.64999999999999858 ) ) ;
#30772=DIRECTION ( 'NONE',  ( 0.5835456732599411112, 0.8120803206700689669, 0.000000000000000000 ) ) ;
#30780=CARTESIAN_POINT ( 'NONE',  ( 29.13393739769619728, -4.468739684871080087, -35.14999999999999858 ) ) ;
#30782=CARTESIAN_POINT ( 'NONE',  ( -5.815486204891447741, -48.02745134462772825, -40.24138896526777387 ) ) ;
#30790=DIRECTION ( 'NONE',  ( 0.000000000000000000, -1.000000000000000000, 0.000000000000000000 ) ) ;
#30809=CARTESIAN_POINT ( 'NONE',  ( 46.12656867617091905, -40.10072528304355899, -56.34446073384248166 ) ) ;
#30819=ORIENTED_EDGE ( 'NONE', *, *, #917, .T. ) ;
#30827=CARTESIAN_POINT ( 'NONE',  ( 44.13393739769620083, -33.11618894467930829, -54.27132075603720551 ) ) ;
#30828=CARTESIAN_POINT ( 'NONE',  ( 8.643744238043529649, 17.52287609088129727, -35.14999999999999858 ) ) ;
#30832=CARTESIAN_POINT ( 'NONE',  ( 18.13393739769620083, -32.62399965035220362, -35.14999999999999858 ) ) ;
#30837=DIRECTION ( 'NONE',  ( -0.3487035033511789450, 0.9372330909387559528, 0.000000000000000000 ) ) ;
#30845=DIRECTION ( 'NONE',  ( 0.000000000000000000, 0.000000000000000000, 1.000000000000000000 ) ) ;
#30852=ORIENTED_EDGE ( 'NONE', *, *, #50302, .F. ) ;
#30856=AXIS2_PLACEMENT_3D ( 'NONE', #25945, #10251, #38549 ) ;
#30865=CARTESIAN_POINT ( 'NONE',  ( 46.60111831227250434, -39.96272243613920239, -54.61658773935999989 ) ) ;
#30871=CARTESIAN_POINT ( 'NONE',  ( 23.53669455186048864, 17.69319178430572137, -34.79644561402099612 ) ) ;
#30876=CARTESIAN_POINT ( 'NONE',  ( -21.18743422985509994, -3.890487093983819644, -53.43809524694220414 ) ) ;
#30886=CARTESIAN_POINT ( 'NONE',  ( 46.39209508087989775, 9.012977385794867402, -54.53647718218035578 ) ) ;
#30895=EDGE_LOOP ( 'NONE', ( #19709, #40460, #37603, #46978, #36260, #38941 ) ) ;
#30897=ORIENTED_EDGE ( 'NONE', *, *, #32662, .F. ) ;
#30905=ORIENTED_EDGE ( 'NONE', *, *, #18638, .F. ) ;
#30907=ORIENTED_EDGE ( 'NONE', *, *, #36227, .T. ) ;
#30909=EDGE_CURVE ( 'NONE', #20523, #11224, #45716, .T. ) ;
#30916=EDGE_CURVE ( 'NONE', #50655, #47312, #50938, .T. ) ;
#30921=EDGE_CURVE ( 'NONE', #18539, #23485, #34050, .T. ) ;
#30924=CARTESIAN_POINT ( 'NONE',  ( 46.17549598699994107, -38.17137574164103597, -59.44215122485496039 ) ) ;
#30925=ORIENTED_EDGE ( 'NONE', *, *, #23312, .F. ) ;
#30926=ORIENTED_EDGE ( 'NONE', *, *, #14274, .F. ) ;
#30933=AXIS2_PLACEMENT_3D ( 'NONE', #293, #49300, #12610 ) ;
#30937=CARTESIAN_POINT ( 'NONE',  ( 0.03729862092324889855, 14.54995912156149984, -34.73403371893299862 ) ) ;
#30957=FACE_OUTER_BOUND ( 'NONE', #32316, .T. ) ;
#30958=DIRECTION ( 'NONE',  ( 0.000000000000000000, 1.000000000000000000, 0.000000000000000000 ) ) ;
#30960=CARTESIAN_POINT ( 'NONE',  ( 13.00414154252432120, 18.14234304701931322, -34.70142521051216278 ) ) ;
#30961=CIRCLE ( 'NONE', #26776, 0.5000000000000004441 ) ;
#30973=DIRECTION ( 'NONE',  ( 0.3863301728269200042, -0.9223605572462009183, 0.000000000000000000 ) ) ;
#30976=B_SPLINE_CURVE_WITH_KNOTS ( 'NONE', 3,
 ( #23215, #18787, #46854, #10942, #3078, #36836, #24761, #8809, #36308, #28185, #24496, #35811, #23981, #8286, #40771, #20319, #15897, #36061, #4872, #12477, #11976, #48381, #43681, #40514, #23731, #51794, #4093, #3849, #44187, #11716, #27680, #20577, #7781, #48123, #32104, #12222, #673, #39747, #27931, #19823, #48647, #418, #168, #40005, #43933, #24234, #40259, #20839, #4351, #28445, #31854, #47873, #8030, #16662, #20067, #16405, #941, #16937, #44704, #32362, #47615, #44447, #8553, #4603, #16145, #36570, #32619, #12747, #28702, #1459, #33414, #33926, #28967, #38141, #5147, #45491, #41290, #13781, #49432, #14034, #10106, #9589, #32881, #45751, #49943, #5400, #29224, #42073, #2241, #21101, #13529, #9339, #29993, #49687, #21357, #33672, #25543, #48915, #13269, #13012, #1720, #46015, #29486, #26066, #9845, #6175, #21877, #37360, #29735, #37887, #22134, #17958, #41547, #44966, #17449, #25798, #5663, #21610, #41806, #37614, #1201, #17704, #9069, #25017, #17193, #41031, #5912, #1979, #37104, #45231, #33150, #49177, #25286, #51239, #50710, #18988, #38925, #23162, #42600, #31283, #27113, #38674, #14809, #50459, #50200, #2759, #7466, #39179, #10629, #14292, #42337, #6436, #22654, #11404, #26328, #23419, #34182, #2498, #43116, #15065, #27366, #35232, #47316, #22395, #11143, #19250 ),
 .UNSPECIFIED., .F., .F.,
 ( 4, 2, 2, 2, 2, 1, 1, 2, 2, 2, 2, 1, 1, 1, 2, 2, 2, 2, 1, 1, 1, 2, 2, 2, 2, 1, 1, 1, 2, 2, 2, 2, 1, 1, 1, 2, 2, 2, 2, 1, 1, 2, 2, 2, 2, 1, 1, 2, 2, 2, 2, 1, 1, 2, 2, 2, 2, 1, 1, 2, 2, 2, 2, 1, 1, 2, 2, 2, 2, 1, 1, 2, 2, 2, 2, 1, 1, 1, 2, 2, 2, 2, 1, 1, 1, 2, 2, 2, 2, 1, 1, 1, 2, 2, 2, 2, 1, 1, 1, 2, 2, 4 ),
 ( 0.000000000000000000, 0.007812499999983147161, 0.01562499999996629432, 0.03124999999993430255, 0.04687499999990230731, 0.05468749999988631316, 0.05859374999987772281, 0.06054687499987279620, 0.06249999999986786958, 0.09374999999980140886, 0.1093749999997681993, 0.1171874999997514766, 0.1210937499997431221, 0.1230468749997389588, 0.1240234374997369882, 0.1249999999997350175, 0.1562499999996768141, 0.1718749999996477262, 0.1796874999996338484, 0.1835937499996276034, 0.1855468749996250499, 0.1865234374996244116, 0.1874999999996237732, 0.2187499999995946853, 0.2343749999995808353, 0.2421874999995740352, 0.2460937499995706490, 0.2480468749995677347, 0.2490234374995661526, 0.2499999999995645705, 0.2812499999995325406, 0.2968749999995165534, 0.3046874999995086153, 0.3085937499995046185, 0.3105468749995026201, 0.3115234374995022315, 0.3124999999995018429, 0.3437499999994832467, 0.3593749999994740318, 0.3671874999994684807, 0.3710937499994668154, 0.3730468749994660937, 0.3749999999994653721, 0.4062499999994700350, 0.4218749999994716449, 0.4296874999994724775, 0.4335937499994735878, 0.4355468749994740874, 0.4374999999994745870, 0.4687499999994834132, 0.4843749999994878541, 0.4921874999994891864, 0.4960937499994897415, 0.4980468749994909627, 0.4999999999994921840, 0.5312499999995180522, 0.5468749999995308197, 0.5546874999995378142, 0.5585937499995413669, 0.5605468749995424771, 0.5624999999995435873, 0.5937499999995519140, 0.6093749999995561328, 0.6171874999995581312, 0.6210937499995600186, 0.6230468749995621280, 0.6249999999995642375, 0.6562499999995939914, 0.6718749999996094235, 0.6796874999996179723, 0.6835937499996220801, 0.6855468749996240785, 0.6874999999996260769, 0.7187499999996537214, 0.7343749999996674882, 0.7421874999996742606, 0.7460937499996777023, 0.7480468749996793676, 0.7490234374996802558, 0.7499999999996811439, 0.7812499999997200018, 0.7968749999997398747, 0.8046874999997497557, 0.8085937499997547517, 0.8105468749997569722, 0.8115234374997581934, 0.8124999999997594147, 0.8437499999997956079, 0.8593749999998133715, 0.8671874999998223643, 0.8710937499998268052, 0.8730468749998290257, 0.8740234374998301359, 0.8749999999998312461, 0.9062499999998698819, 0.9218749999998896438, 0.9296874999998994138, 0.9335937499999042988, 0.9355468749999069633, 0.9365234374999084066, 0.9374999999999098499, 1.000000000000000000 ),
 .UNSPECIFIED. ) ;
#30979=EDGE_LOOP ( 'NONE', ( #39567, #42614, #48255, #9 ) ) ;
#30984=CYLINDRICAL_SURFACE ( 'NONE', #31774, 3.000000000000000444 ) ;
#30987=CARTESIAN_POINT ( 'NONE',  ( 43.48293223442611577, 6.614494798211716819, -72.90498134187569690 ) ) ;
#31014=EDGE_CURVE ( 'NONE', #3841, #39608, #6079, .T. ) ;
#31048=VERTEX_POINT ( 'NONE', #28613 ) ;
#31049=CARTESIAN_POINT ( 'NONE',  ( 12.86517331568640010, -49.11618894467930829, -34.64999999999999858 ) ) ;
#31052=VERTEX_POINT ( 'NONE', #44357 ) ;
#31053=DIRECTION ( 'NONE',  ( 0.1961161351381830731, 0.000000000000000000, 0.9805806756909203337 ) ) ;
#31060=DIRECTION ( 'NONE',  ( 0.000000000000000000, 0.000000000000000000, 1.000000000000000000 ) ) ;
#31067=CARTESIAN_POINT ( 'NONE',  ( 45.15893990696358173, -40.04164385324116182, -61.04083920648312755 ) ) ;
#31093=CARTESIAN_POINT ( 'NONE',  ( 0.2609591194317604779, -26.58175058825759152, -34.64999999999999147 ) ) ;
#31097=AXIS2_PLACEMENT_3D ( 'NONE', #18058, #42438, #6273 ) ;
#31098=VERTEX_POINT ( 'NONE', #4515 ) ;
#31101=CARTESIAN_POINT ( 'NONE',  ( 19.13393739769600188, 18.38381105532069881, -35.14999999999999858 ) ) ;
#31108=CARTESIAN_POINT ( 'NONE',  ( 19.31296351478360052, 18.65448050664020130, -82.14319696191608955 ) ) ;
#31109=AXIS2_PLACEMENT_3D ( 'NONE', #27678, #31338, #11462 ) ;
#31110=ORIENTED_EDGE ( 'NONE', *, *, #24642, .F. ) ;
#31114=CARTESIAN_POINT ( 'NONE',  ( 0.3209249304026170480, -15.61618894467929941, -35.14999999999999858 ) ) ;
#31131=CARTESIAN_POINT ( 'NONE',  ( 0.08375394646315241498, 19.63944928676770019, -34.70982966457259522 ) ) ;
#31139=EDGE_LOOP ( 'NONE', ( #12180, #32232, #6578, #30897, #11673, #23695 ) ) ;
#31141=( BOUNDED_CURVE ( )  B_SPLINE_CURVE ( 3, ( #40006, #28186, #28446, #28968 ),
 .UNSPECIFIED., .F., .T. ) 
 B_SPLINE_CURVE_WITH_KNOTS ( ( 4, 4 ),
 ( 1.570796326794886344, 2.356194490192476731 ),
 .UNSPECIFIED. ) 
 CURVE ( )  GEOMETRIC_REPRESENTATION_ITEM ( )  RATIONAL_B_SPLINE_CURVE ( ( 1.000000000000000000, 0.9492530216741729143, 0.9492530216741729143, 1.000000000000000000 ) ) 
 REPRESENTATION_ITEM ( '' )  );
#31143=CIRCLE ( 'NONE', #36207, 39.00000000000000000 ) ;
#31145=CARTESIAN_POINT ( 'NONE',  ( 46.75983893905041100, 8.015321561625365021, -57.03879444339121818 ) ) ;
#31148=CARTESIAN_POINT ( 'NONE',  ( 47.07753517504149698, -39.26143421117000543, -34.91082242604309727 ) ) ;
#31178=CARTESIAN_POINT ( 'NONE',  ( 46.39112542121452520, -38.19271976108705502, -58.36405639519246336 ) ) ;
#31180=ORIENTED_EDGE ( 'NONE', *, *, #51871, .T. ) ;
#31185=CARTESIAN_POINT ( 'NONE',  ( 44.13393739769620083, -33.11618894467940066, -54.27132075603720551 ) ) ;
#31196=EDGE_CURVE ( 'NONE', #19168, #14168, #18829, .T. ) ;
#31197=DIRECTION ( 'NONE',  ( -1.000000000000000000, 0.000000000000000000, 0.000000000000000000 ) ) ;
#31213=CARTESIAN_POINT ( 'NONE',  ( 40.75465142538513419, -33.99486860111964859, -82.06602514716892927 ) ) ;
#31232=EDGE_CURVE ( 'NONE', #25171, #31048, #8690, .T. ) ;
#31236=CARTESIAN_POINT ( 'NONE',  ( -0.03447620312152044342, -8.421650097910747590, -34.79644660940672196 ) ) ;
#31237=CARTESIAN_POINT ( 'NONE',  ( 42.95888890335680799, 6.539414064201790389, -75.52524143611269380 ) ) ;
#31239=ORIENTED_EDGE ( 'NONE', *, *, #51114, .T. ) ;
#31241=AXIS2_PLACEMENT_3D ( 'NONE', #3301, #140, #11174 ) ;
#31254=DIRECTION ( 'NONE',  ( 0.6339889056055360017, 0.000000000000000000, -0.7733421413379041320 ) ) ;
#31267=EDGE_CURVE ( 'NONE', #51550, #37751, #47917, .T. ) ;
#31271=DIRECTION ( 'NONE',  ( 0.8529225269813149879, 0.5196435251606980055, -0.04993765839895900061 ) ) ;
#31279=ORIENTED_EDGE ( 'NONE', *, *, #8251, .T. ) ;
#31283=CARTESIAN_POINT ( 'NONE',  ( 45.40902987668481217, 8.825533465273407430, -59.82804123183892386 ) ) ;
#31286=ORIENTED_EDGE ( 'NONE', *, *, #49415, .F. ) ;
#31300=CARTESIAN_POINT ( 'NONE',  ( 46.63393739769619373, -15.61618894467929941, -35.14999999999999858 ) ) ;
#31301=( BOUNDED_CURVE ( )  B_SPLINE_CURVE ( 2, ( #22651, #46277, #30771 ),
 .UNSPECIFIED., .F., .T. ) 
 B_SPLINE_CURVE_WITH_KNOTS ( ( 3, 3 ),
 ( 0.1321855491485360024, 2.139356573196280031 ),
 .UNSPECIFIED. ) 
 CURVE ( )  GEOMETRIC_REPRESENTATION_ITEM ( )  RATIONAL_B_SPLINE_CURVE ( ( 1.001093714210500085, 1.008874108803850200, 1.000760730680210209 ) ) 
 REPRESENTATION_ITEM ( '' )  );
#31303=CARTESIAN_POINT ( 'NONE',  ( 45.14832757675640096, 2.060512883921409966, -35.14999999999999858 ) ) ;
#31308=CARTESIAN_POINT ( 'NONE',  ( 13.13393739769600010, 18.38381105532060289, -35.14999999999999858 ) ) ;
#31314=CARTESIAN_POINT ( 'NONE',  ( 34.13393739769599478, 18.23736444591407135, -34.79644660940672907 ) ) ;
#31317=ORIENTED_EDGE ( 'NONE', *, *, #5899, .F. ) ;
#31322=CARTESIAN_POINT ( 'NONE',  ( 44.88531378893124213, -40.02229542238428905, -62.36962640805702307 ) ) ;
#31327=CARTESIAN_POINT ( 'NONE',  ( -0.8554694999317272730, 0.5322876908067696311, 4.943674098299870145 ) ) ;
#31334=EDGE_LOOP ( 'NONE', ( #23646, #1020, #6013, #35943 ) ) ;
#31338=DIRECTION ( 'NONE',  ( -0.8660254037844387076, 0.4999999999999998890, 1.942890293094024439E-16 ) ) ;
#31340=CARTESIAN_POINT ( 'NONE',  ( 14.63393739769630031, 0.9255523191757060175, -34.64999999999999858 ) ) ;
#31349=CARTESIAN_POINT ( 'NONE',  ( 29.13393739769619728, -4.468739684871080087, -35.14999999999999858 ) ) ;
#31355=DIRECTION ( 'NONE',  ( 0.000000000000000000, -1.000000000000000000, 0.000000000000000000 ) ) ;
#31366=CARTESIAN_POINT ( 'NONE',  ( 16.13393739769620083, -15.61618894467929941, -35.14999999999999858 ) ) ;
#31378=DIRECTION ( 'NONE',  ( 0.8660254037844381525, 0.5000000000000007772, 0.000000000000000000 ) ) ;
#31391=CARTESIAN_POINT ( 'NONE',  ( 47.13180046211940066, -38.11666126782029806, -54.64277967633139355 ) ) ;
#31399=CARTESIAN_POINT ( 'NONE',  ( 41.69094003941798832, 7.483996613871343406, -82.16073232984879837 ) ) ;
#31415=DIRECTION ( 'NONE',  ( -0.8660254037844379305, 0.5000000000000011102, 0.000000000000000000 ) ) ;
#31421=EDGE_LOOP ( 'NONE', ( #12091, #13398 ) ) ;
#31424=CARTESIAN_POINT ( 'NONE',  ( 20.13393739769620083, -28.89524513604070322, -62.14999999999999858 ) ) ;
#31431=EDGE_CURVE ( 'NONE', #50288, #14340, #46442, .T. ) ;
#31432=CARTESIAN_POINT ( 'NONE',  ( -11.36606260230380094, -15.61618894467929941, -54.64999999999999858 ) ) ;
#31436=VERTEX_POINT ( 'NONE', #36612 ) ;
#31437=CARTESIAN_POINT ( 'NONE',  ( -22.75376598977980080, -12.76162732185420268, -54.69834592236689019 ) ) ;
#31441=AXIS2_PLACEMENT_3D ( 'NONE', #32610, #20309, #44957 ) ;
#31444=CARTESIAN_POINT ( 'NONE',  ( 9.895693118437268510, 22.37718731335050038, -34.65000333313919612 ) ) ;
#31459=ORIENTED_EDGE ( 'NONE', *, *, #27834, .T. ) ;
#31491=CARTESIAN_POINT ( 'NONE',  ( 44.75655348390716881, 6.781133406353570869, -66.53686104485265673 ) ) ;
#31509=ADVANCED_FACE ( 'NONE', ( #32150 ), #13310, .F. ) ;
#31523=ORIENTED_EDGE ( 'NONE', *, *, #40329, .T. ) ;
#31524=FACE_OUTER_BOUND ( 'NONE', #45184, .T. ) ;
#31525=DIRECTION ( 'NONE',  ( 0.000000000000000000, 0.000000000000000000, 1.000000000000000000 ) ) ;
#31533=CARTESIAN_POINT ( 'NONE',  ( -0.1135338934745361295, -20.70530579567934026, -34.86513988225942740 ) ) ;
#31541=CARTESIAN_POINT ( 'NONE',  ( 22.16915665782680023, -54.07211264381400184, -34.88336916441289759 ) ) ;
#31570=FACE_OUTER_BOUND ( 'NONE', #35305, .T. ) ;
#31573=ORIENTED_EDGE ( 'NONE', *, *, #29431, .F. ) ;
#31574=CARTESIAN_POINT ( 'NONE',  ( 23.53669455186071602, -48.92556967366427756, -34.79644561402096770 ) ) ;
#31577=CARTESIAN_POINT ( 'NONE',  ( 42.50259719104650458, -39.81721345468353235, -73.90402679261637786 ) ) ;
#31586=EDGE_LOOP ( 'NONE', ( #40220, #29998, #12151, #17589 ) ) ;
#31593=AXIS2_PLACEMENT_3D ( 'NONE', #39075, #30149, #34600 ) ;
#31596=CARTESIAN_POINT ( 'NONE',  ( 14.39116781407899914, 1.145880372108919909, -34.70985242058469566 ) ) ;
#31598=CARTESIAN_POINT ( 'NONE',  ( 30.37740194055309928, 4.394033142310519224, -84.60975078156931772 ) ) ;
#31601=DIRECTION ( 'NONE',  ( 1.000000000000000000, 0.000000000000000000, 0.000000000000000000 ) ) ;
#31602=EDGE_CURVE ( 'NONE', #20523, #49499, #10407, .T. ) ;
#31604=AXIS2_PLACEMENT_3D ( 'NONE', #25737, #38078, #49877 ) ;
#31610=ORIENTED_EDGE ( 'NONE', *, *, #40619, .F. ) ;
#31611=CARTESIAN_POINT ( 'NONE',  ( 28.63393739769619728, -4.678675331415849570, -34.64999999999999858 ) ) ;
#31612=CARTESIAN_POINT ( 'NONE',  ( -18.86687343253337090, 1.668172178233732206, -51.44400016804027587 ) ) ;
#31620=DIRECTION ( 'NONE',  ( 1.000000000000000000, 0.000000000000000000, 0.000000000000000000 ) ) ;
#31621=CARTESIAN_POINT ( 'NONE',  ( 16.13393739769599833, 14.38381105532070059, -35.14999999999999858 ) ) ;
#31635=VERTEX_POINT ( 'NONE', #25584 ) ;
#31644=DIRECTION ( 'NONE',  ( 0.6933752452815366007, -0.7071067811865471286, -0.1386750490563077864 ) ) ;
#31645=CARTESIAN_POINT ( 'NONE',  ( 40.57649240635721810, 4.883811055320659733, -83.97002642401369599 ) ) ;
#31647=FACE_OUTER_BOUND ( 'NONE', #42342, .T. ) ;
#31652=CARTESIAN_POINT ( 'NONE',  ( 43.90669715076391810, 6.478564597039538242, -70.75373661325032515 ) ) ;
#31653=CARTESIAN_POINT ( 'NONE',  ( 14.28038400710292777, -23.61618894467940066, -34.79644660940672907 ) ) ;
#31682=CARTESIAN_POINT ( 'NONE',  ( 45.68512934788849833, -33.42474020775232191, -54.50653973161868038 ) ) ;
#31688=CARTESIAN_POINT ( 'NONE',  ( 16.13393739769620083, -15.61618894467929941, -34.64999999999999858 ) ) ;
#31689=CARTESIAN_POINT ( 'NONE',  ( 46.02470361814555844, -38.15599428330931886, -60.19611770114092053 ) ) ;
#31693=CARTESIAN_POINT ( 'NONE',  ( 19.94107633810069657, -40.34105917676275510, -34.79644660940672907 ) ) ;
#31698=AXIS2_PLACEMENT_3D ( 'NONE', #36540, #28412, #45197 ) ;
#31701=CIRCLE ( 'NONE', #9146, 2.999999999999999112 ) ;
#31713=DIRECTION ( 'NONE',  ( 1.000000000000000000, 0.000000000000000000, 0.000000000000000000 ) ) ;
#31720=ADVANCED_FACE ( 'NONE', ( #30034 ), #48167, .T. ) ;
#31722=CARTESIAN_POINT ( 'NONE',  ( 13.05521822061467319, 18.23736444591386174, -34.79644660940673617 ) ) ;
#31724=FACE_BOUND ( 'NONE', #5349, .T. ) ;
#31728=CARTESIAN_POINT ( 'NONE',  ( -4.615472129303443971, -42.73836944035205931, -38.77992132782590318 ) ) ;
#31731=FACE_OUTER_BOUND ( 'NONE', #17206, .T. ) ;
#31733=ORIENTED_EDGE ( 'NONE', *, *, #39016, .F. ) ;
#31736=VERTEX_POINT ( 'NONE', #15626 ) ;
#31739=CARTESIAN_POINT ( 'NONE',  ( 29.13393739769619728, -26.76363820448759867, -35.14999999999999858 ) ) ;
#31746=CARTESIAN_POINT ( 'NONE',  ( 44.33589047729159915, 6.728771102257818271, -68.64023485869353181 ) ) ;
#31749=AXIS2_PLACEMENT_3D ( 'NONE', #13084, #49744, #36632 ) ;
#31758=( BOUNDED_CURVE ( )  B_SPLINE_CURVE ( 3, ( #30612, #37721, #46379, #1816 ),
 .UNSPECIFIED., .F., .T. ) 
 B_SPLINE_CURVE_WITH_KNOTS ( ( 4, 4 ),
 ( 2.356194490192327962, 3.141592653589778905 ),
 .UNSPECIFIED. ) 
 CURVE ( )  GEOMETRIC_REPRESENTATION_ITEM ( )  RATIONAL_B_SPLINE_CURVE ( ( 1.000000000000000000, 0.9492530216741907889, 0.9492530216741907889, 1.000000000000000000 ) ) 
 REPRESENTATION_ITEM ( '' )  );
#31759=DIRECTION ( 'NONE',  ( 0.000000000000000000, 0.000000000000000000, -1.000000000000000000 ) ) ;
#31767=ORIENTED_EDGE ( 'NONE', *, *, #4771, .T. ) ;
#31773=FACE_OUTER_BOUND ( 'NONE', #40405, .T. ) ;
#31774=AXIS2_PLACEMENT_3D ( 'NONE', #26800, #42812, #7 ) ;
#31777=CYLINDRICAL_SURFACE ( 'NONE', #38147, 0.4999999999999983347 ) ;
#31780=DIRECTION ( 'NONE',  ( 0.7071067811865461294, -0.7071067811865490160, 0.000000000000000000 ) ) ;
#31781=CIRCLE ( 'NONE', #9234, 0.5000000000000028866 ) ;
#31788=CARTESIAN_POINT ( 'NONE',  ( -0.1863042805355769327, -20.57828601760577669, -34.92844344776042220 ) ) ;
#31791=CARTESIAN_POINT ( 'NONE',  ( 20.30127474080349970, -42.11618894467939356, -34.64999999999999858 ) ) ;
#31799=DIRECTION ( 'NONE',  ( 1.000000000000000000, 0.000000000000000000, 0.000000000000000000 ) ) ;
#31801=EDGE_LOOP ( 'NONE', ( #46957, #42592, #6608, #10045, #50706 ) ) ;
#31807=DIRECTION ( 'NONE',  ( -0.3863301728269311619, 0.9223605572461961444, 1.110223024625156171E-16 ) ) ;
#31823=DIRECTION ( 'NONE',  ( 0.000000000000000000, 0.000000000000000000, -1.000000000000000000 ) ) ;
#31829=ORIENTED_EDGE ( 'NONE', *, *, #39955, .T. ) ;
#31830=DIRECTION ( 'NONE',  ( 0.000000000000000000, 0.000000000000000000, 1.000000000000000000 ) ) ;
#31834=CARTESIAN_POINT ( 'NONE',  ( 44.26457877669638918, -39.97584597393014150, -65.37864771724724733 ) ) ;
#31843=ORIENTED_EDGE ( 'NONE', *, *, #2588, .F. ) ;
#31854=CARTESIAN_POINT ( 'NONE',  ( 42.40667996754965685, 8.575301686933304524, -74.36634363102189127 ) ) ;
#31855=CARTESIAN_POINT ( 'NONE',  ( 44.65669779474150403, -33.16208384341911852, -44.90189889201600693 ) ) ;
#31860=CARTESIAN_POINT ( 'NONE',  ( -5.316689532470439516, -0.1743001472114563133, -59.64999999999999147 ) ) ;
#31862=LINE ( 'NONE', #35814, #40695 ) ;
#31865=CARTESIAN_POINT ( 'NONE',  ( 16.13393739769620083, -15.61618894467919816, -82.14319696191608955 ) ) ;
#31870=DIRECTION ( 'NONE',  ( -0.3502816565540429750, 0.000000000000000000, 0.9366444154970205993 ) ) ;
#31877=ORIENTED_EDGE ( 'NONE', *, *, #35492, .T. ) ;
#31887=CONICAL_SURFACE ( 'NONE', #6829, 1.154999999999999361, 0.08090409915523018303 ) ;
#31911=CARTESIAN_POINT ( 'NONE',  ( 47.33846070720256449, 6.770505468649851366, -53.56164933099653780 ) ) ;
#31916=CARTESIAN_POINT ( 'NONE',  ( -0.4410626023037880206, -27.49517073325580085, -35.14999999999999858 ) ) ;
#31935=ORIENTED_EDGE ( 'NONE', *, *, #34467, .F. ) ;
#31940=ORIENTED_EDGE ( 'NONE', *, *, #20306, .F. ) ;
#31941=CARTESIAN_POINT ( 'NONE',  ( 19.22157560178293423, -49.74868907930050455, -82.73668660645817852 ) ) ;
#31945=CARTESIAN_POINT ( 'NONE',  ( 22.13393739769589885, 22.91950879131610108, -35.14999999999999858 ) ) ;
#31946=CARTESIAN_POINT ( 'NONE',  ( 46.61351573269507043, -38.21450491841939368, -57.25208055290525522 ) ) ;
#31950=EDGE_CURVE ( 'NONE', #26981, #19127, #44999, .T. ) ;
#31951=CARTESIAN_POINT ( 'NONE',  ( 38.67452568954060155, 4.883811055320659733, -84.65000000000000568 ) ) ;
#31957=CARTESIAN_POINT ( 'NONE',  ( 0.1246572822142906628, 19.61312073211624707, -34.68957853602456964 ) ) ;
#31958=AXIS2_PLACEMENT_3D ( 'NONE', #31865, #3341, #19057 ) ;
#31962=B_SPLINE_CURVE_WITH_KNOTS ( 'NONE', 3,
 ( #6715, #37638, #18233, #49708, #34727, #29754 ),
 .UNSPECIFIED., .F., .F.,
 ( 4, 2, 4 ),
 ( -0.3033244957681310305, -0.3025616577353109626, -0.2608998691367954148 ),
 .UNSPECIFIED. ) ;
#31964=DIRECTION ( 'NONE',  ( 0.5835456732599411112, 0.8120803206700689669, 0.000000000000000000 ) ) ;
#31969=CARTESIAN_POINT ( 'NONE',  ( 22.37218167695459670, 22.37718731335059985, -34.65000333313919612 ) ) ;
#31985=FACE_BOUND ( 'NONE', #15541, .T. ) ;
#31994=ORIENTED_EDGE ( 'NONE', *, *, #28600, .T. ) ;
#32003=CARTESIAN_POINT ( 'NONE',  ( 17.73647699123739940, 1.019008445897469972, -34.65800258959620095 ) ) ;
#32029=DIRECTION ( 'NONE',  ( 0.5516667872527449834, 0.8340645993220396903, 2.775557561562889194E-17 ) ) ;
#32046=VERTEX_POINT ( 'NONE', #35652 ) ;
#32047=CARTESIAN_POINT ( 'NONE',  ( 16.13393739769620083, -15.61618894467929941, -54.64999999999999858 ) ) ;
#32049=DIRECTION ( 'NONE',  ( -0.3487035033511758919, -0.9372330909387569520, 0.000000000000000000 ) ) ;
#32053=VERTEX_POINT ( 'NONE', #51639 ) ;
#32055=CIRCLE ( 'NONE', #35450, 6.999999999999999112 ) ;
#32056=VERTEX_POINT ( 'NONE', #46956 ) ;
#32059=( BOUNDED_CURVE ( )  B_SPLINE_CURVE ( 3, ( #14740, #18919, #30960, #31722 ),
 .UNSPECIFIED., .F., .T. ) 
 B_SPLINE_CURVE_WITH_KNOTS ( ( 4, 4 ),
 ( 1.570796326794896558, 2.356194490192338620 ),
 .UNSPECIFIED. ) 
 CURVE ( )  GEOMETRIC_REPRESENTATION_ITEM ( )  RATIONAL_B_SPLINE_CURVE ( ( 1.000000000000000000, 0.9492530216741918991, 0.9492530216741918991, 1.000000000000000000 ) ) 
 REPRESENTATION_ITEM ( '' )  );
#32069=ORIENTED_EDGE ( 'NONE', *, *, #845, .T. ) ;
#32083=AXIS2_PLACEMENT_3D ( 'NONE', #3424, #19395, #35376 ) ;
#32087=CARTESIAN_POINT ( 'NONE',  ( 43.64633900757768714, -39.92480820678616027, -68.37225813791066287 ) ) ;
#32104=CARTESIAN_POINT ( 'NONE',  ( 41.85500005128616152, 8.516429740364495515, -77.03127993483552416 ) ) ;
#32110=ORIENTED_EDGE ( 'NONE', *, *, #16127, .F. ) ;
#32112=ORIENTED_EDGE ( 'NONE', *, *, #32482, .T. ) ;
#32115=CARTESIAN_POINT ( 'NONE',  ( 23.13393739769620083, -28.89524513604070322, -39.64999999999999858 ) ) ;
#32119=EDGE_LOOP ( 'NONE', ( #40736, #23677, #45295, #41382 ) ) ;
#32120=CARTESIAN_POINT ( 'NONE',  ( -0.1695375756935748601, 14.25975516931139708, -34.91378044826135607 ) ) ;
#32121=CARTESIAN_POINT ( 'NONE',  ( -20.18262829310297590, -1.399661344290894061, -52.57430347528295300 ) ) ;
#32140=EDGE_CURVE ( 'NONE', #5719, #21125, #50988, .T. ) ;
#32150=FACE_OUTER_BOUND ( 'NONE', #51266, .T. ) ;
#32152=EDGE_CURVE ( 'NONE', #22659, #23707, #4446, .T. ) ;
#32163=ORIENTED_EDGE ( 'NONE', *, *, #16093, .T. ) ;
#32164=CARTESIAN_POINT ( 'NONE',  ( 64.90705159044762240, -17.44293478064540892, -18.18360580342293531 ) ) ;
#32165=CARTESIAN_POINT ( 'NONE',  ( 14.18536260820837214, -41.66761415519157197, -34.89146800830128825 ) ) ;
#32166=DIRECTION ( 'NONE',  ( -1.000000000000000000, 0.000000000000000000, 0.000000000000000000 ) ) ;
#32172=ORIENTED_EDGE ( 'NONE', *, *, #21396, .T. ) ;
#32175=ORIENTED_EDGE ( 'NONE', *, *, #6889, .F. ) ;
#32183=VERTEX_POINT ( 'NONE', #41067 ) ;
#32187=ORIENTED_EDGE ( 'NONE', *, *, #40329, .F. ) ;
#32188=DIRECTION ( 'NONE',  ( -0.5516667872527389882, -0.8340645993220436871, 8.326672684688667890E-17 ) ) ;
#32191=EDGE_LOOP ( 'NONE', ( #47956, #50509, #45543, #36794 ) ) ;
#32193=CARTESIAN_POINT ( 'NONE',  ( 18.11900864776890074, -32.59522544870679894, -35.02873218748179340 ) ) ;
#32200=VERTEX_POINT ( 'NONE', #51828 ) ;
#32211=DIRECTION ( 'NONE',  ( -1.000000000000000000, 0.000000000000000000, 0.000000000000000000 ) ) ;
#32215=CARTESIAN_POINT ( 'NONE',  ( 40.78962545348711188, -39.66124797165849714, -82.01204344300963101 ) ) ;
#32218=EDGE_CURVE ( 'NONE', #2647, #4309, #36337, .T. ) ;
#32223=TOROIDAL_SURFACE ( 'NONE', #14717, 2.500000000000000000, 0.5000000000000000000 ) ;
#32232=ORIENTED_EDGE ( 'NONE', *, *, #33759, .T. ) ;
#32235=FACE_BOUND ( 'NONE', #40344, .T. ) ;
#32239=DIRECTION ( 'NONE',  ( 0.000000000000000000, -1.000000000000000000, 0.000000000000000000 ) ) ;
#32249=CARTESIAN_POINT ( 'NONE',  ( 0.08551642312349798380, -45.86262496382770593, -34.70586877331279396 ) ) ;
#32255=CARTESIAN_POINT ( 'NONE',  ( 41.98072431426170681, 6.388270017410889068, -80.41599570558052790 ) ) ;
#32259=CARTESIAN_POINT ( 'NONE',  ( 42.98612411504951325, -37.77564690010735404, -75.38906579693129117 ) ) ;
#32284=VECTOR ( 'NONE', #39500, 1000.000000000000000 ) ;
#32293=AXIS2_PLACEMENT_3D ( 'NONE', #18207, #46270, #50190 ) ;
#32300=CARTESIAN_POINT ( 'NONE',  ( 14.28038400710293487, -41.76263555408612405, -34.79644660940672907 ) ) ;
#32315=CARTESIAN_POINT ( 'NONE',  ( 16.13393739769620083, -15.61618894467929941, -35.14999999999999858 ) ) ;
#32316=EDGE_LOOP ( 'NONE', ( #26392, #42954, #36636, #19323 ) ) ;
#32317=LINE ( 'NONE', #24971, #41051 ) ;
#32318=CARTESIAN_POINT ( 'NONE',  ( 4.133937397696209715, -8.687985714403829718, -47.64999999999999858 ) ) ;
#32321=VECTOR ( 'NONE', #38381, 1000.000000000000000 ) ;
#32322=CARTESIAN_POINT ( 'NONE',  ( 14.13393739769619906, -45.61618894467940066, -35.14999999999999858 ) ) ;
#32328=VECTOR ( 'NONE', #7571, 1000.000000000000114 ) ;
#32343=CARTESIAN_POINT ( 'NONE',  ( 43.85372935305733932, -39.94273075073680701, -67.36733013287428662 ) ) ;
#32352=FACE_OUTER_BOUND ( 'NONE', #39668, .T. ) ;
#32362=CARTESIAN_POINT ( 'NONE',  ( 42.65610030855648205, 8.600309723121037919, -73.16201499959163357 ) ) ;
#32363=CARTESIAN_POINT ( 'NONE',  ( 0.3209249304026170480, -23.01378514180129997, -34.64999999999999858 ) ) ;
#32364=CARTESIAN_POINT ( 'NONE',  ( 30.46076380116034343, 4.402158596034774440, -84.61108498746632733 ) ) ;
#32366=ORIENTED_EDGE ( 'NONE', *, *, #13250, .T. ) ;
#32377=EDGE_LOOP ( 'NONE', ( #50921, #44805, #47834, #3776 ) ) ;
#32387=CARTESIAN_POINT ( 'NONE',  ( -11.80944000494499768, -34.05870648691990255, -45.03554556751409166 ) ) ;
#32406=DIRECTION ( 'NONE',  ( 0.3535533905932799481, 0.6123724356957926940, 0.7071067811865460184 ) ) ;
#32408=FACE_OUTER_BOUND ( 'NONE', #32119, .T. ) ;
#32409=DIRECTION ( 'NONE',  ( 0.000000000000000000, 0.000000000000000000, -1.000000000000000000 ) ) ;
#32414=ORIENTED_EDGE ( 'NONE', *, *, #21078, .T. ) ;
#32427=EDGE_CURVE ( 'NONE', #16602, #24198, #43021, .T. ) ;
#32439=LINE ( 'NONE', #4692, #48459 ) ;
#32443=CARTESIAN_POINT ( 'NONE',  ( 10.13393739769589885, 22.91950879131600161, -35.14999999999999858 ) ) ;
#32445=AXIS2_PLACEMENT_3D ( 'NONE', #27189, #20095, #31620 ) ;
#32460=CARTESIAN_POINT ( 'NONE',  ( 15.63466510375951302, -49.61614664559245114, -83.23984175397698948 ) ) ;
#32479=CARTESIAN_POINT ( 'NONE',  ( 26.13393739769619728, -2.337132753317950229, -39.64999999999999858 ) ) ;
#32482=EDGE_CURVE ( 'NONE', #29117, #6764, #27015, .T. ) ;
#32484=CARTESIAN_POINT ( 'NONE',  ( 16.13393739769620083, -15.61618894467929941, -35.02873218748179340 ) ) ;
#32490=ADVANCED_FACE ( 'NONE', ( #7117 ), #22000, .T. ) ;
#32491=CARTESIAN_POINT ( 'NONE',  ( 0.1457841021255935343, -15.61618894467929941, -34.68167779225149161 ) ) ;
#32494=B_SPLINE_CURVE_WITH_KNOTS ( 'NONE', 3,
 ( #51718, #43351, #20242, #35212 ),
 .UNSPECIFIED., .F., .F.,
 ( 4, 4 ),
 ( 0.000000000000000000, 1.000000000000000000 ),
 .UNSPECIFIED. ) ;
#32497=EDGE_LOOP ( 'NONE', ( #29935, #40692, #50477, #30767 ) ) ;
#32498=VERTEX_POINT ( 'NONE', #47469 ) ;
#32499=DIRECTION ( 'NONE',  ( -1.000000000000000000, 0.000000000000000000, 0.000000000000000000 ) ) ;
#32504=VERTEX_POINT ( 'NONE', #11564 ) ;
#32505=CARTESIAN_POINT ( 'NONE',  ( -0.1295185695944119919, -31.87964491196989414, 4.943674098299959851 ) ) ;
#32510=CARTESIAN_POINT ( 'NONE',  ( 45.34325132301859895, 2.693353616613840096, -34.65000333093299645 ) ) ;
#32511=CARTESIAN_POINT ( 'NONE',  ( 42.04061362852223027, -37.63029778570905393, -80.11654543539063411 ) ) ;
#32512=EDGE_CURVE ( 'NONE', #17157, #30658, #44285, .T. ) ;
#32517=AXIS2_PLACEMENT_3D ( 'NONE', #24030, #20119, #28499 ) ;
#32539=PLANE ( 'NONE',  #40824 ) ;
#32554=VECTOR ( 'NONE', #22808, 1000.000000000000000 ) ;
#32561=ORIENTED_EDGE ( 'NONE', *, *, #16484, .F. ) ;
#32575=CARTESIAN_POINT ( 'NONE',  ( 26.13393739769619728, -2.337132753317950229, -84.65000000000000568 ) ) ;
#32576=CARTESIAN_POINT ( 'NONE',  ( 38.67452568954060155, -33.11618894467940066, -81.65000000000000568 ) ) ;
#32586=VECTOR ( 'NONE', #51060, 1000.000000000000000 ) ;
#32596=ADVANCED_FACE ( 'NONE', ( #16769 ), #16249, .T. ) ;
#32601=ADVANCED_FACE ( 'NONE', ( #5504 ), #4976, .F. ) ;
#32602=CARTESIAN_POINT ( 'NONE',  ( 44.14365615324429371, -39.96620590573778742, -65.96444131013311107 ) ) ;
#32603=( NAMED_UNIT ( * ) PLANE_ANGLE_UNIT ( ) SI_UNIT ( $, .RADIAN. ) );
#32604=CARTESIAN_POINT ( 'NONE',  ( -1.143840380081600161, -14.00933513942850794, -35.76111111111113416 ) ) ;
#32607=CARTESIAN_POINT ( 'NONE',  ( 46.13393739769619373, 2.762490711761015572, -83.77132034355965118 ) ) ;
#32610=CARTESIAN_POINT ( 'NONE',  ( 0.1339373976962109913, -15.61618894467929941, -34.64999999999999858 ) ) ;
#32611=ORIENTED_EDGE ( 'NONE', *, *, #42644, .F. ) ;
#32618=DIRECTION ( 'NONE',  ( 0.000000000000000000, 0.000000000000000000, -1.000000000000000000 ) ) ;
#32619=CARTESIAN_POINT ( 'NONE',  ( 42.92096165568810306, 8.626172559110205640, -71.88163569493146099 ) ) ;
#32620=CARTESIAN_POINT ( 'NONE',  ( 0.2609591194317595897, -22.97916386469509575, -34.64999999999999147 ) ) ;
#32628=CARTESIAN_POINT ( 'NONE',  ( 41.13393739769620083, -15.61618894467929941, -84.65000000000000568 ) ) ;
#32629=AXIS2_PLACEMENT_3D ( 'NONE', #31300, #47074, #27130 ) ;
#32638=AXIS2_PLACEMENT_3D ( 'NONE', #49587, #13930, #5806 ) ;
#32639=CARTESIAN_POINT ( 'NONE',  ( -0.3803200024020541581, 14.07826830858616063, -35.09718034791147545 ) ) ;
#32652=CARTESIAN_POINT ( 'NONE',  ( 27.50893739769620083, -36.61730498645199816, -35.14999999999999858 ) ) ;
#32662=EDGE_CURVE ( 'NONE', #24695, #42065, #43127, .T. ) ;
#32664=( BOUNDED_CURVE ( )  B_SPLINE_CURVE ( 2, ( #47890, #27948, #18806 ),
 .UNSPECIFIED., .F., .T. ) 
 B_SPLINE_CURVE_WITH_KNOTS ( ( 3, 3 ),
 ( 0.2168422315598149963, 3.147551163863049783 ),
 .UNSPECIFIED. ) 
 CURVE ( )  GEOMETRIC_REPRESENTATION_ITEM ( )  RATIONAL_B_SPLINE_CURVE ( ( 1.000597593688320019, 1.004455541115450101, 1.003436844929990190 ) ) 
 REPRESENTATION_ITEM ( '' )  );
#32666=CIRCLE ( 'NONE', #6749, 16.60961179679780031 ) ;
#32673=DIRECTION ( 'NONE',  ( 0.000000000000000000, 1.000000000000000000, 0.000000000000000000 ) ) ;
#32679=DIRECTION ( 'NONE',  ( 0.000000000000000000, -1.000000000000000000, 0.000000000000000000 ) ) ;
#32696=CARTESIAN_POINT ( 'NONE',  ( 18.13393739769639978, 6.292713355527299157, -54.64999999999999858 ) ) ;
#32703=CARTESIAN_POINT ( 'NONE',  ( 22.23620501646714587, -53.91985561452059272, -34.73809820100315449 ) ) ;
#32711=CARTESIAN_POINT ( 'NONE',  ( 2.458146360389370511, -25.65221394861527671, -34.79644291222910368 ) ) ;
#32716=ORIENTED_EDGE ( 'NONE', *, *, #29719, .T. ) ;
#32717=CYLINDRICAL_SURFACE ( 'NONE', #1919, 0.4999999999999982236 ) ;
#32723=EDGE_CURVE ( 'NONE', #12924, #25427, #42794, .T. ) ;
#32729=CARTESIAN_POINT ( 'NONE',  ( 16.13393739769620083, -45.61618894467940066, -49.33749999999999858 ) ) ;
#32739=DIRECTION ( 'NONE',  ( 0.000000000000000000, 1.000000000000000000, 0.000000000000000000 ) ) ;
#32777=CARTESIAN_POINT ( 'NONE',  ( 41.82154896394096255, -37.59484916107987118, -81.21190131928830169 ) ) ;
#32778=VERTEX_POINT ( 'NONE', #7399 ) ;
#32789=LINE ( 'NONE', #48814, #28108 ) ;
#32819=DIRECTION ( 'NONE',  ( -1.000000000000000000, 0.000000000000000000, 0.000000000000000000 ) ) ;
#32821=VECTOR ( 'NONE', #47395, 1000.000000000000000 ) ;
#32828=ORIENTED_EDGE ( 'NONE', *, *, #47790, .T. ) ;
#32833=VERTEX_POINT ( 'NONE', #47749 ) ;
#32835=VERTEX_POINT ( 'NONE', #299 ) ;
#32836=CARTESIAN_POINT ( 'NONE',  ( 46.63393739769619373, 7.878491304262099426, -34.64999999999999858 ) ) ;
#32837=VERTEX_POINT ( 'NONE', #28317 ) ;
#32857=CARTESIAN_POINT ( 'NONE',  ( 18.11714455905759635, 1.361188710403589797, -35.02127583263639821 ) ) ;
#32861=CARTESIAN_POINT ( 'NONE',  ( 41.30259114575395785, -39.68594778607436524, -79.69702892170657549 ) ) ;
#32873=ORIENTED_EDGE ( 'NONE', *, *, #45865, .F. ) ;
#32877=DIRECTION ( 'NONE',  ( 0.000000000000000000, 0.000000000000000000, -1.000000000000000000 ) ) ;
#32881=CARTESIAN_POINT ( 'NONE',  ( 43.55216548528601805, 8.684117711060597600, -68.82845419862523784 ) ) ;
#32884=DIRECTION ( 'NONE',  ( 0.000000000000000000, 0.000000000000000000, -1.000000000000000000 ) ) ;
#32888=VERTEX_POINT ( 'NONE', #35935 ) ;
#32897=AXIS2_PLACEMENT_3D ( 'NONE', #33744, #28787, #41365 ) ;
#32898=ORIENTED_EDGE ( 'NONE', *, *, #27181, .T. ) ;
#32899=ADVANCED_FACE ( 'NONE', ( #31985, #28842, #28578, #31724, #12886, #32235, #24374, #44578, #24634 ), #44318, .T. ) ;
#32910=ORIENTED_EDGE ( 'NONE', *, *, #49883, .F. ) ;
#32933=CIRCLE ( 'NONE', #8688, 5.251829701412241924 ) ;
#32946=CARTESIAN_POINT ( 'NONE',  ( 2.464092196720417238, -5.608468378986529501, -34.77490583097448251 ) ) ;
#32947=DIRECTION ( 'NONE',  ( 0.8445663830063383504, 0.5331299045725292896, -0.04980089904888002073 ) ) ;
#32948=CARTESIAN_POINT ( 'NONE',  ( 0.4253373362157371607, -22.38267892379094093, -35.06583844469808042 ) ) ;
#32955=CONICAL_SURFACE ( 'NONE', #18755, 19.50000000000000000, 0.2449786631268651149 ) ;
#32962=CARTESIAN_POINT ( 'NONE',  ( 0.1375711481831189409, -10.50541980564829814, -34.68474920830804820 ) ) ;
#32965=CARTESIAN_POINT ( 'NONE',  ( 40.75465142538514840, 2.762490711761011575, -82.06602514716892927 ) ) ;
#32967=LINE ( 'NONE', #37184, #42371 ) ;
#32970=DIRECTION ( 'NONE',  ( 1.000000000000000000, 0.000000000000000000, 0.000000000000000000 ) ) ;
#32989=CARTESIAN_POINT ( 'NONE',  ( 0.03808610503981946921, -22.85048806984080372, -34.73334895013599777 ) ) ;
#32994=DIRECTION ( 'NONE',  ( 0.000000000000000000, -1.000000000000000000, 0.000000000000000000 ) ) ;
#32998=CARTESIAN_POINT ( 'NONE',  ( 18.14127191746197809, -49.61613219182720513, -83.14624708861497027 ) ) ;
#33002=CARTESIAN_POINT ( 'NONE',  ( 42.17665618391549742, -39.84915031662858809, -75.20399989164987176 ) ) ;
#33004=DIRECTION ( 'NONE',  ( 0.000000000000000000, 0.000000000000000000, -1.000000000000000000 ) ) ;
#33023=CARTESIAN_POINT ( 'NONE',  ( 30.13393739769619728, -38.61618894467930119, -84.65000000000000568 ) ) ;
#33026=CARTESIAN_POINT ( 'NONE',  ( 46.63499162694400724, 7.878850272075009542, -34.64999999999999858 ) ) ;
#33028=CARTESIAN_POINT ( 'NONE',  ( 15.13522224570046149, -17.17987958086359512, -34.79644660940672907 ) ) ;
#33043=CARTESIAN_POINT ( 'NONE',  ( 42.31744474875747386, 6.441884423166124307, -78.73246318642024733 ) ) ;
#33048=CARTESIAN_POINT ( 'NONE',  ( 41.61626771661330082, -37.56081407618439982, -82.23834840541459812 ) ) ;
#33054=ADVANCED_FACE ( 'NONE', ( #9971 ), #7337, .T. ) ;
#33061=ORIENTED_EDGE ( 'NONE', *, *, #46807, .F. ) ;
#33071=DIRECTION ( 'NONE',  ( -1.000000000000000000, 0.000000000000000000, 0.000000000000000000 ) ) ;
#33073=CYLINDRICAL_SURFACE ( 'NONE', #40717, 0.4999999999999990008 ) ;
#33075=FACE_OUTER_BOUND ( 'NONE', #25031, .T. ) ;
#33079=B_SPLINE_CURVE_WITH_KNOTS ( 'NONE', 3,
 ( #2924, #50877, #47473, #7122, #30937, #22814 ),
 .UNSPECIFIED., .F., .F.,
 ( 4, 2, 4 ),
 ( 0.03318971727292711893, 0.03563426461091390163, 0.06411833789063960121 ),
 .UNSPECIFIED. ) ;
#33093=EDGE_CURVE ( 'NONE', #32046, #20864, #12202, .T. ) ;
#33110=EDGE_LOOP ( 'NONE', ( #25401, #31239 ) ) ;
#33111=ORIENTED_EDGE ( 'NONE', *, *, #5169, .T. ) ;
#33129=( BOUNDED_CURVE ( )  B_SPLINE_CURVE ( 3, ( #45070, #28033, #48749, #4978 ),
 .UNSPECIFIED., .F., .T. ) 
 B_SPLINE_CURVE_WITH_KNOTS ( ( 4, 4 ),
 ( 0.003439152616818795267, 0.3469259656636344835 ),
 .UNSPECIFIED. ) 
 CURVE ( )  GEOMETRIC_REPRESENTATION_ITEM ( )  RATIONAL_B_SPLINE_CURVE ( ( 1.000000000000000000, 0.9901922104150019388, 0.9901922104150019388, 1.000000000000000000 ) ) 
 REPRESENTATION_ITEM ( '' )  );
#33136=B_SPLINE_CURVE_WITH_KNOTS ( 'NONE', 3,
 ( #17189, #17444, #33146, #49428, #49173, #13524 ),
 .UNSPECIFIED., .F., .F.,
 ( 4, 1, 1, 4 ),
 ( 0.000000000000000000, 0.3333697255252178193, 0.6667202725206615721, 1.000000000000000000 ),
 .UNSPECIFIED. ) ;
#33137=VECTOR ( 'NONE', #11202, 1000.000000000000000 ) ;
#33142=EDGE_LOOP ( 'NONE', ( #37047, #33145, #22080, #34008, #40673, #7408 ) ) ;
#33145=ORIENTED_EDGE ( 'NONE', *, *, #30921, .T. ) ;
#33146=CARTESIAN_POINT ( 'NONE',  ( 0.006082813051881367540, -51.09064178927788191, -34.98052497386454007 ) ) ;
#33150=CARTESIAN_POINT ( 'NONE',  ( 45.10518118625895312, 8.805447820864591435, -61.30236472867089503 ) ) ;
#33151=CARTESIAN_POINT ( 'NONE',  ( 18.13393739769630031, 1.391621760993470014, -35.14999999999999858 ) ) ;
#33152=FACE_OUTER_BOUND ( 'NONE', #17513, .T. ) ;
#33154=ORIENTED_EDGE ( 'NONE', *, *, #9648, .F. ) ;
#33157=EDGE_CURVE ( 'NONE', #14308, #45450, #12655, .T. ) ;
#33159=FACE_OUTER_BOUND ( 'NONE', #37712, .T. ) ;
#33161=ADVANCED_FACE ( 'NONE', ( #42052 ), #29972, .T. ) ;
#33169=AXIS2_PLACEMENT_3D ( 'NONE', #9835, #42064, #25276 ) ;
#33171=CARTESIAN_POINT ( 'NONE',  ( -8.427464958487524527, 14.67799636298092203, -42.48227204479578489 ) ) ;
#33172=DIRECTION ( 'NONE',  ( 0.5897727341282541502, 0.3900873262218164661, 0.7071067811865459074 ) ) ;
#33174=DIRECTION ( 'NONE',  ( -0.1961161351381840723, -2.837236618486510447E-16, -0.9805806756909202226 ) ) ;
#33176=CARTESIAN_POINT ( 'NONE',  ( 29.13393739769619728, -36.11618894467930119, -81.65000000000000568 ) ) ;
#33182=AXIS2_PLACEMENT_3D ( 'NONE', #19417, #42766, #6865 ) ;
#33183=CARTESIAN_POINT ( 'NONE',  ( 8.693390981131532413, 17.62014253445611800, -34.86893418027936775 ) ) ;
#33201=EDGE_CURVE ( 'NONE', #38136, #13016, #17696, .T. ) ;
#33211=ORIENTED_EDGE ( 'NONE', *, *, #45734, .T. ) ;
#33213=AXIS2_PLACEMENT_3D ( 'NONE', #17516, #33488, #49502 ) ;
#33214=FACE_OUTER_BOUND ( 'NONE', #19056, .T. ) ;
#33228=CARTESIAN_POINT ( 'NONE',  ( 16.13393739769620083, -45.61618894467940066, -49.33749999999999858 ) ) ;
#33229=CARTESIAN_POINT ( 'NONE',  ( -14.25993951570189999, -0.3776770037709330508, -34.64999999999999858 ) ) ;
#33232=CARTESIAN_POINT ( 'NONE',  ( -13.74979103991289975, -41.20090589574910211, -47.05386678597589878 ) ) ;
#33234=DIRECTION ( 'NONE',  ( 0.000000000000000000, 1.000000000000000000, 0.000000000000000000 ) ) ;
#33236=PLANE ( 'NONE',  #35883 ) ;
#33251=ORIENTED_EDGE ( 'NONE', *, *, #37996, .F. ) ;
#33254=VECTOR ( 'NONE', #21114, 1000.000000000000000 ) ;
#33263=CARTESIAN_POINT ( 'NONE',  ( 17.94517161182763942, -49.61615078444357607, -83.16479114451217924 ) ) ;
#33273=VERTEX_POINT ( 'NONE', #24415 ) ;
#33285=ORIENTED_EDGE ( 'NONE', *, *, #9506, .F. ) ;
#33287=B_SPLINE_CURVE_WITH_KNOTS ( 'NONE', 3,
 ( #24008, #36867, #48939, #966 ),
 .UNSPECIFIED., .F., .F.,
 ( 4, 4 ),
 ( 0.4931821390625270030, 20.02578215755499969 ),
 .UNSPECIFIED. ) ;
#33295=CARTESIAN_POINT ( 'NONE',  ( 46.63393739769619373, 7.878491304262099426, -34.64999999999999858 ) ) ;
#33311=ORIENTED_EDGE ( 'NONE', *, *, #4957, .F. ) ;
#33317=CARTESIAN_POINT ( 'NONE',  ( 41.95166363962292877, -37.61591301745547611, -80.56130022381232436 ) ) ;
#33353=CARTESIAN_POINT ( 'NONE',  ( 16.91199818135557109, 14.75900075713340165, -34.79644660940672907 ) ) ;
#33355=CARTESIAN_POINT ( 'NONE',  ( 5.057652393281839132, 1.468834192434126829, -59.64999999999999147 ) ) ;
#33360=EDGE_LOOP ( 'NONE', ( #44574, #14754, #18420, #47369, #24060, #41801, #49891, #17067, #33621, #2716, #10721, #38930 ) ) ;
#33379=VERTEX_POINT ( 'NONE', #14849 ) ;
#33382=CARTESIAN_POINT ( 'NONE',  ( 44.13393739769620083, 4.883811055320659733, -34.64999999999999858 ) ) ;
#33384=DIRECTION ( 'NONE',  ( -1.000000000000000000, 0.000000000000000000, 0.000000000000000000 ) ) ;
#33394=DIRECTION ( 'NONE',  ( 0.8660254037844390407, 0.4999999999999995004, 2.775557561562887037E-17 ) ) ;
#33397=AXIS2_PLACEMENT_3D ( 'NONE', #29962, #29706, #25513 ) ;
#33406=ORIENTED_EDGE ( 'NONE', *, *, #39873, .T. ) ;
#33409=ORIENTED_EDGE ( 'NONE', *, *, #18638, .T. ) ;
#33414=CARTESIAN_POINT ( 'NONE',  ( 43.02593272906347011, 8.636460564420850972, -71.37299277478172144 ) ) ;
#33417=CARTESIAN_POINT ( 'NONE',  ( 10.07017945893940869, -54.00735027851921188, -34.80997524098909679 ) ) ;
#33424=CARTESIAN_POINT ( 'NONE',  ( 28.13393739769619728, -22.54439217495490055, -47.64999999999999858 ) ) ;
#33428=ORIENTED_EDGE ( 'NONE', *, *, #23269, .T. ) ;
#33430=CARTESIAN_POINT ( 'NONE',  ( -16.54679035245789365, 5.671130177897621749, -49.45205420238420402 ) ) ;
#33431=CARTESIAN_POINT ( 'NONE',  ( 13.37178884610072060, 18.38381105532060644, -83.05213603420975232 ) ) ;
#33439=CIRCLE ( 'NONE', #2473, 2.499999999999998668 ) ;
#33454=DIRECTION ( 'NONE',  ( 0.8660254037844387076, 0.4999999999999998890, 0.000000000000000000 ) ) ;
#33456=EDGE_CURVE ( 'NONE', #49499, #26299, #24528, .T. ) ;
#33467=AXIS2_PLACEMENT_3D ( 'NONE', #25751, #29178, #1932 ) ;
#33476=CIRCLE ( 'NONE', #5885, 39.00000000000000711 ) ;
#33488=DIRECTION ( 'NONE',  ( 0.9223605572461988089, 0.3863301728269249447, 0.000000000000000000 ) ) ;
#33492=CARTESIAN_POINT ( 'NONE',  ( -1.470455565318980140, -50.51083130937980314, -36.42379920433069884 ) ) ;
#33499=DIRECTION ( 'NONE',  ( -1.000000000000000000, 0.000000000000000000, 0.000000000000000000 ) ) ;
#33502=CARTESIAN_POINT ( 'NONE',  ( 29.13393739769619728, 1.883811055320659955, -53.85091742636659973 ) ) ;
#33508=DIRECTION ( 'NONE',  ( 0.000000000000000000, 0.000000000000000000, -1.000000000000000000 ) ) ;
#33512=AXIS2_PLACEMENT_3D ( 'NONE', #41770, #29956, #6398 ) ;
#33519=CIRCLE ( 'NONE', #90, 2.999999999999999112 ) ;
#33530=CARTESIAN_POINT ( 'NONE',  ( 42.54468173148520549, -37.68289285273589684, -77.59564625393689141 ) ) ;
#33541=CARTESIAN_POINT ( 'NONE',  ( 28.90964706005109974, -26.65681833330370054, -34.73148477628539865 ) ) ;
#33558=AXIS2_PLACEMENT_3D ( 'NONE', #33228, #10436, #50008 ) ;
#33563=CARTESIAN_POINT ( 'NONE',  ( 20.63393739769620083, -41.61618894467930119, -54.64999999999999858 ) ) ;
#33567=CARTESIAN_POINT ( 'NONE',  ( -3.839728563314020349, -6.393788602144800493, -54.64999999999999858 ) ) ;
#33571=DIRECTION ( 'NONE',  ( 0.000000000000000000, -1.000000000000000000, 0.000000000000000000 ) ) ;
#33577=CARTESIAN_POINT ( 'NONE',  ( 44.54563194250441427, -37.98763156856614387, -67.59149508629086256 ) ) ;
#33587=VECTOR ( 'NONE', #7400, 1000.000000000000000 ) ;
#33591=EDGE_CURVE ( 'NONE', #42649, #37266, #7847, .T. ) ;
#33607=CARTESIAN_POINT ( 'NONE',  ( 35.31742556088838825, 11.23513843205707019, -54.64999999999999858 ) ) ;
#33617=DIRECTION ( 'NONE',  ( 0.000000000000000000, -0.7071067811865492381, 0.7071067811865457964 ) ) ;
#33621=ORIENTED_EDGE ( 'NONE', *, *, #6759, .T. ) ;
#33626=LINE ( 'NONE', #50144, #44552 ) ;
#33629=ORIENTED_EDGE ( 'NONE', *, *, #45563, .F. ) ;
#33644=CARTESIAN_POINT ( 'NONE',  ( 14.28038400710302724, 10.53025766472732450, -34.79644660940672907 ) ) ;
#33662=CARTESIAN_POINT ( 'NONE',  ( -1.143840380081567076, -15.61618894467929941, -35.76111111111109864 ) ) ;
#33664=EDGE_LOOP ( 'NONE', ( #10038, #1069, #48601, #12427, #47877, #41752 ) ) ;
#33667=ORIENTED_EDGE ( 'NONE', *, *, #43621, .T. ) ;
#33672=CARTESIAN_POINT ( 'NONE',  ( 43.96339835255960082, 8.719345853256658785, -66.83668497728366731 ) ) ;
#33679=ORIENTED_EDGE ( 'NONE', *, *, #38391, .T. ) ;
#33680=CARTESIAN_POINT ( 'NONE',  ( -22.84941987848104006, -15.84866128047474376, -54.74989008055889883 ) ) ;
#33684=ORIENTED_EDGE ( 'NONE', *, *, #7554, .F. ) ;
#33687=EDGE_CURVE ( 'NONE', #25181, #36007, #26231, .T. ) ;
#33691=ORIENTED_EDGE ( 'NONE', *, *, #19140, .F. ) ;
#33695=LINE ( 'NONE', #17219, #48798 ) ;
#33698=CARTESIAN_POINT ( 'NONE',  ( 2.458146360389407370, -5.580163940743402051, -34.79644291222906105 ) ) ;
#33709=VECTOR ( 'NONE', #51676, 1000.000000000000000 ) ;
#33720=ORIENTED_EDGE ( 'NONE', *, *, #41521, .F. ) ;
#33724=ORIENTED_EDGE ( 'NONE', *, *, #7281, .T. ) ;
#33734=LINE ( 'NONE', #2566, #36491 ) ;
#33743=CARTESIAN_POINT ( 'NONE',  ( -3.688670878366239858, -49.30016108328199920, -38.41768699663800390 ) ) ;
#33744=CARTESIAN_POINT ( 'NONE',  ( -0.1295185695942999982, 0.6472670226113349523, 4.943674098299870145 ) ) ;
#33756=ORIENTED_EDGE ( 'NONE', *, *, #36175, .T. ) ;
#33758=PLANE ( 'NONE',  #48753 ) ;
#33759=EDGE_CURVE ( 'NONE', #24768, #40719, #17504, .T. ) ;
#33764=ORIENTED_EDGE ( 'NONE', *, *, #10308, .T. ) ;
#33771=DIRECTION ( 'NONE',  ( 0.000000000000000000, 1.000000000000000000, 0.000000000000000000 ) ) ;
#33778=CARTESIAN_POINT ( 'NONE',  ( 29.07912664786299928, -4.512658877537830016, -34.92075920103120268 ) ) ;
#33781=CARTESIAN_POINT ( 'NONE',  ( 0.2392085819250069911, 19.81485081108809965, -34.59935833162420238 ) ) ;
#33783=CARTESIAN_POINT ( 'NONE',  ( 43.47966092493172852, -39.00974599031439283, -73.04851394742181014 ) ) ;
#33784=DIRECTION ( 'NONE',  ( -0.2846079131720410937, -0.9586440088791334801, 0.000000000000000000 ) ) ;
#33791=CARTESIAN_POINT ( 'NONE',  ( 41.27131287472999333, 8.477448802151759111, -79.73408454280998114 ) ) ;
#33792=LINE ( 'NONE', #49801, #20157 ) ;
#33795=CARTESIAN_POINT ( 'NONE',  ( 28.67375133668760157, -26.56866050586220140, -34.65024193067809222 ) ) ;
#33800=ORIENTED_EDGE ( 'NONE', *, *, #9163, .F. ) ;
#33819=ADVANCED_FACE ( 'NONE', ( #1263 ), #27909, .T. ) ;
#33822=EDGE_CURVE ( 'NONE', #13283, #32835, #34868, .T. ) ;
#33823=CARTESIAN_POINT ( 'NONE',  ( 39.83216070239956252, -15.95952177966980123, -34.79644660940672907 ) ) ;
#33824=CARTESIAN_POINT ( 'NONE',  ( 11.63393739769619906, -41.61618894467930119, -35.14999999999999858 ) ) ;
#33825=EDGE_CURVE ( 'NONE', #46428, #6450, #17864, .T. ) ;
#33828=CARTESIAN_POINT ( 'NONE',  ( 0.1294298976606224894, -20.72822689018533637, -34.68804011290717426 ) ) ;
#33829=CARTESIAN_POINT ( 'NONE',  ( 44.57690765188346660, -37.99148801630303751, -67.43510758073952616 ) ) ;
#33845=CARTESIAN_POINT ( 'NONE',  ( 41.79440130354939242, -39.74212845547013018, -77.32389498022952523 ) ) ;
#33851=EDGE_CURVE ( 'NONE', #30043, #25181, #46775, .T. ) ;
#33857=DIRECTION ( 'NONE',  ( 0.6339889056055382222, 0.000000000000000000, -0.7733421413379021336 ) ) ;
#33858=CARTESIAN_POINT ( 'NONE',  ( 38.67452568954060155, -15.61618894467929941, -81.65000000000000568 ) ) ;
#33860=FACE_OUTER_BOUND ( 'NONE', #43503, .T. ) ;
#33866=PLANE ( 'NONE',  #31604 ) ;
#33883=ADVANCED_FACE ( 'NONE', ( #19760 ), #11917, .T. ) ;
#33886=CARTESIAN_POINT ( 'NONE',  ( 45.33172459800163523, 6.848706388641467413, -63.66100526906988222 ) ) ;
#33893=VERTEX_POINT ( 'NONE', #26374 ) ;
#33897=CARTESIAN_POINT ( 'NONE',  ( 47.13393739769619373, 7.029298498933709283, -54.64999999999999858 ) ) ;
#33899=CARTESIAN_POINT ( 'NONE',  ( 14.13393739769639801, 10.38381105532069171, -35.01561944896768352 ) ) ;
#33923=DIRECTION ( 'NONE',  ( -0.1961161351381831008, 1.073215590470984393E-15, -0.9805806756909204447 ) ) ;
#33926=CARTESIAN_POINT ( 'NONE',  ( 43.11479320284178129, 8.644770638213781666, -70.94330782894907372 ) ) ;
#33933=ORIENTED_EDGE ( 'NONE', *, *, #33591, .T. ) ;
#33944=VERTEX_POINT ( 'NONE', #12165 ) ;
#33952=CARTESIAN_POINT ( 'NONE',  ( 33.13393739769620083, 7.383811055320659733, -84.65000000000000568 ) ) ;
#33953=DIRECTION ( 'NONE',  ( 0.000000000000000000, 0.000000000000000000, 1.000000000000000000 ) ) ;
#33956=DIRECTION ( 'NONE',  ( 0.5516667872527449834, 0.8340645993220396903, 2.775557561562889194E-17 ) ) ;
#33959=VECTOR ( 'NONE', #11717, 1000.000000000000000 ) ;
#33968=EDGE_CURVE ( 'NONE', #21257, #41771, #113, .T. ) ;
#33969=STYLED_ITEM ( 'NONE', ( #7507 ), #10093 ) ;
#33978=CARTESIAN_POINT ( 'NONE',  ( 29.46622902366960162, 1.883811055320659955, -54.64999999999999858 ) ) ;
#33979=CARTESIAN_POINT ( 'NONE',  ( 46.99731062513885149, 8.001896800055366299, -34.80647497723111883 ) ) ;
#33983=CARTESIAN_POINT ( 'NONE',  ( 19.33046814882964881, -49.25056949571164466, -34.64999999999999858 ) ) ;
#33985=LINE ( 'NONE', #38458, #48723 ) ;
#33988=CIRCLE ( 'NONE', #11429, 39.00000000000000711 ) ;
#33990=ORIENTED_EDGE ( 'NONE', *, *, #37546, .F. ) ;
#33995=AXIS2_PLACEMENT_3D ( 'NONE', #24293, #4657, #18461 ) ;
#33997=EDGE_LOOP ( 'NONE', ( #41512, #35283, #8967, #14952, #48662, #46789, #15248 ) ) ;
#33998=EDGE_CURVE ( 'NONE', #11865, #9063, #32055, .T. ) ;
#33999=CARTESIAN_POINT ( 'NONE',  ( -19.00919503052239889, -32.92138004297220277, -51.31717196595420205 ) ) ;
#34001=CARTESIAN_POINT ( 'NONE',  ( -12.25993951570199947, -34.31880250072530458, -34.64999999999999858 ) ) ;
#34008=ORIENTED_EDGE ( 'NONE', *, *, #26416, .F. ) ;
#34009=LINE ( 'NONE', #34533, #12432 ) ;
#34034=CARTESIAN_POINT ( 'NONE',  ( -9.375152675533279023, 14.02725416202859954, -42.91803494044829392 ) ) ;
#34036=CARTESIAN_POINT ( 'NONE',  ( 46.48809362348643504, -39.29542413733557993, -58.13476177693350877 ) ) ;
#34050=CIRCLE ( 'NONE', #14813, 3.000000000000004885 ) ;
#34053=ORIENTED_EDGE ( 'NONE', *, *, #18756, .F. ) ;
#34065=ORIENTED_EDGE ( 'NONE', *, *, #31950, .F. ) ;
#34083=CARTESIAN_POINT ( 'NONE',  ( 43.85723124748935930, -37.89848476597786231, -71.03349786720269776 ) ) ;
#34093=ORIENTED_EDGE ( 'NONE', *, *, #39733, .F. ) ;
#34097=CARTESIAN_POINT ( 'NONE',  ( 46.70917532059600319, -39.13647700890110315, -34.65437117444129456 ) ) ;
#34135=B_SPLINE_CURVE_WITH_KNOTS ( 'NONE', 3,
 ( #35326, #40038, #47402, #3114, #19600, #11755, #47650, #15161, #46891, #51832 ),
 .UNSPECIFIED., .F., .F.,
 ( 4, 2, 2, 2, 4 ),
 ( -0.0004107207313030360294, 0.000000000000000000, 0.01419180571504649949, 0.04450164637014340785, 0.05031563485850510525 ),
 .UNSPECIFIED. ) ;
#34137=CARTESIAN_POINT ( 'NONE',  ( 2.422196078461449797, -25.82482932757800143, -35.02873218748179340 ) ) ;
#34140=CARTESIAN_POINT ( 'NONE',  ( 45.26400037985666813, 6.841219675276395407, -63.99964612493251792 ) ) ;
#34147=CYLINDRICAL_SURFACE ( 'NONE', #50104, 39.00000000000000711 ) ;
#34150=EDGE_CURVE ( 'NONE', #1146, #24768, #36715, .T. ) ;
#34157=CARTESIAN_POINT ( 'NONE',  ( 19.21265657477752598, -49.46974233527256359, -34.79644660940672907 ) ) ;
#34163=B_SPLINE_CURVE_WITH_KNOTS ( 'NONE', 3,
 ( #51440, #3745, #15785, #11872, #43321, #7415, #34920, #10832, #14758, #23114 ),
 .UNSPECIFIED., .F., .F.,
 ( 4, 2, 2, 2, 4 ),
 ( -0.1857717838147150136, -0.1853436703551470111, -0.1652145016229930041, -0.1459149143040530117, -0.1350635247378738635 ),
 .UNSPECIFIED. ) ;
#34164=CARTESIAN_POINT ( 'NONE',  ( 3.768317948728554079, -22.75548266223732341, -34.65000000000000568 ) ) ;
#34165=CYLINDRICAL_SURFACE ( 'NONE', #49476, 0.4999999999999980571 ) ;
#34167=ADVANCED_FACE ( 'NONE', ( #31570 ), #27651, .T. ) ;
#34176=ORIENTED_EDGE ( 'NONE', *, *, #18275, .T. ) ;
#34182=CARTESIAN_POINT ( 'NONE',  ( 46.03612365166910791, 8.863419595963454967, -56.78333922229177944 ) ) ;
#34193=ORIENTED_EDGE ( 'NONE', *, *, #6010, .F. ) ;
#34203=EDGE_CURVE ( 'NONE', #12629, #21587, #11179, .T. ) ;
#34219=CARTESIAN_POINT ( 'NONE',  ( 44.71501321890448821, -40.01020284909822777, -63.19468146700351951 ) ) ;
#34228=EDGE_LOOP ( 'NONE', ( #2672, #43511, #46226, #40215 ) ) ;
#34231=FACE_OUTER_BOUND ( 'NONE', #11487, .T. ) ;
#34232=LINE ( 'NONE', #33978, #5139 ) ;
#34237=CARTESIAN_POINT ( 'NONE',  ( 9.026390854478798076, 16.60930999848670098, -54.64999999999999858 ) ) ;
#34238=CARTESIAN_POINT ( 'NONE',  ( 0.4371248283887909647, -22.38658506580789975, -35.02873218748179340 ) ) ;
#34241=CARTESIAN_POINT ( 'NONE',  ( 29.13393739769619728, -33.11618894467940066, -53.85091742636659973 ) ) ;
#34248=PLANE ( 'NONE',  #50227 ) ;
#34254=CARTESIAN_POINT ( 'NONE',  ( 0.9246403334604839097, -51.52825870078270043, -34.45773271021280237 ) ) ;
#34268=ADVANCED_FACE ( 'NONE', ( #51517 ), #20293, .T. ) ;
#34272=ADVANCED_FACE ( 'NONE', ( #35783 ), #51767, .T. ) ;
#34277=CARTESIAN_POINT ( 'NONE',  ( 17.63393739769620083, -32.15793020853440254, -34.64999999999999858 ) ) ;
#34278=ORIENTED_EDGE ( 'NONE', *, *, #7158, .F. ) ;
#34279=B_SPLINE_CURVE_WITH_KNOTS ( 'NONE', 3,
 ( #38683, #18741, #50978, #14300, #42345, #30269, #11155, #19001, #6447, #30782, #46810, #22918 ),
 .UNSPECIFIED., .F., .F.,
 ( 4, 2, 2, 2, 2, 4 ),
 ( 0.000000000000000000, 0.1249999999999997780, 0.2499999999999995559, 0.4999999999999996669, 0.7499999999999997780, 1.000000000000000000 ),
 .UNSPECIFIED. ) ;
#34292=EDGE_CURVE ( 'NONE', #6345, #40975, #27903, .T. ) ;
#34295=CARTESIAN_POINT ( 'NONE',  ( 0.02643090884201690013, 19.86906729127069937, -34.96342131435890366 ) ) ;
#34297=CARTESIAN_POINT ( 'NONE',  ( 42.78911202776321687, -38.92818100861666863, -76.46643483648848871 ) ) ;
#34298=AXIS2_PLACEMENT_3D ( 'NONE', #5542, #9475, #25422 ) ;
#34299=ADVANCED_FACE ( 'NONE', ( #36805 ), #24566, .T. ) ;
#34305=EDGE_LOOP ( 'NONE', ( #26558, #34391, #10505, #12742 ) ) ;
#34306=CARTESIAN_POINT ( 'NONE',  ( 46.39380079123251477, 9.013081426918761352, -54.52813979131429534 ) ) ;
#34330=DIRECTION ( 'NONE',  ( 0.000000000000000000, 0.000000000000000000, -1.000000000000000000 ) ) ;
#34334=ORIENTED_EDGE ( 'NONE', *, *, #28370, .F. ) ;
#34335=CARTESIAN_POINT ( 'NONE',  ( 18.13393739769620083, -41.61618894467930119, -54.64999999999999858 ) ) ;
#34338=CARTESIAN_POINT ( 'NONE',  ( 0.1457841021255935343, -26.78123956999450428, -34.68167779225149161 ) ) ;
#34346=CARTESIAN_POINT ( 'NONE',  ( 44.45943562239641977, -37.97683504137048516, -68.02249989722677981 ) ) ;
#34361=CARTESIAN_POINT ( 'NONE',  ( 41.20166900923489095, -39.67422119637704725, -80.18288832365365693 ) ) ;
#34363=EDGE_CURVE ( 'NONE', #677, #37056, #41263, .T. ) ;
#34366=EDGE_LOOP ( 'NONE', ( #33311, #10641, #31843, #34715, #47371 ) ) ;
#34367=( BOUNDED_CURVE ( )  B_SPLINE_CURVE ( 3, ( #34589, #30653, #7345, #43504 ),
 .UNSPECIFIED., .F., .T. ) 
 B_SPLINE_CURVE_WITH_KNOTS ( ( 4, 4 ),
 ( 4.712388980384689674, 4.724464978221631917 ),
 .UNSPECIFIED. ) 
 CURVE ( )  GEOMETRIC_REPRESENTATION_ITEM ( )  RATIONAL_B_SPLINE_CURVE ( ( 1.000000000000000000, 0.9999878475599406347, 0.9999878475599406347, 1.000000000000000000 ) ) 
 REPRESENTATION_ITEM ( '' )  );
#34373=CARTESIAN_POINT ( 'NONE',  ( 20.63393739769599833, 10.38381105532070059, -35.14999999999999858 ) ) ;
#34379=CARTESIAN_POINT ( 'NONE',  ( 17.98749448546718455, 1.245406012443906807, -34.79644291222912500 ) ) ;
#34390=B_SPLINE_CURVE_WITH_KNOTS ( 'NONE', 3,
 ( #46437, #8319, #28217, #44218, #43018, #30415, #43275, #31437, #38828, #26744, #40292, #448, #18631, #46960, #6856, #47465 ),
 .UNSPECIFIED., .F., .F.,
 ( 4, 2, 2, 2, 2, 2, 2, 4 ),
 ( 0.000000000000000000, 0.1191611659050043209, 0.1489514573812555642, 0.1787417488575067936, 0.2383223318100099186, 0.2979029147625130158, 0.3574834977150160853, 0.4766446636200218356 ),
 .UNSPECIFIED. ) ;
#34391=ORIENTED_EDGE ( 'NONE', *, *, #5721, .T. ) ;
#34401=CARTESIAN_POINT ( 'NONE',  ( 45.15161791705966721, 6.828204371508110881, -64.56158714047771241 ) ) ;
#34402=CARTESIAN_POINT ( 'NONE',  ( -17.65868355449891069, 3.871249156093727439, -50.40641985204897679 ) ) ;
#34406=CARTESIAN_POINT ( 'NONE',  ( 16.13393739769620083, -15.61618894467929941, -644.5164532144519853 ) ) ;
#34410=CYLINDRICAL_SURFACE ( 'NONE', #46953, 2.999999999999994227 ) ;
#34412=EDGE_CURVE ( 'NONE', #6571, #24387, #40483, .T. ) ;
#34417=ADVANCED_FACE ( 'NONE', ( #12447 ), #2003, .F. ) ;
#34438=DIRECTION ( 'NONE',  ( 0.000000000000000000, 0.000000000000000000, 1.000000000000000000 ) ) ;
#34453=AXIS2_PLACEMENT_3D ( 'NONE', #41219, #20767, #37290 ) ;
#34454=CARTESIAN_POINT ( 'NONE',  ( 40.57649240635721100, -15.61618894467929941, -83.97002642401369599 ) ) ;
#34467=EDGE_CURVE ( 'NONE', #42352, #14961, #9042, .T. ) ;
#34468=EDGE_LOOP ( 'NONE', ( #27316, #39226, #25862, #3137, #47435 ) ) ;
#34474=CARTESIAN_POINT ( 'NONE',  ( 2.428024600086259976, -5.435758813730029892, -34.95504743437659556 ) ) ;
#34482=CARTESIAN_POINT ( 'NONE',  ( 46.99617165126079499, 8.227715268217000499, -54.09194780417729476 ) ) ;
#34485=ORIENTED_EDGE ( 'NONE', *, *, #22929, .T. ) ;
#34486=B_SPLINE_CURVE_WITH_KNOTS ( 'NONE', 3,
 ( #28930, #40224, #28406, #12713, #29188, #24724 ),
 .UNSPECIFIED., .F., .F.,
 ( 4, 2, 4 ),
 ( -0.1582496144710479891, -0.1579281415405880129, -0.1400863131347609980 ),
 .UNSPECIFIED. ) ;
#34492=CARTESIAN_POINT ( 'NONE',  ( 44.35280653673021334, -39.98289970179189368, -64.95046479719039212 ) ) ;
#34502=ORIENTED_EDGE ( 'NONE', *, *, #33093, .T. ) ;
#34520=DIRECTION ( 'NONE',  ( 0.000000000000000000, 0.000000000000000000, -1.000000000000000000 ) ) ;
#34524=VERTEX_POINT ( 'NONE', #27248 ) ;
#34526=DIRECTION ( 'NONE',  ( 0.000000000000000000, 0.000000000000000000, -1.000000000000000000 ) ) ;
#34533=CARTESIAN_POINT ( 'NONE',  ( 14.63393739769620083, -42.11618894467930119, -34.64999999999999858 ) ) ;
#34537=DIRECTION ( 'NONE',  ( 0.000000000000000000, 0.000000000000000000, -1.000000000000000000 ) ) ;
#34538=EDGE_CURVE ( 'NONE', #26276, #2299, #39833, .T. ) ;
#34548=CARTESIAN_POINT ( 'NONE',  ( 1.277530937145179957, -21.88413813711040135, -34.64999999999999858 ) ) ;
#34549=ORIENTED_EDGE ( 'NONE', *, *, #9038, .T. ) ;
#34555=VECTOR ( 'NONE', #9036, 1000.000000000000000 ) ;
#34559=CARTESIAN_POINT ( 'NONE',  ( -21.93025022046069950, -6.936381044561869658, -53.85448886108699185 ) ) ;
#34563=DIRECTION ( 'NONE',  ( 0.000000000000000000, 1.000000000000000000, 0.000000000000000000 ) ) ;
#34568=CARTESIAN_POINT ( 'NONE',  ( 44.98679317390966048, 8.902100338333454488, -61.45383541554941331 ) ) ;
#34580=ADVANCED_FACE ( 'NONE', ( #8377 ), #49714, .T. ) ;
#34589=CARTESIAN_POINT ( 'NONE',  ( 44.07452568954059302, -33.11618894467940066, -54.64999999999999858 ) ) ;
#34594=EDGE_LOOP ( 'NONE', ( #10320, #44932, #48437, #44623, #35802 ) ) ;
#34595=CARTESIAN_POINT ( 'NONE',  ( 31.79224979287389985, -36.11618894467930119, -84.65000000000000568 ) ) ;
#34598=EDGE_LOOP ( 'NONE', ( #18601, #47929, #45575, #18801, #12031 ) ) ;
#34599=AXIS2_PLACEMENT_3D ( 'NONE', #50418, #42292, #17211 ) ;
#34600=DIRECTION ( 'NONE',  ( -1.000000000000000000, 0.000000000000000000, 0.000000000000000000 ) ) ;
#34604=ADVANCED_FACE ( 'NONE', ( #4181 ), #6201, .T. ) ;
#34607=CARTESIAN_POINT ( 'NONE',  ( 45.31728293652347617, -38.07934818043975866, -63.73322212158187483 ) ) ;
#34613=CARTESIAN_POINT ( 'NONE',  ( 17.25678305769739751, -43.96113075119600211, -62.64999999999999858 ) ) ;
#34623=CARTESIAN_POINT ( 'NONE',  ( 46.67317881810730285, -39.12423041205359908, -34.65023821785899116 ) ) ;
#34636=FACE_OUTER_BOUND ( 'NONE', #33142, .T. ) ;
#34638=ADVANCED_FACE ( 'NONE', ( #3681 ), #8, .F. ) ;
#34649=EDGE_LOOP ( 'NONE', ( #6239, #28010, #12805, #2066 ) ) ;
#34650=AXIS2_PLACEMENT_3D ( 'NONE', #15615, #39718, #19794 ) ;
#34661=CARTESIAN_POINT ( 'NONE',  ( 43.60039976138143913, 6.630830045952984975, -72.31767848873290916 ) ) ;
#34666=DIRECTION ( 'NONE',  ( -0.3502816565540492477, 0.000000000000000000, 0.9366444154970182678 ) ) ;
#34671=SHAPE_REPRESENTATION_RELATIONSHIP ( 'NONE' , 'NONE' ,  #28088, #14816 ) ;
#34673=CIRCLE ( 'NONE', #43890, 34.41780050634729804 ) ;
#34677=CARTESIAN_POINT ( 'NONE',  ( 30.13393739769619728, 7.383811055320659733, -59.64999999999999147 ) ) ;
#34699=CARTESIAN_POINT ( 'NONE',  ( 28.13393739769619728, -22.54439217495490055, -47.64999999999999858 ) ) ;
#34707=DIRECTION ( 'NONE',  ( -0.7071067811865510144, -0.7071067811865440200, 0.000000000000000000 ) ) ;
#34708=FACE_OUTER_BOUND ( 'NONE', #45583, .T. ) ;
#34711=DIRECTION ( 'NONE',  ( 0.000000000000000000, 0.000000000000000000, -1.000000000000000000 ) ) ;
#34715=ORIENTED_EDGE ( 'NONE', *, *, #34879, .F. ) ;
#34720=CARTESIAN_POINT ( 'NONE',  ( 41.61626771661330082, 4.883811055320659733, -82.23834840541459812 ) ) ;
#34727=CARTESIAN_POINT ( 'NONE',  ( 0.2019267050626805393, -46.05559318631305388, -34.66067870389102978 ) ) ;
#34743=CARTESIAN_POINT ( 'NONE',  ( 45.98590630150382452, -40.09308313156154213, -57.02683514883391069 ) ) ;
#34746=AXIS2_PLACEMENT_3D ( 'NONE', #6605, #45662, #46197 ) ;
#34756=ORIENTED_EDGE ( 'NONE', *, *, #47912, .T. ) ;
#34757=EDGE_CURVE ( 'NONE', #27942, #38690, #20465, .T. ) ;
#34773=VERTEX_POINT ( 'NONE', #44792 ) ;
#34777=CYLINDRICAL_SURFACE ( 'NONE', #10984, 0.5000000000000000000 ) ;
#34783=VECTOR ( 'NONE', #20830, 1000.000000000000114 ) ;
#34791=CARTESIAN_POINT ( 'NONE',  ( 16.13393739769620083, -15.61618894467929941, -54.64999999999999858 ) ) ;
#34793=EDGE_LOOP ( 'NONE', ( #2464, #42278, #3417, #25502 ) ) ;
#34807=CARTESIAN_POINT ( 'NONE',  ( 46.68560842045859971, -39.85656240628109970, -54.55231085272809821 ) ) ;
#34811=DIRECTION ( 'NONE',  ( 0.5000000000000012212, 0.8660254037844380415, 0.000000000000000000 ) ) ;
#34813=CARTESIAN_POINT ( 'NONE',  ( 8.744443678271828446, -48.95118247924426669, -34.77532226276707661 ) ) ;
#34818=CARTESIAN_POINT ( 'NONE',  ( -21.99696017279149984, -6.875435248926140552, -54.08310780595149936 ) ) ;
#34824=EDGE_CURVE ( 'NONE', #6632, #46602, #51563, .T. ) ;
#34827=VERTEX_POINT ( 'NONE', #15149 ) ;
#34828=CARTESIAN_POINT ( 'NONE',  ( 44.51201659540226530, 8.863513744426830598, -63.77110661413982484 ) ) ;
#34837=CARTESIAN_POINT ( 'NONE',  ( 15.29511290902279974, -43.80059717415329601, -59.64999999999999147 ) ) ;
#34849=ORIENTED_EDGE ( 'NONE', *, *, #14209, .F. ) ;
#34850=DIRECTION ( 'NONE',  ( -0.3502816565540492477, 0.000000000000000000, 0.9366444154970182678 ) ) ;
#34863=CARTESIAN_POINT ( 'NONE',  ( 17.63393739769620083, -32.15793020853440254, -34.64999999999999858 ) ) ;
#34867=ORIENTED_EDGE ( 'NONE', *, *, #12703, .F. ) ;
#34868=B_SPLINE_CURVE_WITH_KNOTS ( 'NONE', 3,
 ( #17001, #32948, #48974, #13080 ),
 .UNSPECIFIED., .F., .F.,
 ( 4, 4 ),
 ( 0.000000000000000000, 1.000000000000000000 ),
 .UNSPECIFIED. ) ;
#34872=AXIS2_PLACEMENT_3D ( 'NONE', #5475, #37432, #25610 ) ;
#34876=EDGE_CURVE ( 'NONE', #25290, #20336, #43022, .T. ) ;
#34879=EDGE_CURVE ( 'NONE', #16544, #12971, #22876, .T. ) ;
#34909=DIRECTION ( 'NONE',  ( 0.000000000000000000, 1.000000000000000000, 0.000000000000000000 ) ) ;
#34920=CARTESIAN_POINT ( 'NONE',  ( 0.7461747575530269794, -8.744437018640690340, -34.70985242058479514 ) ) ;
#34924=CARTESIAN_POINT ( 'NONE',  ( 44.97616441016351274, 6.807270547622365164, -65.43885644857014938 ) ) ;
#34928=DIRECTION ( 'NONE',  ( 1.000000000000000000, 0.000000000000000000, 0.000000000000000000 ) ) ;
#34935=EDGE_CURVE ( 'NONE', #24695, #24503, #24719, .T. ) ;
#34937=ADVANCED_FACE ( 'NONE', ( #36792 ), #32955, .T. ) ;
#34948=CARTESIAN_POINT ( 'NONE',  ( 12.98614995704589248, 18.60725077530888782, -82.44267625234913055 ) ) ;
#34957=DIRECTION ( 'NONE',  ( 1.000000000000000000, 0.000000000000000000, 0.000000000000000000 ) ) ;
#34962=CARTESIAN_POINT ( 'NONE',  ( 20.63393739769619017, -41.61618894467939356, -35.01561944896766221 ) ) ;
#34969=CARTESIAN_POINT ( 'NONE',  ( 15.29511290902279974, -43.80059717415329601, -59.64999999999999147 ) ) ;
#34972=ORIENTED_EDGE ( 'NONE', *, *, #27181, .F. ) ;
#34975=ORIENTED_EDGE ( 'NONE', *, *, #44250, .T. ) ;
#34979=CONICAL_SURFACE ( 'NONE', #29915, 19.50000000000000000, 0.2449786631268651149 ) ;
#34980=ORIENTED_EDGE ( 'NONE', *, *, #45330, .F. ) ;
#34982=VERTEX_POINT ( 'NONE', #16895 ) ;
#34986=CARTESIAN_POINT ( 'NONE',  ( 44.97883126316192204, 2.004041975891398764, -38.63153946226272950 ) ) ;
#34994=CARTESIAN_POINT ( 'NONE',  ( 0.9903310742090041252, -22.56644434022149781, -34.65032322548069743 ) ) ;
#34997=VERTEX_POINT ( 'NONE', #19841 ) ;
#34998=B_SPLINE_CURVE_WITH_KNOTS ( 'NONE', 3,
 ( #33295, #33026, #4232, #49311, #48262, #13406, #28583, #24896, #48783, #44583 ),
 .UNSPECIFIED., .F., .F.,
 ( 4, 2, 2, 2, 4 ),
 ( -0.0003341005055044069861, 0.000000000000000000, 0.01143402714056380130, 0.02281319364104390096, 0.04082353370410345822 ),
 .UNSPECIFIED. ) ;
#35002=CARTESIAN_POINT ( 'NONE',  ( 45.56211211820503593, -40.06741977676035305, -59.08583076237255227 ) ) ;
#35005=FILL_AREA_STYLE_COLOUR ( '', #27296 ) ;
#35016=VERTEX_POINT ( 'NONE', #32575 ) ;
#35019=CARTESIAN_POINT ( 'NONE',  ( -0.4410626023037880206, -3.737207156102679839, -35.14999999999999858 ) ) ;
#35025=DIRECTION ( 'NONE',  ( -0.6561787149247867434, 0.000000000000000000, 0.7546055221635046273 ) ) ;
#35028=ORIENTED_EDGE ( 'NONE', *, *, #24807, .F. ) ;
#35029=ORIENTED_EDGE ( 'NONE', *, *, #22235, .T. ) ;
#35044=ORIENTED_EDGE ( 'NONE', *, *, #5906, .T. ) ;
#35048=CIRCLE ( 'NONE', #39215, 2.999999999999994227 ) ;
#35050=AXIS2_PLACEMENT_3D ( 'NONE', #6059, #22017, #6320 ) ;
#35057=EDGE_CURVE ( 'NONE', #14108, #16597, #49392, .T. ) ;
#35061=CARTESIAN_POINT ( 'NONE',  ( 46.53772422082609950, -40.04183304982790048, -54.64305748561629628 ) ) ;
#35069=AXIS2_PLACEMENT_3D ( 'NONE', #8132, #258, #29065 ) ;
#35074=CARTESIAN_POINT ( 'NONE',  ( 46.66163704272000246, -38.09001934925220212, -56.99730829862610193 ) ) ;
#35075=PLANE ( 'NONE',  #29367 ) ;
#35078=VERTEX_POINT ( 'NONE', #37061 ) ;
#35083=CARTESIAN_POINT ( 'NONE',  ( 45.28026775681226468, 6.614598366022641507, -63.87362864251259964 ) ) ;
#35092=CARTESIAN_POINT ( 'NONE',  ( 16.13393739769620083, -15.61618894467929941, -54.64999999999999858 ) ) ;
#35100=DIRECTION ( 'NONE',  ( 0.000000000000000000, 0.000000000000000000, -1.000000000000000000 ) ) ;
#35101=B_SPLINE_CURVE_WITH_KNOTS ( 'NONE', 3,
 ( #7308, #23259, #4138, #43974, #4917, #16983, #35851, #12268 ),
 .UNSPECIFIED., .F., .F.,
 ( 4, 2, 2, 4 ),
 ( 0.1514974462201259253, 0.1570050336056500184, 0.1722850272388009862, 0.1726615410485390079 ),
 .UNSPECIFIED. ) ;
#35106=ORIENTED_EDGE ( 'NONE', *, *, #620, .T. ) ;
#35123=EDGE_LOOP ( 'NONE', ( #3825, #5460, #13991, #13282 ) ) ;
#35128=VECTOR ( 'NONE', #42657, 1000.000000000000000 ) ;
#35144=B_SPLINE_CURVE_WITH_KNOTS ( 'NONE', 3,
 ( #15476, #27771, #31941, #47963 ),
 .UNSPECIFIED., .F., .F.,
 ( 4, 4 ),
 ( 0.000000000000000000, 1.000000000000000000 ),
 .UNSPECIFIED. ) ;
#35160=VECTOR ( 'NONE', #30790, 1000.000000000000000 ) ;
#35170=AXIS2_PLACEMENT_3D ( 'NONE', #1976, #33923, #22905 ) ;
#35178=VERTEX_POINT ( 'NONE', #9553 ) ;
#35185=CARTESIAN_POINT ( 'NONE',  ( 43.20094691158656985, 6.574965196572723158, -74.31491011093504540 ) ) ;
#35191=AXIS2_PLACEMENT_3D ( 'NONE', #14320, #13559, #46308 ) ;
#35207=EDGE_LOOP ( 'NONE', ( #18223, #18737, #42605, #40713, #49585, #35514 ) ) ;
#35212=CARTESIAN_POINT ( 'NONE',  ( 2.404741263826640107, -5.380232784273969671, -35.14999999999999858 ) ) ;
#35218=DIRECTION ( 'NONE',  ( 0.000000000000000000, 0.000000000000000000, -1.000000000000000000 ) ) ;
#35219=CARTESIAN_POINT ( 'NONE',  ( 16.13393739769599833, 14.38381105532070059, -49.33749999999999858 ) ) ;
#35228=ORIENTED_EDGE ( 'NONE', *, *, #13626, .F. ) ;
#35232=CARTESIAN_POINT ( 'NONE',  ( 46.11714933639719760, 8.867842174310458958, -56.39015576205443381 ) ) ;
#35235=VERTEX_POINT ( 'NONE', #3496 ) ;
#35237=ORIENTED_EDGE ( 'NONE', *, *, #26436, .T. ) ;
#35243=EDGE_CURVE ( 'NONE', #1811, #42352, #17127, .T. ) ;
#35244=PRODUCT_DEFINITION_FORMATION_WITH_SPECIFIED_SOURCE ( 'ANY', '', #21513, .NOT_KNOWN. ) ;
#35245=CIRCLE ( 'NONE', #12654, 0.4999999999999982236 ) ;
#35254=B_SPLINE_CURVE_WITH_KNOTS ( 'NONE', 3,
 ( #8827, #12763, #24255, #435, #47887, #35824, #957, #32120, #16954, #43948, #16422, #32639, #39761 ),
 .UNSPECIFIED., .F., .F.,
 ( 4, 2, 2, 1, 2, 2, 4 ),
 ( 0.000000000000000000, 0.2500000000000033307, 0.3750000000000147660, 0.4375000000000204836, 0.4687500000000233702, 0.5000000000000262013, 1.000000000000000000 ),
 .UNSPECIFIED. ) ;
#35271=CARTESIAN_POINT ( 'NONE',  ( 45.79170134131306469, -40.08162185648630782, -57.97045409603698829 ) ) ;
#35283=ORIENTED_EDGE ( 'NONE', *, *, #20863, .T. ) ;
#35287=CARTESIAN_POINT ( 'NONE',  ( 3.633937397696210159, -8.399310579809009525, -34.64999999999999858 ) ) ;
#35290=DIRECTION ( 'NONE',  ( 0.000000000000000000, -0.7071067811865466846, -0.7071067811865483499 ) ) ;
#35292=CARTESIAN_POINT ( 'NONE',  ( -0.1826151910073069984, -10.64742273529058636, -34.92526559962323063 ) ) ;
#35295=ORIENTED_EDGE ( 'NONE', *, *, #36134, .T. ) ;
#35298=ADVANCED_FACE ( 'NONE', ( #22866 ), #43059, .F. ) ;
#35305=EDGE_LOOP ( 'NONE', ( #43970, #7670, #8697, #44658 ) ) ;
#35307=CARTESIAN_POINT ( 'NONE',  ( 31.79224979287389985, 4.883811055320679273, -84.65000000000000568 ) ) ;
#35316=AXIS2_PLACEMENT_3D ( 'NONE', #47618, #46857, #7016 ) ;
#35323=EDGE_CURVE ( 'NONE', #15666, #27249, #40533, .T. ) ;
#35326=CARTESIAN_POINT ( 'NONE',  ( 8.943569970476479725, 18.10127401595480023, -34.64999999999999858 ) ) ;
#35334=DIRECTION ( 'NONE',  ( 0.5835456732599438867, -0.8120803206700670795, 0.000000000000000000 ) ) ;
#35340=CARTESIAN_POINT ( 'NONE',  ( 47.31175340403380147, -38.13240412724670136, -53.74300098232180289 ) ) ;
#35348=CARTESIAN_POINT ( 'NONE',  ( 42.84191978890740415, 7.628041268320568946, -76.47496320122499469 ) ) ;
#35360=ADVANCED_FACE ( 'NONE', ( #26544 ), #6650, .T. ) ;
#35376=DIRECTION ( 'NONE',  ( 1.000000000000000000, 0.000000000000000000, 0.000000000000000000 ) ) ;
#35384=CARTESIAN_POINT ( 'NONE',  ( 46.40825105427388308, -38.19443686813398386, -58.27843028287923488 ) ) ;
#35397=CARTESIAN_POINT ( 'NONE',  ( 9.995687254860799342, 22.60556764129900031, -34.69483829921999529 ) ) ;
#35399=EDGE_CURVE ( 'NONE', #26463, #43797, #7951, .T. ) ;
#35405=DIRECTION ( 'NONE',  ( -1.000000000000000000, 0.000000000000000000, 0.000000000000000000 ) ) ;
#35408=ORIENTED_EDGE ( 'NONE', *, *, #447, .F. ) ;
#35430=CARTESIAN_POINT ( 'NONE',  ( 16.13393739769620083, -1.590680505402594314, -34.79644660940672196 ) ) ;
#35443=ORIENTED_EDGE ( 'NONE', *, *, #34363, .F. ) ;
#35444=CARTESIAN_POINT ( 'NONE',  ( 0.4371248283887909647, -22.38658506580789975, -35.02873218748179340 ) ) ;
#35445=CARTESIAN_POINT ( 'NONE',  ( 42.66764366557126920, 6.495846304519615977, -76.98140147941434464 ) ) ;
#35446=EDGE_CURVE ( 'NONE', #11926, #17858, #28339, .T. ) ;
#35450=AXIS2_PLACEMENT_3D ( 'NONE', #4040, #24433, #24951 ) ;
#35464=VECTOR ( 'NONE', #39781, 1000.000000000000000 ) ;
#35466=AXIS2_PLACEMENT_3D ( 'NONE', #23517, #4139, #35334 ) ;
#35477=DIRECTION ( 'NONE',  ( 0.7071067811865475727, 0.7071067811865475727, 0.000000000000000000 ) ) ;
#35488=AXIS2_PLACEMENT_3D ( 'NONE', #392, #47842, #16376 ) ;
#35492=EDGE_CURVE ( 'NONE', #51786, #37751, #7307, .T. ) ;
#35508=CARTESIAN_POINT ( 'NONE',  ( 16.13393739769639623, 7.383811055320659733, 4.943674098299959851 ) ) ;
#35514=ORIENTED_EDGE ( 'NONE', *, *, #22468, .T. ) ;
#35515=CARTESIAN_POINT ( 'NONE',  ( 33.13393739769620083, 7.383811055320659733, -59.64999999999999147 ) ) ;
#35521=LINE ( 'NONE', #51513, #40603 ) ;
#35528=AXIS2_PLACEMENT_3D ( 'NONE', #41333, #20623, #8856 ) ;
#35531=CARTESIAN_POINT ( 'NONE',  ( 38.67452568954050207, 4.883811055320659733, -81.65000000000000568 ) ) ;
#35537=CARTESIAN_POINT ( 'NONE',  ( 43.73738396686909624, -39.93285218904156864, -67.93068977794935392 ) ) ;
#35543=DIRECTION ( 'NONE',  ( -0.9750030843198951302, 0.2182216943050036273, -0.04181241085306048461 ) ) ;
#35556=DIRECTION ( 'NONE',  ( -1.000000000000000000, 0.000000000000000000, 0.000000000000000000 ) ) ;
#35560=ORIENTED_EDGE ( 'NONE', *, *, #28773, .T. ) ;
#35561=CARTESIAN_POINT ( 'NONE',  ( 0.1094292354459709959, 19.93927366128230005, -35.12965084568739371 ) ) ;
#35593=CARTESIAN_POINT ( 'NONE',  ( 46.92619617342869986, -39.55025295385299700, -54.22374093852179300 ) ) ;
#35594=VERTEX_POINT ( 'NONE', #41192 ) ;
#35607=CARTESIAN_POINT ( 'NONE',  ( 46.89115067490939737, -38.09589644477580350, -55.84613562826960020 ) ) ;
#35608=DIRECTION ( 'NONE',  ( -1.000000000000000000, 0.000000000000000000, 0.000000000000000000 ) ) ;
#35611=EDGE_LOOP ( 'NONE', ( #44961, #34176, #48084, #9539, #5804, #6151, #22667, #18470 ) ) ;
#35615=CARTESIAN_POINT ( 'NONE',  ( 47.55417156253681554, 6.784838323329733356, -52.48116776818960716 ) ) ;
#35618=CARTESIAN_POINT ( 'NONE',  ( 46.99244837402765995, -39.23262767327315714, -34.80140398659612089 ) ) ;
#35632=DIRECTION ( 'NONE',  ( -0.9223605572461988089, 0.3863301728269249447, 0.000000000000000000 ) ) ;
#35648=CARTESIAN_POINT ( 'NONE',  ( 0.1457841021255935343, -8.319710351909083812, -34.68167779225149161 ) ) ;
#35652=CARTESIAN_POINT ( 'NONE',  ( 11.96660005458890019, -42.11618894467939356, -34.64999999999999858 ) ) ;
#35659=CARTESIAN_POINT ( 'NONE',  ( 16.13393739769620083, -15.61618894467929941, -35.02873218748179340 ) ) ;
#35665=CARTESIAN_POINT ( 'NONE',  ( 10.04852440033089600, 22.72579217771966142, -34.76477869314942382 ) ) ;
#35670=AXIS2_PLACEMENT_3D ( 'NONE', #28137, #31807, #4823 ) ;
#35676=CARTESIAN_POINT ( 'NONE',  ( 44.13393739769620083, -33.11618894467940066, -54.35294145922159714 ) ) ;
#35681=CARTESIAN_POINT ( 'NONE',  ( 4.133937397696209715, -22.54439217495480108, -35.14999999999999858 ) ) ;
#35693=CARTESIAN_POINT ( 'NONE',  ( 10.47081843707173299, 11.49830782136799634, -84.65000000000000568 ) ) ;
#35696=CARTESIAN_POINT ( 'NONE',  ( -8.191285341990415247, -39.36383343069419993, -41.88932412146674267 ) ) ;
#35703=DIRECTION ( 'NONE',  ( 0.000000000000000000, -1.000000000000000000, 0.000000000000000000 ) ) ;
#35708=ORIENTED_EDGE ( 'NONE', *, *, #15093, .F. ) ;
#35710=CARTESIAN_POINT ( 'NONE',  ( 44.06836400025156308, 6.694124833047266243, -69.97780465984523346 ) ) ;
#35727=ADVANCED_FACE ( 'NONE', ( #51128 ), #43939, .F. ) ;
#35754=CARTESIAN_POINT ( 'NONE',  ( 16.13393739769620083, -15.61618894467929941, -35.14999999999999858 ) ) ;
#35767=B_SPLINE_CURVE_WITH_KNOTS ( 'NONE', 3,
 ( #23915, #12162, #31533, #31788, #47551, #20254, #11647, #43618, #48315, #8740, #12411, #19996 ),
 .UNSPECIFIED., .F., .F.,
 ( 4, 2, 2, 2, 1, 1, 4 ),
 ( 0.000000000000000000, 0.5000000000000769385, 0.5625000000000804912, 0.5937500000000822675, 0.6250000000000840439, 0.7500000000000469624, 1.000000000000000000 ),
 .UNSPECIFIED. ) ;
#35776=CARTESIAN_POINT ( 'NONE',  ( 44.73223296007571292, 1.943966071894212222, -43.46537174154696004 ) ) ;
#35779=AXIS2_PLACEMENT_3D ( 'NONE', #10692, #3089, #23481 ) ;
#35783=FACE_OUTER_BOUND ( 'NONE', #22858, .T. ) ;
#35784=LINE ( 'NONE', #26614, #8860 ) ;
#35787=ORIENTED_EDGE ( 'NONE', *, *, #36862, .F. ) ;
#35791=PRODUCT_DEFINITION_CONTEXT ( 'detailed design', #4024, 'design' ) ;
#35793=CARTESIAN_POINT ( 'NONE',  ( 43.64323166376460961, -39.92453440565081024, -68.38731717000798938 ) ) ;
#35794=CARTESIAN_POINT ( 'NONE',  ( 14.63393739769630031, 1.354373803797940035, -35.14999999999999858 ) ) ;
#35802=ORIENTED_EDGE ( 'NONE', *, *, #40971, .T. ) ;
#35805=ORIENTED_EDGE ( 'NONE', *, *, #35399, .T. ) ;
#35811=CARTESIAN_POINT ( 'NONE',  ( 41.11789956691032444, 8.431943849971739624, -80.58643109008846750 ) ) ;
#35813=ORIENTED_EDGE ( 'NONE', *, *, #22969, .F. ) ;
#35814=CARTESIAN_POINT ( 'NONE',  ( 44.07452568954059302, 1.883811055320659955, -54.64999999999999858 ) ) ;
#35816=CIRCLE ( 'NONE', #30753, 33.00000000000000000 ) ;
#35821=ORIENTED_EDGE ( 'NONE', *, *, #16851, .T. ) ;
#35822=EDGE_CURVE ( 'NONE', #14168, #5719, #18883, .T. ) ;
#35824=CARTESIAN_POINT ( 'NONE',  ( -0.1397480543147154586, 14.29295295954979927, -34.88775788892196061 ) ) ;
#35825=CARTESIAN_POINT ( 'NONE',  ( 16.13393739769620083, -15.61618894467929941, -35.02873218748179340 ) ) ;
#35828=CARTESIAN_POINT ( 'NONE',  ( 10.06369629474122185, 22.76024865223496363, -34.79644414665609986 ) ) ;
#35833=CARTESIAN_POINT ( 'NONE',  ( 8.643872352929088620, -48.75656286698969666, -35.12503119152809461 ) ) ;
#35838=CARTESIAN_POINT ( 'NONE',  ( 17.98749078828947745, -41.76263555408611694, -34.79644660940672907 ) ) ;
#35845=CARTESIAN_POINT ( 'NONE',  ( 46.56799392459599574, -40.00405894838129939, -54.63041858883969581 ) ) ;
#35851=CARTESIAN_POINT ( 'NONE',  ( 0.3198708682049009600, 19.48717932910869877, -34.64999999999999858 ) ) ;
#35864=EDGE_LOOP ( 'NONE', ( #38665, #7363, #35813, #24177, #14693, #35805, #17799 ) ) ;
#35865=CARTESIAN_POINT ( 'NONE',  ( 46.43281365467359478, 6.703450485939987047, -58.09721321091641499 ) ) ;
#35875=ORIENTED_EDGE ( 'NONE', *, *, #27849, .T. ) ;
#35883=AXIS2_PLACEMENT_3D ( 'NONE', #16486, #32970, #20662 ) ;
#35892=FACE_OUTER_BOUND ( 'NONE', #30321, .T. ) ;
#35894=CARTESIAN_POINT ( 'NONE',  ( 16.13393739769620083, -15.61618894467929941, -35.14999999999999858 ) ) ;
#35895=ORIENTED_EDGE ( 'NONE', *, *, #14353, .F. ) ;
#35899=CARTESIAN_POINT ( 'NONE',  ( 2.422700639432790126, -25.82238555492689969, -35.02127583263639821 ) ) ;
#35902=CARTESIAN_POINT ( 'NONE',  ( 46.00717017453583679, -38.15421180662563216, -60.28378775688172198 ) ) ;
#35905=DIRECTION ( 'NONE',  ( 0.5835456732599438867, -0.8120803206700667465, 0.000000000000000000 ) ) ;
#35911=PLANE ( 'NONE',  #13863 ) ;
#35921=DIRECTION ( 'NONE',  ( -1.451273000000000212E-17, 7.532081000000000189E-18, -1.000000000000000000 ) ) ;
#35930=CARTESIAN_POINT ( 'NONE',  ( 0.2609591194317602558, -4.650627301100893618, -34.64999999999999858 ) ) ;
#35935=CARTESIAN_POINT ( 'NONE',  ( 38.67452568954060155, -33.99486860111965569, -83.77132034355965118 ) ) ;
#35943=ORIENTED_EDGE ( 'NONE', *, *, #765, .T. ) ;
#35956=CARTESIAN_POINT ( 'NONE',  ( 17.68664282411139865, 0.9736865341432859866, -34.65032322548090349 ) ) ;
#35984=DIRECTION ( 'NONE',  ( 1.000000000000000000, 0.000000000000000000, 0.000000000000000000 ) ) ;
#36000=CARTESIAN_POINT ( 'NONE',  ( 16.13393739769620083, -15.61618894467929941, -34.64999999999999858 ) ) ;
#36002=ORIENTED_EDGE ( 'NONE', *, *, #26884, .F. ) ;
#36005=EDGE_LOOP ( 'NONE', ( #15529, #51564, #18644, #5768 ) ) ;
#36007=VERTEX_POINT ( 'NONE', #31945 ) ;
#36020=ORIENTED_EDGE ( 'NONE', *, *, #46627, .T. ) ;
#36021=ORIENTED_EDGE ( 'NONE', *, *, #29680, .F. ) ;
#36026=ADVANCED_FACE ( 'NONE', ( #24076 ), #15481, .T. ) ;
#36029=EDGE_CURVE ( 'NONE', #23707, #45957, #43091, .T. ) ;
#36040=CARTESIAN_POINT ( 'NONE',  ( 42.72381319638073194, -39.83914644532161731, -72.83559664042903137 ) ) ;
#36048=CARTESIAN_POINT ( 'NONE',  ( 14.32489919860644179, -32.43785826095948721, -34.75586992539663811 ) ) ;
#36055=EDGE_LOOP ( 'NONE', ( #50236, #9304, #34502, #47449 ) ) ;
#36061=CARTESIAN_POINT ( 'NONE',  ( 41.39457728824679350, 8.464282045044221547, -79.25350500381260588 ) ) ;
#36063=CARTESIAN_POINT ( 'NONE',  ( 30.43389199679464241, 4.399289011473882738, -84.61061572685468946 ) ) ;
#36069=VERTEX_POINT ( 'NONE', #13113 ) ;
#36075=ORIENTED_EDGE ( 'NONE', *, *, #39016, .T. ) ;
#36079=CARTESIAN_POINT ( 'NONE',  ( -20.88509709344132759, -3.337410866617939842, -53.17709637982930104 ) ) ;
#36102=ORIENTED_EDGE ( 'NONE', *, *, #21391, .T. ) ;
#36105=CARTESIAN_POINT ( 'NONE',  ( 16.13393739769620083, -15.61618894467929941, -44.64999999999999858 ) ) ;
#36111=CYLINDRICAL_SURFACE ( 'NONE', #40936, 0.4999999999999982236 ) ;
#36112=EDGE_CURVE ( 'NONE', #46925, #23386, #14027, .T. ) ;
#36113=DIRECTION ( 'NONE',  ( -1.000000000000000000, 0.000000000000000000, 0.000000000000000000 ) ) ;
#36115=DIRECTION ( 'NONE',  ( 1.000000000000000000, 0.000000000000000000, 0.000000000000000000 ) ) ;
#36120=CARTESIAN_POINT ( 'NONE',  ( 44.44997065502152367, 7.812898992897342687, -68.49922028869087853 ) ) ;
#36130=ORIENTED_EDGE ( 'NONE', *, *, #40036, .T. ) ;
#36134=EDGE_CURVE ( 'NONE', #32056, #6345, #12982, .T. ) ;
#36140=VERTEX_POINT ( 'NONE', #17223 ) ;
#36145=ORIENTED_EDGE ( 'NONE', *, *, #21916, .T. ) ;
#36151=CARTESIAN_POINT ( 'NONE',  ( 18.11714455905750043, -32.59356659976219817, -35.02127583263639821 ) ) ;
#36165=DIRECTION ( 'NONE',  ( 0.000000000000000000, 0.000000000000000000, 1.000000000000000000 ) ) ;
#36170=CARTESIAN_POINT ( 'NONE',  ( 41.25851182071981071, -39.72332991368651278, -79.73195694794895871 ) ) ;
#36174=CARTESIAN_POINT ( 'NONE',  ( 16.13393739769620083, -15.61618894467929941, -35.12503119152809461 ) ) ;
#36175=EDGE_CURVE ( 'NONE', #2647, #23957, #21386, .T. ) ;
#36176=VERTEX_POINT ( 'NONE', #5687 ) ;
#36190=CARTESIAN_POINT ( 'NONE',  ( 10.13393739769589885, 22.91950879131600161, -54.64999999999999858 ) ) ;
#36204=DIRECTION ( 'NONE',  ( 0.000000000000000000, 0.000000000000000000, 1.000000000000000000 ) ) ;
#36207=AXIS2_PLACEMENT_3D ( 'NONE', #31366, #51568, #19593 ) ;
#36209=CARTESIAN_POINT ( 'NONE',  ( 17.83125332364319959, 1.104866772713940071, -34.68801049095939959 ) ) ;
#36213=CARTESIAN_POINT ( 'NONE',  ( 42.94456142498044926, -37.76943540611747352, -75.59687433678018920 ) ) ;
#36227=EDGE_CURVE ( 'NONE', #11818, #25290, #27243, .T. ) ;
#36233=ORIENTED_EDGE ( 'NONE', *, *, #41068, .T. ) ;
#36247=CARTESIAN_POINT ( 'NONE',  ( 44.12711257345860361, -33.11618894467940066, -54.38706558040979644 ) ) ;
#36256=ORIENTED_EDGE ( 'NONE', *, *, #16484, .T. ) ;
#36260=ORIENTED_EDGE ( 'NONE', *, *, #6403, .T. ) ;
#36269=ORIENTED_EDGE ( 'NONE', *, *, #2977, .F. ) ;
#36286=AXIS2_PLACEMENT_3D ( 'NONE', #35894, #19651, #28271 ) ;
#36288=CARTESIAN_POINT ( 'NONE',  ( 23.34813653593170102, -49.28809633162250492, -34.65024031912469837 ) ) ;
#36291=CARTESIAN_POINT ( 'NONE',  ( 42.94172388228522408, -39.86051557588725558, -71.78134772292702337 ) ) ;
#36292=CARTESIAN_POINT ( 'NONE',  ( 11.63393739769600010, 10.38381105532060111, -34.64999999999999858 ) ) ;
#36298=LINE ( 'NONE', #4863, #34783 ) ;
#36308=CARTESIAN_POINT ( 'NONE',  ( 41.00753304566280377, 8.418767411291142366, -81.11804229810685740 ) ) ;
#36309=CARTESIAN_POINT ( 'NONE',  ( -0.01592648613901413018, -8.413074003574475768, -34.78031642072628671 ) ) ;
#36311=FACE_OUTER_BOUND ( 'NONE', #18781, .T. ) ;
#36326=LINE ( 'NONE', #11481, #13628 ) ;
#36334=LINE ( 'NONE', #27955, #32821 ) ;
#36337=LINE ( 'NONE', #48946, #46426 ) ;
#36344=DIRECTION ( 'NONE',  ( 0.7071067811865457964, -0.7071067811865492381, 0.000000000000000000 ) ) ;
#36354=EDGE_CURVE ( 'NONE', #20085, #47128, #19382, .T. ) ;
#36393=VERTEX_POINT ( 'NONE', #8840 ) ;
#36396=CARTESIAN_POINT ( 'NONE',  ( 10.11211546542380013, 22.87009133999800170, -34.93361312117499295 ) ) ;
#36398=CARTESIAN_POINT ( 'NONE',  ( 2.446837772604945727, -25.70616092178045875, -34.84133294386909085 ) ) ;
#36406=ORIENTED_EDGE ( 'NONE', *, *, #29611, .T. ) ;
#36421=CARTESIAN_POINT ( 'NONE',  ( 41.01311687426999697, -39.69858908207098125, -80.89458633909558216 ) ) ;
#36428=AXIS2_PLACEMENT_3D ( 'NONE', #15751, #19925, #43791 ) ;
#36437=AXIS2_PLACEMENT_3D ( 'NONE', #51215, #3518, #11385 ) ;
#36439=CARTESIAN_POINT ( 'NONE',  ( -11.59939519444589529, 2.705059169678001307, -49.87766025524430091 ) ) ;
#36458=ORIENTED_EDGE ( 'NONE', *, *, #38935, .F. ) ;
#36460=CARTESIAN_POINT ( 'NONE',  ( 42.13803780587668513, 6.413235773433889619, -79.62945665582455490 ) ) ;
#36464=CIRCLE ( 'NONE', #23914, 3.000000000000001776 ) ;
#36466=CARTESIAN_POINT ( 'NONE',  ( 45.22285809734859896, 2.278851623075559996, -34.76403944585129580 ) ) ;
#36467=CARTESIAN_POINT ( 'NONE',  ( 41.87134808728646362, -37.60294274168957429, -80.96289175035070684 ) ) ;
#36481=ORIENTED_EDGE ( 'NONE', *, *, #9876, .F. ) ;
#36491=VECTOR ( 'NONE', #18538, 1000.000000000000000 ) ;
#36506=( BOUNDED_CURVE ( )  B_SPLINE_CURVE ( 3, ( #18395, #30703, #6613, #34373 ),
 .UNSPECIFIED., .F., .T. ) 
 B_SPLINE_CURVE_WITH_KNOTS ( ( 4, 4 ),
 ( 2.356194490192396351, 3.141592653589795781 ),
 .UNSPECIFIED. ) 
 CURVE ( )  GEOMETRIC_REPRESENTATION_ITEM ( )  RATIONAL_B_SPLINE_CURVE ( ( 1.000000000000000000, 0.9492530216741973392, 0.9492530216741973392, 1.000000000000000000 ) ) 
 REPRESENTATION_ITEM ( '' )  );
#36512=DIRECTION ( 'NONE',  ( 1.000000000000000000, 0.000000000000000000, 0.000000000000000000 ) ) ;
#36518=ORIENTED_EDGE ( 'NONE', *, *, #40283, .F. ) ;
#36523=CARTESIAN_POINT ( 'NONE',  ( -11.80944000494499768, -34.05870648691990255, -45.03554556751409166 ) ) ;
#36540=CARTESIAN_POINT ( 'NONE',  ( 38.67452568954060155, 4.883811055320659733, -81.65000000000000568 ) ) ;
#36543=AXIS2_PLACEMENT_3D ( 'NONE', #33023, #43629, #31799 ) ;
#36546=EDGE_CURVE ( 'NONE', #7583, #40660, #46022, .T. ) ;
#36553=CARTESIAN_POINT ( 'NONE',  ( 42.93292300981802612, -39.85965248063442345, -71.82398325773546333 ) ) ;
#36561=CARTESIAN_POINT ( 'NONE',  ( -0.4123484725610440105, 14.05881538531380137, -35.12503119152799513 ) ) ;
#36565=EDGE_LOOP ( 'NONE', ( #30662, #34093, #1715, #28401, #17297, #4695 ) ) ;
#36570=CARTESIAN_POINT ( 'NONE',  ( 42.91356006583662008, 8.625454777037399268, -71.91745137691370360 ) ) ;
#36574=VERTEX_POINT ( 'NONE', #10912 ) ;
#36586=ORIENTED_EDGE ( 'NONE', *, *, #4960, .T. ) ;
#36610=EDGE_CURVE ( 'NONE', #42739, #29610, #13802, .T. ) ;
#36612=CARTESIAN_POINT ( 'NONE',  ( 19.13393739769620083, -49.61618894467939356, -35.14999999999999858 ) ) ;
#36619=AXIS2_PLACEMENT_3D ( 'NONE', #18146, #41475, #33857 ) ;
#36627=CARTESIAN_POINT ( 'NONE',  ( 33.38393739769599478, 10.88381105532080007, -35.14999999999999858 ) ) ;
#36632=DIRECTION ( 'NONE',  ( 0.1564344650402237358, -0.9876883405951387696, 0.000000000000000000 ) ) ;
#36635=ORIENTED_EDGE ( 'NONE', *, *, #10432, .F. ) ;
#36636=ORIENTED_EDGE ( 'NONE', *, *, #47061, .T. ) ;
#36643=CARTESIAN_POINT ( 'NONE',  ( 0.7740850027469919903, -51.13355895648079752, -34.09234346398749693 ) ) ;
#36662=PRODUCT_CONTEXT ( 'NONE', #38860, 'mechanical' ) ;
#36675=B_SPLINE_CURVE_WITH_KNOTS ( 'NONE', 3,
 ( #7529, #11722, #47119, #27686, #19828, #39752, #23736, #15647, #19052, #35561, #43686, #7786 ),
 .UNSPECIFIED., .F., .F.,
 ( 4, 2, 2, 2, 2, 4 ),
 ( 5.801249110064609653E-07, 0.01391382196184159925, 0.02795653394361129543, 0.04029818000215710377, 0.05270323408096880269, 0.05591482578471518999 ),
 .UNSPECIFIED. ) ;
#36677=CARTESIAN_POINT ( 'NONE',  ( 0.4047412638266219553, -8.844334399411719616, -35.14999999999999858 ) ) ;
#36679=CARTESIAN_POINT ( 'NONE',  ( 30.03924614610626520, -35.61560227024466485, -84.60794077557196147 ) ) ;
#36698=ORIENTED_EDGE ( 'NONE', *, *, #20278, .F. ) ;
#36715=B_SPLINE_CURVE_WITH_KNOTS ( 'NONE', 3,
 ( #2789, #3046, #19018, #34994, #8000, #43907, #11434, #27140, #48096, #39976 ),
 .UNSPECIFIED., .F., .F.,
 ( 4, 2, 2, 2, 4 ),
 ( -0.0004281134593881059914, 0.000000000000000000, 0.02012916873249290597, 0.03942875605179270437, 0.05028014561811239291 ),
 .UNSPECIFIED. ) ;
#36723=CARTESIAN_POINT ( 'NONE',  ( 42.40479495363826601, 6.455874691308983948, -78.29570199813332465 ) ) ;
#36728=CARTESIAN_POINT ( 'NONE',  ( 43.30851615596512971, -37.82231177387381393, -73.77704280282122795 ) ) ;
#36729=VERTEX_POINT ( 'NONE', #16112 ) ;
#36732=CIRCLE ( 'NONE', #42626, 3.000000000000005773 ) ;
#36735=EDGE_CURVE ( 'NONE', #25918, #47312, #14686, .T. ) ;
#36740=ORIENTED_EDGE ( 'NONE', *, *, #37815, .T. ) ;
#36755=DIRECTION ( 'NONE',  ( 1.000000000000000000, 0.000000000000000000, 0.000000000000000000 ) ) ;
#36760=ADVANCED_FACE ( 'NONE', ( #19533 ), #51764, .T. ) ;
#36766=ORIENTED_EDGE ( 'NONE', *, *, #35057, .F. ) ;
#36767=CARTESIAN_POINT ( 'NONE',  ( -0.2149313111747337413, -10.70936568845926828, -34.95336413010216603 ) ) ;
#36777=ORIENTED_EDGE ( 'NONE', *, *, #24738, .T. ) ;
#36784=EDGE_CURVE ( 'NONE', #22924, #27937, #35521, .T. ) ;
#36786=ORIENTED_EDGE ( 'NONE', *, *, #47664, .F. ) ;
#36792=FACE_OUTER_BOUND ( 'NONE', #33664, .T. ) ;
#36794=ORIENTED_EDGE ( 'NONE', *, *, #29640, .T. ) ;
#36795=ORIENTED_EDGE ( 'NONE', *, *, #13127, .F. ) ;
#36805=FACE_OUTER_BOUND ( 'NONE', #21602, .T. ) ;
#36809=ORIENTED_EDGE ( 'NONE', *, *, #45668, .T. ) ;
#36817=CARTESIAN_POINT ( 'NONE',  ( 42.22674147479784068, -39.78872467147441938, -75.23666230762985663 ) ) ;
#36824=EDGE_CURVE ( 'NONE', #425, #15778, #11942, .T. ) ;
#36832=ORIENTED_EDGE ( 'NONE', *, *, #44437, .T. ) ;
#36836=CARTESIAN_POINT ( 'NONE',  ( 40.88902997202897183, 8.404135775541593745, -81.68995767638860173 ) ) ;
#36850=DIRECTION ( 'NONE',  ( -0.8660254037844380415, 0.5000000000000012212, -1.387778780781449373E-16 ) ) ;
#36859=CARTESIAN_POINT ( 'NONE',  ( -15.44067079850665181, 7.275931003700006450, -48.50294866079644862 ) ) ;
#36862=EDGE_CURVE ( 'NONE', #34982, #41459, #44793, .T. ) ;
#36865=ORIENTED_EDGE ( 'NONE', *, *, #6384, .T. ) ;
#36866=FACE_OUTER_BOUND ( 'NONE', #19979, .T. ) ;
#36867=CARTESIAN_POINT ( 'NONE',  ( 8.773163715961540987, -48.44626589138000128, -41.74835364836469864 ) ) ;
#36878=DIRECTION ( 'NONE',  ( -1.000000000000000000, 0.000000000000000000, 0.000000000000000000 ) ) ;
#36894=CARTESIAN_POINT ( 'NONE',  ( 23.36719009658099822, -48.14181044607700244, -48.24693240285689910 ) ) ;
#36896=ORIENTED_EDGE ( 'NONE', *, *, #14510, .F. ) ;
#36921=FACE_OUTER_BOUND ( 'NONE', #37893, .T. ) ;
#36923=DIRECTION ( 'NONE',  ( 0.000000000000000000, 0.000000000000000000, -1.000000000000000000 ) ) ;
#36932=VECTOR ( 'NONE', #561, 1000.000000000000114 ) ;
#36939=CARTESIAN_POINT ( 'NONE',  ( -0.8602693046289541234, -18.80587780509931051, -35.51452756723926996 ) ) ;
#36942=CARTESIAN_POINT ( 'NONE',  ( 0.1457841021255935343, -22.91266753744946527, -34.68167779225149161 ) ) ;
#36948=CARTESIAN_POINT ( 'NONE',  ( 14.68576648362313541, -49.61617023087686817, -83.19397497661746854 ) ) ;
#36951=EDGE_CURVE ( 'NONE', #611, #39828, #30389, .T. ) ;
#36959=EDGE_CURVE ( 'NONE', #14025, #39703, #27202, .T. ) ;
#36978=DIRECTION ( 'NONE',  ( 0.02902962677397545252, 0.04063306972650054805, 0.9987523388778446476 ) ) ;
#36989=EDGE_CURVE ( 'NONE', #6854, #51808, #30076, .T. ) ;
#36996=CARTESIAN_POINT ( 'NONE',  ( 42.05506414891981848, 6.400113107552978242, -80.04430332523035929 ) ) ;
#37000=CARTESIAN_POINT ( 'NONE',  ( 42.64819641985740617, -37.72516299508219362, -77.07863785855882099 ) ) ;
#37005=AXIS2_PLACEMENT_3D ( 'NONE', #32484, #12102, #12350 ) ;
#37018=EDGE_CURVE ( 'NONE', #37975, #50570, #18003, .T. ) ;
#37038=VERTEX_POINT ( 'NONE', #40356 ) ;
#37042=DIRECTION ( 'NONE',  ( 0.000000000000000000, -0.7071067811865475727, 0.7071067811865475727 ) ) ;
#37047=ORIENTED_EDGE ( 'NONE', *, *, #4336, .T. ) ;
#37049=EDGE_LOOP ( 'NONE', ( #2830, #8133, #43437, #29246, #13662, #11408, #41611 ) ) ;
#37056=VERTEX_POINT ( 'NONE', #20679 ) ;
#37061=CARTESIAN_POINT ( 'NONE',  ( -0.007164426707907000161, -50.71887597443840434, -34.77269723932290191 ) ) ;
#37084=EDGE_CURVE ( 'NONE', #26020, #21076, #51527, .T. ) ;
#37085=CARTESIAN_POINT ( 'NONE',  ( 14.37540540599763794, 10.62527906362193519, -34.70142521051219120 ) ) ;
#37092=AXIS2_PLACEMENT_3D ( 'NONE', #11857, #12104, #27812 ) ;
#37104=CARTESIAN_POINT ( 'NONE',  ( 45.05697163777319503, 8.802134928348412046, -61.53621250105515372 ) ) ;
#37113=VERTEX_POINT ( 'NONE', #31951 ) ;
#37114=PLANE ( 'NONE',  #11915 ) ;
#37118=AXIS2_PLACEMENT_3D ( 'NONE', #51307, #39762, #4110 ) ;
#37122=EDGE_LOOP ( 'NONE', ( #5554, #1466, #14009, #20261, #33933, #41798, #44396, #34334 ) ) ;
#37124=CARTESIAN_POINT ( 'NONE',  ( -8.713277369480067591, 14.44436079558252928, -42.72765124578886287 ) ) ;
#37125=FACE_OUTER_BOUND ( 'NONE', #5235, .T. ) ;
#37134=EDGE_CURVE ( 'NONE', #26529, #45038, #44033, .T. ) ;
#37135=CARTESIAN_POINT ( 'NONE',  ( 8.643872352928719138, 17.52418497763089889, -35.12503119152809461 ) ) ;
#37136=AXIS2_PLACEMENT_3D ( 'NONE', #12812, #44768, #4932 ) ;
#37149=LINE ( 'NONE', #37657, #24714 ) ;
#37165=CARTESIAN_POINT ( 'NONE',  ( 11.63393739769600010, 10.38381105532060111, -35.14999999999999858 ) ) ;
#37181=ORIENTED_EDGE ( 'NONE', *, *, #51047, .F. ) ;
#37182=CARTESIAN_POINT ( 'NONE',  ( -22.53234341801570295, -21.49586800030930078, -54.54381104595779561 ) ) ;
#37184=CARTESIAN_POINT ( 'NONE',  ( 18.13393739769630031, 1.391621760993470014, -35.14999999999999858 ) ) ;
#37185=VECTOR ( 'NONE', #26562, 1000.000000000000114 ) ;
#37187=FACE_OUTER_BOUND ( 'NONE', #34649, .T. ) ;
#37207=AXIS2_PLACEMENT_3D ( 'NONE', #34406, #7423, #11105 ) ;
#37214=EDGE_CURVE ( 'NONE', #13573, #46163, #6316, .T. ) ;
#37218=CARTESIAN_POINT ( 'NONE',  ( 44.27243015989088804, -40.08314457256550867, -64.90451195649632155 ) ) ;
#37253=DIRECTION ( 'NONE',  ( 0.000000000000000000, -1.000000000000000000, 0.000000000000000000 ) ) ;
#37260=CARTESIAN_POINT ( 'NONE',  ( 11.73137203405252826, -41.76263555408610273, -34.79644660940672196 ) ) ;
#37263=EDGE_CURVE ( 'NONE', #16348, #6096, #18979, .T. ) ;
#37265=CARTESIAN_POINT ( 'NONE',  ( 42.25617998614456639, -37.66442862941680403, -79.03878004411602376 ) ) ;
#37266=VERTEX_POINT ( 'NONE', #24608 ) ;
#37272=LINE ( 'NONE', #8460, #22285 ) ;
#37286=CARTESIAN_POINT ( 'NONE',  ( 22.16915665782660128, 22.83973475445539947, -34.88336916441289759 ) ) ;
#37290=DIRECTION ( 'NONE',  ( 1.000000000000000000, 0.000000000000000000, 0.000000000000000000 ) ) ;
#37291=CARTESIAN_POINT ( 'NONE',  ( 46.63393739769619373, -36.11618894467930119, -34.64999999999999858 ) ) ;
#37300=CARTESIAN_POINT ( 'NONE',  ( 34.00893739769620083, -11.50256827670329862, -35.14999999999999858 ) ) ;
#37302=CARTESIAN_POINT ( 'NONE',  ( 16.13393739769620083, -1.759782484128330049, -47.64999999999999858 ) ) ;
#37322=CARTESIAN_POINT ( 'NONE',  ( 20.63393739769599833, 10.38381105532070059, -35.14999999999999858 ) ) ;
#37325=ADVANCED_FACE ( 'NONE', ( #49280 ), #39785, .F. ) ;
#37329=EDGE_CURVE ( 'NONE', #16369, #40975, #10508, .T. ) ;
#37331=CARTESIAN_POINT ( 'NONE',  ( 16.13393739769599833, 14.38381105532070059, -35.14999999999999858 ) ) ;
#37333=DIRECTION ( 'NONE',  ( 0.000000000000000000, 0.000000000000000000, -1.000000000000000000 ) ) ;
#37355=ORIENTED_EDGE ( 'NONE', *, *, #408, .F. ) ;
#37360=CARTESIAN_POINT ( 'NONE',  ( 44.34565080150579064, 8.750017722592588143, -64.98493568350201599 ) ) ;
#37365=VECTOR ( 'NONE', #42832, 1000.000000000000000 ) ;
#37366=VERTEX_POINT ( 'NONE', #22754 ) ;
#37368=AXIS2_PLACEMENT_3D ( 'NONE', #36292, #12730, #13512 ) ;
#37372=DIRECTION ( 'NONE',  ( 0.7071067811865510144, 0.000000000000000000, 0.7071067811865441310 ) ) ;
#37376=ORIENTED_EDGE ( 'NONE', *, *, #34757, .F. ) ;
#37383=DIRECTION ( 'NONE',  ( -0.5516667872527503125, 0.8340645993220362486, -1.942890293094025918E-16 ) ) ;
#37385=CARTESIAN_POINT ( 'NONE',  ( 38.67452568954060155, -15.61618894467929941, -81.65000000000000568 ) ) ;
#37388=EDGE_CURVE ( 'NONE', #51495, #40473, #9945, .T. ) ;
#37390=VECTOR ( 'NONE', #47874, 1000.000000000000000 ) ;
#37391=CARTESIAN_POINT ( 'NONE',  ( 8.645706001916069638, 17.52774233096719669, -35.08633291502819418 ) ) ;
#37397=CARTESIAN_POINT ( 'NONE',  ( 46.85203200633210230, 8.412936757578801661, -54.34706384622469244 ) ) ;
#37403=CARTESIAN_POINT ( 'NONE',  ( 46.30117189897522678, -40.10998932786493043, -55.49701588496500904 ) ) ;
#37404=CARTESIAN_POINT ( 'NONE',  ( 30.13393739769619728, 7.383811055320659733, -72.14999999999999147 ) ) ;
#37421=ADVANCED_FACE ( 'NONE', ( #6534 ), #29840, .T. ) ;
#37432=DIRECTION ( 'NONE',  ( 0.000000000000000000, 0.000000000000000000, 1.000000000000000000 ) ) ;
#37433=CARTESIAN_POINT ( 'NONE',  ( 16.13393739769620083, -45.61618894467940066, -35.14999999999999858 ) ) ;
#37434=DIRECTION ( 'NONE',  ( 0.06538141124691357331, -0.04750237581189067221, -0.9967290481146758863 ) ) ;
#37436=CARTESIAN_POINT ( 'NONE',  ( -20.70080641011480083, -28.63484290321709835, -52.76718538126279867 ) ) ;
#37437=DIRECTION ( 'NONE',  ( 1.000000000000000000, 0.000000000000000000, 0.000000000000000000 ) ) ;
#37442=( BOUNDED_CURVE ( )  B_SPLINE_CURVE ( 3, ( #37260, #9493, #29635, #33824 ),
 .UNSPECIFIED., .F., .T. ) 
 B_SPLINE_CURVE_WITH_KNOTS ( ( 4, 4 ),
 ( 2.356194490192361712, 3.141592653589784234 ),
 .UNSPECIFIED. ) 
 CURVE ( )  GEOMETRIC_REPRESENTATION_ITEM ( )  RATIONAL_B_SPLINE_CURVE ( ( 1.000000000000000000, 0.9492530216741945637, 0.9492530216741945637, 1.000000000000000000 ) ) 
 REPRESENTATION_ITEM ( '' )  );
#37445=CARTESIAN_POINT ( 'NONE',  ( 20.63393739769599833, 10.38381105532070059, -35.14999999999999858 ) ) ;
#37447=CARTESIAN_POINT ( 'NONE',  ( 9.661801442696654973, -10.91390692633954451, -47.64999999999999858 ) ) ;
#37448=CARTESIAN_POINT ( 'NONE',  ( 24.75751086271734280, -18.45471230805310370, -34.79644660940672907 ) ) ;
#37465=CARTESIAN_POINT ( 'NONE',  ( 37.13393739769620083, -49.46974233527257780, -34.79644660940672907 ) ) ;
#37468=B_SPLINE_CURVE_WITH_KNOTS ( 'NONE', 3,
 ( #4000, #12124, #19961, #35956, #32003, #36209, #48023, #28080, #44085, #1094 ),
 .UNSPECIFIED., .F., .F.,
 ( 4, 2, 2, 2, 4 ),
 ( -0.0004281134595752249749, 0.000000000000000000, 0.02012916873231600234, 0.03942875605144609968, 0.05028014561772611163 ),
 .UNSPECIFIED. ) ;
#37472=CARTESIAN_POINT ( 'NONE',  ( 47.18509805015050063, -39.34325223768411917, -54.67923127845079279 ) ) ;
#37504=CARTESIAN_POINT ( 'NONE',  ( 0.1457841021255935343, -50.71887597443840434, -34.68167779225149161 ) ) ;
#37506=CARTESIAN_POINT ( 'NONE',  ( 13.13393739769619906, -49.61618894467939356, -83.01107220193038927 ) ) ;
#37517=CARTESIAN_POINT ( 'NONE',  ( 44.41215812983547551, -37.97064865278709078, -68.25889606298196099 ) ) ;
#37519=ORIENTED_EDGE ( 'NONE', *, *, #11470, .F. ) ;
#37524=CARTESIAN_POINT ( 'NONE',  ( 38.67452568954060155, 6.328436186825659782, -81.65000000000000568 ) ) ;
#37544=CARTESIAN_POINT ( 'NONE',  ( 38.67452568954060155, -36.11618894467930119, -81.65000000000000568 ) ) ;
#37546=EDGE_CURVE ( 'NONE', #42649, #1811, #47353, .T. ) ;
#37553=DIRECTION ( 'NONE',  ( -0.5000000000000003331, -0.8660254037844384856, 0.000000000000000000 ) ) ;
#37557=ORIENTED_EDGE ( 'NONE', *, *, #9758, .T. ) ;
#37559=CARTESIAN_POINT ( 'NONE',  ( 15.01109173769490113, 12.72875286183729848, -62.64999999999999858 ) ) ;
#37569=CARTESIAN_POINT ( 'NONE',  ( 46.95981438746490966, 7.013759907145603378, -55.52059116220966928 ) ) ;
#37570=ORIENTED_EDGE ( 'NONE', *, *, #5899, .T. ) ;
#37577=CYLINDRICAL_SURFACE ( 'NONE', #40079, 0.4999999999999985012 ) ;
#37582=DIRECTION ( 'NONE',  ( 8.462868000000000073E-18, -1.066343000000000058E-17, 1.000000000000000000 ) ) ;
#37592=CARTESIAN_POINT ( 'NONE',  ( 14.13393739769599833, 14.38381105532070059, -62.64999999999999858 ) ) ;
#37603=ORIENTED_EDGE ( 'NONE', *, *, #18469, .F. ) ;
#37614=CARTESIAN_POINT ( 'NONE',  ( 44.78558282010767044, 8.783042718080674049, -62.85233582178556588 ) ) ;
#37622=ORIENTED_EDGE ( 'NONE', *, *, #19032, .F. ) ;
#37626=FACE_OUTER_BOUND ( 'NONE', #38754, .T. ) ;
#37627=EDGE_CURVE ( 'NONE', #7528, #43147, #3629, .T. ) ;
#37628=ORIENTED_EDGE ( 'NONE', *, *, #36546, .F. ) ;
#37629=EDGE_LOOP ( 'NONE', ( #40828, #26932, #25353, #44281 ) ) ;
#37635=TOROIDAL_SURFACE ( 'NONE', #26742, 16.60961179679779676, 0.5000000000000000000 ) ;
#37638=CARTESIAN_POINT ( 'NONE',  ( 0.3198710486850210311, -46.24968915917909840, -34.64999999999999858 ) ) ;
#37641=CARTESIAN_POINT ( 'NONE',  ( 14.17038268164659875, -32.57607267493840197, -34.95504743437659556 ) ) ;
#37657=CARTESIAN_POINT ( 'NONE',  ( 4.133937397696209715, -8.687985714403829718, -47.64999999999999858 ) ) ;
#37666=AXIS2_PLACEMENT_3D ( 'NONE', #27053, #3479, #47759 ) ;
#37668=EDGE_CURVE ( 'NONE', #14308, #43415, #51589, .T. ) ;
#37669=EDGE_LOOP ( 'NONE', ( #27694, #50540, #23190, #4 ) ) ;
#37670=VECTOR ( 'NONE', #24958, 1000.000000000000000 ) ;
#37672=CARTESIAN_POINT ( 'NONE',  ( 19.13393739769620083, -49.61618894467939356, -35.14999999999999858 ) ) ;
#37676=AXIS2_PLACEMENT_3D ( 'NONE', #26063, #30257, #42334 ) ;
#37678=CIRCLE ( 'NONE', #49447, 6.999999999999999112 ) ;
#37682=FACE_OUTER_BOUND ( 'NONE', #14465, .T. ) ;
#37691=DIRECTION ( 'NONE',  ( 0.000000000000000000, 1.000000000000000000, 0.000000000000000000 ) ) ;
#37692=VERTEX_POINT ( 'NONE', #28755 ) ;
#37693=CARTESIAN_POINT ( 'NONE',  ( -10.12641005879179978, -44.73605830922169702, -43.60172970322699371 ) ) ;
#37698=ADVANCED_FACE ( 'NONE', ( #989 ), #40307, .T. ) ;
#37712=EDGE_LOOP ( 'NONE', ( #36518, #43496, #46599, #16289, #37355, #25490 ) ) ;
#37717=AXIS2_PLACEMENT_3D ( 'NONE', #32315, #39702, #48335 ) ;
#37721=CARTESIAN_POINT ( 'NONE',  ( 13.10629489870523479, -49.56476373416713699, -34.89146800830128825 ) ) ;
#37729=CARTESIAN_POINT ( 'NONE',  ( 16.63546379641747208, -49.61618961575661046, -83.24416995775972339 ) ) ;
#37733=CARTESIAN_POINT ( 'NONE',  ( 46.37986018651987052, -40.25936219620972167, -54.53427625130012757 ) ) ;
#37741=CARTESIAN_POINT ( 'NONE',  ( 42.18937197816117646, 8.603191575157895343, -75.20614456104748058 ) ) ;
#37742=LINE ( 'NONE', #13893, #45313 ) ;
#37745=CARTESIAN_POINT ( 'NONE',  ( 29.09106731080629871, -26.72413521581369977, -34.94555596725399482 ) ) ;
#37751=VERTEX_POINT ( 'NONE', #40561 ) ;
#37757=AXIS2_PLACEMENT_3D ( 'NONE', #36627, #729, #48707 ) ;
#37773=DIRECTION ( 'NONE',  ( 0.000000000000000000, 0.000000000000000000, -1.000000000000000000 ) ) ;
#37783=CARTESIAN_POINT ( 'NONE',  ( 43.72333004139270685, -37.88011359077987095, -71.70303684443479142 ) ) ;
#37813=DIRECTION ( 'NONE',  ( -1.000000000000000000, 0.000000000000000000, 0.000000000000000000 ) ) ;
#37815=EDGE_CURVE ( 'NONE', #16231, #49938, #25331, .T. ) ;
#37837=VECTOR ( 'NONE', #18786, 1000.000000000000000 ) ;
#37838=CARTESIAN_POINT ( 'NONE',  ( 27.13393739769620083, 7.383811055320659733, -84.65000000000000568 ) ) ;
#37841=CARTESIAN_POINT ( 'NONE',  ( 46.11861065021020067, 6.933294690613563738, -59.72657760612104028 ) ) ;
#37859=VERTEX_POINT ( 'NONE', #44754 ) ;
#37868=VECTOR ( 'NONE', #25629, 1000.000000000000114 ) ;
#37869=CARTESIAN_POINT ( 'NONE',  ( 16.13393739769620083, -15.61618894467929941, -69.65000000000000568 ) ) ;
#37887=CARTESIAN_POINT ( 'NONE',  ( 44.39456236031976033, 8.753821728143037717, -64.74790854932149387 ) ) ;
#37891=ORIENTED_EDGE ( 'NONE', *, *, #14, .F. ) ;
#37893=EDGE_LOOP ( 'NONE', ( #15070, #28645, #26072, #44973 ) ) ;
#37894=CARTESIAN_POINT ( 'NONE',  ( -22.79177331775788673, -17.86816468640815003, -54.71780484469083206 ) ) ;
#37901=CARTESIAN_POINT ( 'NONE',  ( 28.13393739769619728, -8.687985714403851034, -35.14999999999999858 ) ) ;
#37902=CARTESIAN_POINT ( 'NONE',  ( 16.13393739769620083, -29.53197612349504553, -34.89146800830128825 ) ) ;
#37916=CARTESIAN_POINT ( 'NONE',  ( 46.47536507427530239, 8.886826513564159313, -54.64999999999999858 ) ) ;
#37924=DIRECTION ( 'NONE',  ( 0.000000000000000000, 0.000000000000000000, 1.000000000000000000 ) ) ;
#37927=CARTESIAN_POINT ( 'NONE',  ( 19.13393739769620083, -49.61618894467939356, -34.64999999999999858 ) ) ;
#37933=CIRCLE ( 'NONE', #30356, 2.999999999999999112 ) ;
#37935=CIRCLE ( 'NONE', #38818, 33.00000000000000000 ) ;
#37936=ORIENTED_EDGE ( 'NONE', *, *, #19027, .T. ) ;
#37945=CARTESIAN_POINT ( 'NONE',  ( 33.13393739769620083, -38.61618894467930119, -59.64999999999999147 ) ) ;
#37948=ORIENTED_EDGE ( 'NONE', *, *, #12856, .T. ) ;
#37956=CARTESIAN_POINT ( 'NONE',  ( -13.78940531703979921, -41.12028084088070301, -46.90119366654699462 ) ) ;
#37964=ORIENTED_EDGE ( 'NONE', *, *, #5581, .T. ) ;
#37973=EDGE_CURVE ( 'NONE', #43880, #19145, #29001, .T. ) ;
#37975=VERTEX_POINT ( 'NONE', #39160 ) ;
#37979=ADVANCED_FACE ( 'NONE', ( #31524 ), #45659, .F. ) ;
#37981=VECTOR ( 'NONE', #22660, 1000.000000000000114 ) ;
#37991=VECTOR ( 'NONE', #44930, 1000.000000000000000 ) ;
#37992=CARTESIAN_POINT ( 'NONE',  ( -15.80024602150229640, 6.819013759894939852, -48.50583260171929822 ) ) ;
#37994=CARTESIAN_POINT ( 'NONE',  ( 46.26053575279389918, -39.27325360143171196, -59.27255113039620937 ) ) ;
#37996=EDGE_CURVE ( 'NONE', #5090, #46086, #29646, .T. ) ;
#38001=CARTESIAN_POINT ( 'NONE',  ( 47.45189513940888304, 8.060285789217719099, -53.60622457599794899 ) ) ;
#38020=ADVANCED_FACE ( 'NONE', ( #15568 ), #14786, .T. ) ;
#38029=CARTESIAN_POINT ( 'NONE',  ( -11.80944000494479873, 2.826328597561450273, -45.03554556751399929 ) ) ;
#38036=CARTESIAN_POINT ( 'NONE',  ( 0.08961746015897857631, -26.87852304757121402, -34.70268271585498354 ) ) ;
#38042=CARTESIAN_POINT ( 'NONE',  ( 45.92519079177113639, -38.14579169924610369, -60.69370282983792464 ) ) ;
#38043=ORIENTED_EDGE ( 'NONE', *, *, #21679, .T. ) ;
#38060=CARTESIAN_POINT ( 'NONE',  ( 41.91337957294418004, -39.75513214800343320, -76.74976791096347029 ) ) ;
#38062=ORIENTED_EDGE ( 'NONE', *, *, #41819, .T. ) ;
#38063=( BOUNDED_CURVE ( )  B_SPLINE_CURVE ( 2, ( #8738, #5075, #13206 ),
 .UNSPECIFIED., .F., .T. ) 
 B_SPLINE_CURVE_WITH_KNOTS ( ( 3, 3 ),
 ( 0.09013492862022640106, 2.097321517346030006 ),
 .UNSPECIFIED. ) 
 CURVE ( )  GEOMETRIC_REPRESENTATION_ITEM ( )  RATIONAL_B_SPLINE_CURVE ( ( 1.000760683868189949, 1.008873536167329998, 1.001092624574940082 ) ) 
 REPRESENTATION_ITEM ( '' )  );
#38078=DIRECTION ( 'NONE',  ( 0.000000000000000000, 0.000000000000000000, 1.000000000000000000 ) ) ;
#38082=ADVANCED_FACE ( 'NONE', ( #12152 ), #31777, .T. ) ;
#38085=ORIENTED_EDGE ( 'NONE', *, *, #30435, .T. ) ;
#38096=CARTESIAN_POINT ( 'NONE',  ( 16.97276188636949712, 12.56821928479469896, -59.64999999999999147 ) ) ;
#38101=CARTESIAN_POINT ( 'NONE',  ( 45.54888968018341444, 6.872726959284684689, -62.57519952278095587 ) ) ;
#38110=EDGE_CURVE ( 'NONE', #16597, #24679, #8406, .T. ) ;
#38112=VECTOR ( 'NONE', #47717, 1000.000000000000000 ) ;
#38113=CARTESIAN_POINT ( 'NONE',  ( 14.18536260820854800, 10.43523626583284347, -34.89146800830132378 ) ) ;
#38119=CARTESIAN_POINT ( 'NONE',  ( 18.11900864776900022, 1.362847559348050019, -35.02873218748179340 ) ) ;
#38125=CARTESIAN_POINT ( 'NONE',  ( 3.892469389394927148, -22.68380379454831086, -34.70142521051216988 ) ) ;
#38129=DIRECTION ( 'NONE',  ( 0.000000000000000000, 1.000000000000000000, 0.000000000000000000 ) ) ;
#38133=ORIENTED_EDGE ( 'NONE', *, *, #27334, .T. ) ;
#38136=VERTEX_POINT ( 'NONE', #50890 ) ;
#38139=DIRECTION ( 'NONE',  ( 1.000000000000000000, 0.000000000000000000, 0.000000000000000000 ) ) ;
#38141=CARTESIAN_POINT ( 'NONE',  ( 43.19653520511483435, 8.652243319877685579, -70.54837756005113647 ) ) ;
#38147=AXIS2_PLACEMENT_3D ( 'NONE', #47796, #32029, #28106 ) ;
#38150=VERTEX_POINT ( 'NONE', #50116 ) ;
#38151=CARTESIAN_POINT ( 'NONE',  ( -22.70962239977677299, -19.05578711724787411, -54.67894118608715104 ) ) ;
#38175=CARTESIAN_POINT ( 'NONE',  ( 46.78220155478780384, 8.502076674257970978, -54.45081220080809459 ) ) ;
#38177=ORIENTED_EDGE ( 'NONE', *, *, #30685, .F. ) ;
#38183=CARTESIAN_POINT ( 'NONE',  ( 0.3209249304026170480, -15.61618894467929941, -35.14999999999999858 ) ) ;
#38187=MECHANICAL_DESIGN_GEOMETRIC_PRESENTATION_REPRESENTATION('',(#33969),#49089);
#38190=VERTEX_POINT ( 'NONE', #22571 ) ;
#38214=CARTESIAN_POINT ( 'NONE',  ( 0.8822469062514919358, -51.51059052437120300, -34.40037443414259144 ) ) ;
#38239=FACE_OUTER_BOUND ( 'NONE', #23723, .T. ) ;
#38249=CARTESIAN_POINT ( 'NONE',  ( -15.91219141626359956, 7.039674273257229942, -48.73593760451629464 ) ) ;
#38251=CARTESIAN_POINT ( 'NONE',  ( 41.63730079839010045, -38.78348554106982249, -82.15224707392265202 ) ) ;
#38266=DIRECTION ( 'NONE',  ( 0.000000000000000000, 0.000000000000000000, -1.000000000000000000 ) ) ;
#38268=EDGE_CURVE ( 'NONE', #17159, #15981, #28951, .T. ) ;
#38270=EDGE_CURVE ( 'NONE', #1146, #22337, #9750, .T. ) ;
#38281=EDGE_CURVE ( 'NONE', #15666, #40171, #6395, .T. ) ;
#38287=CARTESIAN_POINT ( 'NONE',  ( 16.13393739769620083, -15.61618894467929941, -34.64999999999999858 ) ) ;
#38290=ORIENTED_EDGE ( 'NONE', *, *, #10118, .F. ) ;
#38291=DIRECTION ( 'NONE',  ( 1.000000000000000000, 0.000000000000000000, 0.000000000000000000 ) ) ;
#38295=CARTESIAN_POINT ( 'NONE',  ( 8.643744238043529649, 17.52287609088129727, -35.14999999999999858 ) ) ;
#38298=CARTESIAN_POINT ( 'NONE',  ( 43.48544627107390426, -37.84702645128613341, -72.89241229296673907 ) ) ;
#38299=ADVANCED_FACE ( 'NONE', ( #46808 ), #48334, .T. ) ;
#38316=CARTESIAN_POINT ( 'NONE',  ( 41.47164856782293185, -39.70574416324859612, -78.88105259561210403 ) ) ;
#38318=CARTESIAN_POINT ( 'NONE',  ( 25.03312433582057750, -22.08182671989646906, -84.65000000000000568 ) ) ;
#38326=CARTESIAN_POINT ( 'NONE',  ( 40.57649240635721100, -37.56081407618430035, -83.97002642401369599 ) ) ;
#38344=VERTEX_POINT ( 'NONE', #41244 ) ;
#38345=CARTESIAN_POINT ( 'NONE',  ( 14.13393739769640156, 6.292713355527309815, -54.64999999999999858 ) ) ;
#38353=CARTESIAN_POINT ( 'NONE',  ( 44.13393739769620083, 4.883811055320659733, -35.14999999999999858 ) ) ;
#38354=CARTESIAN_POINT ( 'NONE',  ( 46.55606098839130880, 6.976707678039790750, -57.53936765601046233 ) ) ;
#38355=CARTESIAN_POINT ( 'NONE',  ( -17.22968739472086241, 4.597376488843254450, -50.03813090013385079 ) ) ;
#38367=DIRECTION ( 'NONE',  ( 0.000000000000000000, -1.000000000000000000, 0.000000000000000000 ) ) ;
#38374=DIRECTION ( 'NONE',  ( -1.000000000000000000, 0.000000000000000000, 0.000000000000000000 ) ) ;
#38375=EDGE_CURVE ( 'NONE', #40090, #8235, #48468, .T. ) ;
#38379=CARTESIAN_POINT ( 'NONE',  ( 44.89330862275510725, -33.71195016353239993, -35.14497980672799571 ) ) ;
#38381=DIRECTION ( 'NONE',  ( 0.000000000000000000, 1.000000000000000000, 0.000000000000000000 ) ) ;
#38385=CARTESIAN_POINT ( 'NONE',  ( 11.96660005458869946, 10.88381105532060111, -34.64999999999999858 ) ) ;
#38389=CARTESIAN_POINT ( 'NONE',  ( 16.13393739769620083, -1.590680505402594314, -34.79644660940672196 ) ) ;
#38390=ORIENTED_EDGE ( 'NONE', *, *, #32427, .F. ) ;
#38391=EDGE_CURVE ( 'NONE', #18174, #9837, #40677, .T. ) ;
#38397=CARTESIAN_POINT ( 'NONE',  ( 8.643744238043529649, 17.52287609088129727, -35.14999999999999858 ) ) ;
#38398=VECTOR ( 'NONE', #51759, 1000.000000000000000 ) ;
#38401=CONICAL_SURFACE ( 'NONE', #12553, 36.50000000000000000, 0.1651486774146265213 ) ;
#38404=ADVANCED_FACE ( 'NONE', ( #42287 ), #46752, .T. ) ;
#38405=ORIENTED_EDGE ( 'NONE', *, *, #34876, .T. ) ;
#38413=FACE_OUTER_BOUND ( 'NONE', #16852, .T. ) ;
#38415=ORIENTED_EDGE ( 'NONE', *, *, #7470, .T. ) ;
#38421=CARTESIAN_POINT ( 'NONE',  ( 16.13393739769620083, -30.04994567442000175, -34.64999999999999858 ) ) ;
#38426=CIRCLE ( 'NONE', #40108, 2.999999999999999112 ) ;
#38428=CARTESIAN_POINT ( 'NONE',  ( 46.83318063571350365, 8.437011769841980424, -54.37544270859390139 ) ) ;
#38429=AXIS2_PLACEMENT_3D ( 'NONE', #38287, #34330, #41693 ) ;
#38438=CARTESIAN_POINT ( 'NONE',  ( 44.37302628842170549, -39.98451940133276850, -64.85227893969756963 ) ) ;
#38446=VERTEX_POINT ( 'NONE', #38619 ) ;
#38458=CARTESIAN_POINT ( 'NONE',  ( 20.63393739769620083, -41.61618894467930119, -35.14999999999999858 ) ) ;
#38467=DIRECTION ( 'NONE',  ( -1.000000000000000000, 0.000000000000000000, 0.000000000000000000 ) ) ;
#38481=ORIENTED_EDGE ( 'NONE', *, *, #18469, .T. ) ;
#38498=EDGE_CURVE ( 'NONE', #40171, #43323, #19683, .T. ) ;
#38502=FACE_OUTER_BOUND ( 'NONE', #7838, .T. ) ;
#38513=CARTESIAN_POINT ( 'NONE',  ( 47.17216055865273461, -39.34257126785092140, -54.74311960827047585 ) ) ;
#38516=EDGE_CURVE ( 'NONE', #39196, #46682, #32967, .T. ) ;
#38521=CARTESIAN_POINT ( 'NONE',  ( 46.39291221988571579, 9.013049155818599445, -54.53239148715100271 ) ) ;
#38526=CARTESIAN_POINT ( 'NONE',  ( 29.00424600244190287, -26.69196671705950052, -34.81403640487199880 ) ) ;
#38529=ADVANCED_FACE ( 'NONE', ( #21438 ), #1538, .T. ) ;
#38530=DIRECTION ( 'NONE',  ( 0.6339889056055360017, 0.000000000000000000, -0.7733421413379041320 ) ) ;
#38545=VERTEX_POINT ( 'NONE', #39169 ) ;
#38549=DIRECTION ( 'NONE',  ( 0.000000000000000000, 0.000000000000000000, -1.000000000000000000 ) ) ;
#38552=AXIS2_PLACEMENT_3D ( 'NONE', #32652, #44740, #45001 ) ;
#38558=CARTESIAN_POINT ( 'NONE',  ( 17.87670698131359970, -32.37825826146760733, -34.70985242058469566 ) ) ;
#38559=VECTOR ( 'NONE', #4442, 1000.000000000000000 ) ;
#38563=CARTESIAN_POINT ( 'NONE',  ( 44.94746977831004386, -38.03605091149837136, -65.58232186645768991 ) ) ;
#38569=B_SPLINE_CURVE_WITH_KNOTS ( 'NONE', 3,
 ( #20065, #39493, #19821, #7263, #3591, #7010 ),
 .UNSPECIFIED., .F., .F.,
 ( 4, 2, 4 ),
 ( -0.0003214729304729410479, 0.000000000000000000, 0.01784182840660334182 ),
 .UNSPECIFIED. ) ;
#38571=EDGE_CURVE ( 'NONE', #13264, #13283, #49900, .T. ) ;
#38573=ADVANCED_FACE ( 'NONE', ( #6682 ), #7454, .F. ) ;
#38578=EDGE_LOOP ( 'NONE', ( #21754, #33111, #15637, #29170 ) ) ;
#38582=CARTESIAN_POINT ( 'NONE',  ( 41.17180578240099464, -39.67071095666287306, -80.32671525995388606 ) ) ;
#38583=CARTESIAN_POINT ( 'NONE',  ( 20.30127474080329719, 10.88381105532070059, -34.64999999999999858 ) ) ;
#38589=AXIS2_PLACEMENT_3D ( 'NONE', #25071, #5454, #44760 ) ;
#38599=SPHERICAL_SURFACE ( 'NONE', #2475, 3.000000000000000000 ) ;
#38602=EDGE_CURVE ( 'NONE', #43797, #12820, #7213, .T. ) ;
#38615=ORIENTED_EDGE ( 'NONE', *, *, #4646, .T. ) ;
#38619=CARTESIAN_POINT ( 'NONE',  ( 28.28038400710289935, -8.603434725040973063, -34.79644660940672907 ) ) ;
#38623=CARTESIAN_POINT ( 'NONE',  ( 43.34994082412796956, 6.595960187102031469, -73.56991816002565088 ) ) ;
#38627=DIRECTION ( 'NONE',  ( 0.000000000000000000, -1.000000000000000000, 0.000000000000000000 ) ) ;
#38638=CARTESIAN_POINT ( 'NONE',  ( -0.4410626023037830246, -8.356009309619699010, -35.14999999999999858 ) ) ;
#38639=EDGE_CURVE ( 'NONE', #46452, #9063, #23151, .T. ) ;
#38651=CARTESIAN_POINT ( 'NONE',  ( 14.23931515459926089, 1.282173023328767369, -34.84133294386911217 ) ) ;
#38654=EDGE_CURVE ( 'NONE', #6764, #20524, #7965, .T. ) ;
#38665=ORIENTED_EDGE ( 'NONE', *, *, #27742, .T. ) ;
#38674=CARTESIAN_POINT ( 'NONE',  ( 45.49455817588943773, 8.831023168557877057, -59.41298158052058653 ) ) ;
#38678=ORIENTED_EDGE ( 'NONE', *, *, #27334, .F. ) ;
#38683=CARTESIAN_POINT ( 'NONE',  ( -22.60072279458010058, -20.15755767129849829, -54.65015892017029842 ) ) ;
#38684=EDGE_CURVE ( 'NONE', #37751, #13264, #35767, .T. ) ;
#38688=CARTESIAN_POINT ( 'NONE',  ( 16.13393739769639623, 7.383811055320659733, -59.64999999999999147 ) ) ;
#38689=CARTESIAN_POINT ( 'NONE',  ( 45.17583307331749864, -33.37024725518060109, -34.90149097438519732 ) ) ;
#38690=VERTEX_POINT ( 'NONE', #12680 ) ;
#38691=CARTESIAN_POINT ( 'NONE',  ( 2.404741263826560171, -25.85214510508460251, -35.14999999999999858 ) ) ;
#38701=LINE ( 'NONE', #31314, #25519 ) ;
#38705=ORIENTED_EDGE ( 'NONE', *, *, #6759, .F. ) ;
#38709=CARTESIAN_POINT ( 'NONE',  ( 45.43114679010229651, -40.05928987699603283, -59.72086155090411097 ) ) ;
#38723=LINE ( 'NONE', #2819, #37837 ) ;
#38735=CARTESIAN_POINT ( 'NONE',  ( 41.61626771661330082, -36.11618894467930119, -82.23834840541459812 ) ) ;
#38736=AXIS2_PLACEMENT_3D ( 'NONE', #12766, #25304, #960 ) ;
#38740=ORIENTED_EDGE ( 'NONE', *, *, #3366, .F. ) ;
#38742=ORIENTED_EDGE ( 'NONE', *, *, #20746, .T. ) ;
#38754=EDGE_LOOP ( 'NONE', ( #39455, #24435, #46343, #27879 ) ) ;
#38755=CARTESIAN_POINT ( 'NONE',  ( 16.13393739769620083, -1.182432214938700099, -34.64999999999999858 ) ) ;
#38759=FACE_OUTER_BOUND ( 'NONE', #37049, .T. ) ;
#38771=AXIS2_PLACEMENT_3D ( 'NONE', #5418, #1481, #8829 ) ;
#38778=CARTESIAN_POINT ( 'NONE',  ( -21.99499352544900077, -6.866245975711579241, -54.13127606174950301 ) ) ;
#38783=ORIENTED_EDGE ( 'NONE', *, *, #47093, .F. ) ;
#38786=CARTESIAN_POINT ( 'NONE',  ( 47.23718928093980196, 8.041435364245701933, -54.67975386834223883 ) ) ;
#38812=DIRECTION ( 'NONE',  ( 1.000000000000000000, 0.000000000000000000, 0.000000000000000000 ) ) ;
#38818=AXIS2_PLACEMENT_3D ( 'NONE', #30463, #42804, #10573 ) ;
#38825=CARTESIAN_POINT ( 'NONE',  ( 47.05500271796362455, -38.25475083058559989, -55.04467339866013731 ) ) ;
#38828=CARTESIAN_POINT ( 'NONE',  ( -22.76700179775898292, -12.96293114564705284, -54.70490354874866767 ) ) ;
#38837=( BOUNDED_CURVE ( )  B_SPLINE_CURVE ( 3, ( #32363, #32620, #48382, #44448 ),
 .UNSPECIFIED., .F., .T. ) 
 B_SPLINE_CURVE_WITH_KNOTS ( ( 4, 4 ),
 ( 4.712388980384684345, 5.070260775219124660 ),
 .UNSPECIFIED. ) 
 CURVE ( )  GEOMETRIC_REPRESENTATION_ITEM ( )  RATIONAL_B_SPLINE_CURVE ( ( 1.000000000000000000, 0.9893557610490359977, 0.9893557610490359977, 1.000000000000000000 ) ) 
 REPRESENTATION_ITEM ( '' )  );
#38846=AXIS2_PLACEMENT_3D ( 'NONE', #23526, #7067, #3647 ) ;
#38856=DIRECTION ( 'NONE',  ( 0.8090169943749464521, -0.5877852522924744694, 0.000000000000000000 ) ) ;
#38857=CARTESIAN_POINT ( 'NONE',  ( -0.04495657159227190586, -45.64487445774500429, -34.80555997329428664 ) ) ;
#38859=CARTESIAN_POINT ( 'NONE',  ( 29.46622902366960162, 1.883811055320659955, -54.64999999999999858 ) ) ;
#38860=APPLICATION_CONTEXT ( 'automotive_design' ) ;
#38868=EDGE_LOOP ( 'NONE', ( #44854, #30926, #14620, #41240 ) ) ;
#38869=EDGE_LOOP ( 'NONE', ( #32110, #27873, #47065, #45191, #42777, #161, #16236, #50979, #21868, #39490, #25694, #24441, #30925, #50765, #14235, #45685, #20014, #28678, #18097, #27761, #18994, #36269, #46547, #40371, #29660, #46697, #16320, #49437, #8114, #25292, #13274, #42857, #34193, #29502, #28693, #9824, #45759, #4864, #44888, #23435, #14556, #33684, #115, #50115, #28870, #6256, #20753, #2051, #19203, #25242, #26137, #26164 ) ) ;
#38881=CARTESIAN_POINT ( 'NONE',  ( 44.46199409210488085, 6.744907085701958849, -68.00970624157608313 ) ) ;
#38895=EDGE_CURVE ( 'NONE', #13523, #5090, #1425, .T. ) ;
#38896=EDGE_CURVE ( 'NONE', #26692, #6571, #27681, .T. ) ;
#38915=CARTESIAN_POINT ( 'NONE',  ( 16.13393739769620083, -15.61618894467929941, -35.02873218748179340 ) ) ;
#38923=DIRECTION ( 'NONE',  ( 0.000000000000000000, 0.000000000000000000, -1.000000000000000000 ) ) ;
#38925=CARTESIAN_POINT ( 'NONE',  ( 45.38228619634400474, 8.823823693349686081, -59.95777824142523116 ) ) ;
#38926=CARTESIAN_POINT ( 'NONE',  ( -0.007164427059776000244, -4.186223695871990280, -34.77269723891829756 ) ) ;
#38930=ORIENTED_EDGE ( 'NONE', *, *, #25238, .F. ) ;
#38932=ORIENTED_EDGE ( 'NONE', *, *, #26608, .T. ) ;
#38933=FACE_OUTER_BOUND ( 'NONE', #4365, .T. ) ;
#38935=EDGE_CURVE ( 'NONE', #38545, #2764, #47616, .T. ) ;
#38936=CARTESIAN_POINT ( 'NONE',  ( 16.13393739769620083, -15.61618894467929941, 36.77166666666649775 ) ) ;
#38937=ADVANCED_FACE ( 'NONE', ( #11464 ), #22260, .T. ) ;
#38941=ORIENTED_EDGE ( 'NONE', *, *, #36951, .T. ) ;
#38945=ORIENTED_EDGE ( 'NONE', *, *, #13327, .T. ) ;
#38957=PLANE ( 'NONE',  #22663 ) ;
#38963=CARTESIAN_POINT ( 'NONE',  ( 45.06222871821497478, -40.03483142178188814, -61.51087723771117055 ) ) ;
#38982=DIRECTION ( 'NONE',  ( 0.000000000000000000, 0.000000000000000000, -1.000000000000000000 ) ) ;
#38986=LINE ( 'NONE', #46080, #35128 ) ;
#38987=DIRECTION ( 'NONE',  ( 0.000000000000000000, 0.000000000000000000, -1.000000000000000000 ) ) ;
#38989=ORIENTED_EDGE ( 'NONE', *, *, #12133, .T. ) ;
#38992=EDGE_LOOP ( 'NONE', ( #11870, #34756, #18245, #18750, #36406 ) ) ;
#38997=ORIENTED_EDGE ( 'NONE', *, *, #51250, .T. ) ;
#39007=CARTESIAN_POINT ( 'NONE',  ( 9.124981245646200279, 17.63186422973200251, -35.14566343974350104 ) ) ;
#39009=CARTESIAN_POINT ( 'NONE',  ( 14.13393739769599833, 14.38381105532070059, -49.33749999999999858 ) ) ;
#39011=LINE ( 'NONE', #38755, #30189 ) ;
#39016=EDGE_CURVE ( 'NONE', #29117, #3105, #756, .T. ) ;
#39022=CARTESIAN_POINT ( 'NONE',  ( 46.63300573313630082, -39.92275617562160051, -54.59612248810249469 ) ) ;
#39027=CARTESIAN_POINT ( 'NONE',  ( 23.62342291817629913, 17.52530927293010166, -35.10565360069929852 ) ) ;
#39032=VECTOR ( 'NONE', #19113, 1000.000000000000000 ) ;
#39034=EDGE_CURVE ( 'NONE', #34773, #14662, #419, .T. ) ;
#39036=DIRECTION ( 'NONE',  ( 0.8204012560548797905, 0.5717882292104092823, 0.000000000000000000 ) ) ;
#39039=EDGE_CURVE ( 'NONE', #39828, #13190, #10667, .T. ) ;
#39040=ORIENTED_EDGE ( 'NONE', *, *, #51530, .T. ) ;
#39043=CARTESIAN_POINT ( 'NONE',  ( 47.12471753871997748, 6.751739564498508095, -54.63036517340856335 ) ) ;
#39065=EDGE_CURVE ( 'NONE', #51621, #18232, #31141, .T. ) ;
#39075=CARTESIAN_POINT ( 'NONE',  ( 16.13393739769620083, -15.61618894467919816, -82.14319696191608955 ) ) ;
#39078=DIRECTION ( 'NONE',  ( 0.000000000000000000, -1.000000000000000000, 0.000000000000000000 ) ) ;
#39085=CARTESIAN_POINT ( 'NONE',  ( 13.13393739769619906, -49.61618894467939356, -35.14999999999999858 ) ) ;
#39088=CIRCLE ( 'NONE', #2261, 3.000000000000005773 ) ;
#39089=CARTESIAN_POINT ( 'NONE',  ( 47.13393657218789912, 8.048130458325550407, -53.76789950451890121 ) ) ;
#39100=CARTESIAN_POINT ( 'NONE',  ( 14.14886614762350092, -32.59522544870679894, -35.02873218748179340 ) ) ;
#39102=EDGE_CURVE ( 'NONE', #7036, #24695, #38837, .T. ) ;
#39103=ORIENTED_EDGE ( 'NONE', *, *, #11943, .T. ) ;
#39115=DIRECTION ( 'NONE',  ( 0.7071067811865510144, 0.000000000000000000, 0.7071067811865441310 ) ) ;
#39130=FACE_BOUND ( 'NONE', #19409, .T. ) ;
#39136=CARTESIAN_POINT ( 'NONE',  ( 44.85897114471773506, 6.793334218869983232, -66.02479074488660160 ) ) ;
#39138=ORIENTED_EDGE ( 'NONE', *, *, #48371, .F. ) ;
#39149=CIRCLE ( 'NONE', #11551, 2.500000000000000444 ) ;
#39160=CARTESIAN_POINT ( 'NONE',  ( 45.14919548887390022, -33.29386571476810275, -35.12503119152809461 ) ) ;
#39169=CARTESIAN_POINT ( 'NONE',  ( 16.13393739769620083, -1.759782484128330049, -47.64999999999999858 ) ) ;
#39179=CARTESIAN_POINT ( 'NONE',  ( 45.75084721212736838, 8.846752882301483822, -58.16900694336454336 ) ) ;
#39187=DIRECTION ( 'NONE',  ( 0.000000000000000000, 0.000000000000000000, -1.000000000000000000 ) ) ;
#39195=DIRECTION ( 'NONE',  ( -0.8660254037844472563, -0.4999999999999851785, 0.000000000000000000 ) ) ;
#39196=VERTEX_POINT ( 'NONE', #33151 ) ;
#39211=CARTESIAN_POINT ( 'NONE',  ( 45.06511394444972041, -40.03503324105221850, -61.49686747805221643 ) ) ;
#39215=AXIS2_PLACEMENT_3D ( 'NONE', #45771, #14569, #45514 ) ;
#39226=ORIENTED_EDGE ( 'NONE', *, *, #4646, .F. ) ;
#39239=CARTESIAN_POINT ( 'NONE',  ( 18.13393739769620439, -34.76920587681881614, -43.67210485825550847 ) ) ;
#39244=DIRECTION ( 'NONE',  ( 0.000000000000000000, 0.000000000000000000, -1.000000000000000000 ) ) ;
#39255=CARTESIAN_POINT ( 'NONE',  ( 19.13393739769600188, 18.38381105532069881, -83.01107220193038927 ) ) ;
#39259=CARTESIAN_POINT ( 'NONE',  ( 29.12893361417140525, -26.73813571787616539, -35.06842082984513098 ) ) ;
#39270=DIRECTION ( 'NONE',  ( 0.000000000000000000, 0.000000000000000000, 1.000000000000000000 ) ) ;
#39277=EDGE_CURVE ( 'NONE', #38344, #4837, #45137, .T. ) ;
#39282=CYLINDRICAL_SURFACE ( 'NONE', #24246, 2.999999999999999556 ) ;
#39284=CARTESIAN_POINT ( 'NONE',  ( 47.67266003423409870, -38.15547488882079818, -51.93650398367349652 ) ) ;
#39288=AXIS2_PLACEMENT_3D ( 'NONE', #3685, #12067, #19902 ) ;
#39291=VECTOR ( 'NONE', #45459, 1000.000000000000000 ) ;
#39293=CARTESIAN_POINT ( 'NONE',  ( 44.59253762482858718, 6.549697931826371722, -67.31859651280061030 ) ) ;
#39295=CARTESIAN_POINT ( 'NONE',  ( 46.99731062513887281, -39.23427468941395801, -34.80647497723114725 ) ) ;
#39317=ORIENTED_EDGE ( 'NONE', *, *, #6440, .T. ) ;
#39331=B_SPLINE_CURVE_WITH_KNOTS ( 'NONE', 3,
 ( #17713, #33680, #49695, #13788, #29746, #17967, #37894, #9851, #25807, #41814, #6184, #22141, #38151, #18224, #26334, #30268, #46286 ),
 .UNSPECIFIED., .F., .F.,
 ( 4, 2, 2, 2, 2, 1, 2, 2, 4 ),
 ( 0.4766446636200218356, 0.5420640806675175449, 0.6074834977150133097, 0.7383223318100058385, 0.7546771860718798353, 0.7710320403337540540, 0.8037417488575033797, 0.8691611659050022531, 1.000000000000000000 ),
 .UNSPECIFIED. ) ;
#39332=ORIENTED_EDGE ( 'NONE', *, *, #51515, .T. ) ;
#39333=ORIENTED_EDGE ( 'NONE', *, *, #33201, .F. ) ;
#39340=VECTOR ( 'NONE', #51556, 1000.000000000000000 ) ;
#39353=CARTESIAN_POINT ( 'NONE',  ( 30.95441726489424283, -35.72841810710970378, -84.62495954532434439 ) ) ;
#39356=ORIENTED_EDGE ( 'NONE', *, *, #28990, .T. ) ;
#39377=LINE ( 'NONE', #51430, #49404 ) ;
#39388=CARTESIAN_POINT ( 'NONE',  ( 45.06955000105763531, 6.818482170417528465, -64.97193686384484579 ) ) ;
#39391=ORIENTED_EDGE ( 'NONE', *, *, #408, .T. ) ;
#39397=CIRCLE ( 'NONE', #26810, 16.60961179679778965 ) ;
#39408=AXIS2_PLACEMENT_3D ( 'NONE', #7854, #35632, #42992 ) ;
#39418=CARTESIAN_POINT ( 'NONE',  ( 13.04629919360907309, 18.51631118994176362, -82.73668660645843431 ) ) ;
#39420=CARTESIAN_POINT ( 'NONE',  ( 18.65820481519197926, 18.38381105532056736, -83.09320499157193751 ) ) ;
#39434=DIRECTION ( 'NONE',  ( 0.000000000000000000, 0.000000000000000000, 1.000000000000000000 ) ) ;
#39437=CARTESIAN_POINT ( 'NONE',  ( 16.13393739769620083, -29.64169738395614218, -34.79644660940672907 ) ) ;
#39446=CARTESIAN_POINT ( 'NONE',  ( 23.32430482491560042, -49.33365190531349498, -34.64999999999999858 ) ) ;
#39451=AXIS2_PLACEMENT_3D ( 'NONE', #21891, #29750, #9857 ) ;
#39452=ORIENTED_EDGE ( 'NONE', *, *, #1045, .T. ) ;
#39453=AXIS2_PLACEMENT_3D ( 'NONE', #48463, #28265, #44267 ) ;
#39455=ORIENTED_EDGE ( 'NONE', *, *, #36112, .T. ) ;
#39457=EDGE_CURVE ( 'NONE', #36574, #12279, #28160, .T. ) ;
#39468=DIRECTION ( 'NONE',  ( 1.000000000000000000, 0.000000000000000000, 0.000000000000000000 ) ) ;
#39476=CARTESIAN_POINT ( 'NONE',  ( 45.77061686725269141, -40.08029671403183158, -58.07308786245754106 ) ) ;
#39478=VECTOR ( 'NONE', #17046, 1000.000000000000000 ) ;
#39479=CIRCLE ( 'NONE', #24359, 3.000000000000003997 ) ;
#39480=AXIS2_PLACEMENT_3D ( 'NONE', #50792, #30845, #19066 ) ;
#39490=ORIENTED_EDGE ( 'NONE', *, *, #6376, .F. ) ;
#39493=CARTESIAN_POINT ( 'NONE',  ( 0.3198662801700680181, -20.69846475549559983, -34.64999999999999858 ) ) ;
#39497=CARTESIAN_POINT ( 'NONE',  ( 29.92510725984174158, 4.389127169904199377, -84.60896002036976427 ) ) ;
#39499=ORIENTED_EDGE ( 'NONE', *, *, #17749, .F. ) ;
#39500=DIRECTION ( 'NONE',  ( -0.8660254037844387076, -0.4999999999999998890, 0.000000000000000000 ) ) ;
#39501=ORIENTED_EDGE ( 'NONE', *, *, #30555, .F. ) ;
#39502=ORIENTED_EDGE ( 'NONE', *, *, #29257, .F. ) ;
#39507=ORIENTED_EDGE ( 'NONE', *, *, #40577, .T. ) ;
#39520=DIRECTION ( 'NONE',  ( 0.000000000000000000, 0.000000000000000000, -1.000000000000000000 ) ) ;
#39522=CARTESIAN_POINT ( 'NONE',  ( 16.13393739769620083, -15.61618894467929941, -34.64999999999999858 ) ) ;
#39524=CARTESIAN_POINT ( 'NONE',  ( 17.63393739769620083, -42.11618894467939356, -34.64999999999999858 ) ) ;
#39538=CARTESIAN_POINT ( 'NONE',  ( 11.63393739769619906, -41.61618894467930119, -35.14999999999999858 ) ) ;
#39543=CARTESIAN_POINT ( 'NONE',  ( 44.14642363104649547, -37.85759600627010002, -69.58218121927448863 ) ) ;
#39546=ORIENTED_EDGE ( 'NONE', *, *, #22678, .F. ) ;
#39550=CARTESIAN_POINT ( 'NONE',  ( 40.77547000184679860, 7.884666264946645242, -85.73440608552456865 ) ) ;
#39553=CARTESIAN_POINT ( 'NONE',  ( 47.13393739769619373, -39.28050807707779768, -35.14999999999999858 ) ) ;
#39557=DIRECTION ( 'NONE',  ( 0.000000000000000000, 0.000000000000000000, 1.000000000000000000 ) ) ;
#39566=CARTESIAN_POINT ( 'NONE',  ( 16.13393739769620083, -15.61618894467929941, -69.65000000000000568 ) ) ;
#39567=ORIENTED_EDGE ( 'NONE', *, *, #39102, .T. ) ;
#39576=ORIENTED_EDGE ( 'NONE', *, *, #24172, .T. ) ;
#39577=EDGE_CURVE ( 'NONE', #45957, #2565, #45793, .T. ) ;
#39588=ORIENTED_EDGE ( 'NONE', *, *, #39457, .T. ) ;
#39593=DIRECTION ( 'NONE',  ( 0.000000000000000000, 0.000000000000000000, -1.000000000000000000 ) ) ;
#39597=CARTESIAN_POINT ( 'NONE',  ( 10.06369629474122185, 22.76024865223496363, -34.79644414665609986 ) ) ;
#39608=VERTEX_POINT ( 'NONE', #23319 ) ;
#39618=DIRECTION ( 'NONE',  ( -0.3502816565540492477, 0.000000000000000000, 0.9366444154970182678 ) ) ;
#39619=CARTESIAN_POINT ( 'NONE',  ( 13.13393739769600010, 18.38381105532060289, -35.14999999999999858 ) ) ;
#39626=CARTESIAN_POINT ( 'NONE',  ( 18.13393739769620083, -41.61618894467930119, -35.14999999999999858 ) ) ;
#39632=CARTESIAN_POINT ( 'NONE',  ( 16.13393739769620083, -15.61618894467929941, -643.2998782751060389 ) ) ;
#39635=ORIENTED_EDGE ( 'NONE', *, *, #34292, .T. ) ;
#39637=DIRECTION ( 'NONE',  ( 1.000000000000000000, 0.000000000000000000, 0.000000000000000000 ) ) ;
#39643=CARTESIAN_POINT ( 'NONE',  ( 44.28781032986178445, 6.722397411424160474, -68.88062643755992553 ) ) ;
#39654=DIRECTION ( 'NONE',  ( 0.000000000000000000, 1.000000000000000000, 0.000000000000000000 ) ) ;
#39667=DIRECTION ( 'NONE',  ( 0.000000000000000000, 0.000000000000000000, 1.000000000000000000 ) ) ;
#39668=EDGE_LOOP ( 'NONE', ( #26183, #28241, #46352, #44331, #47713 ) ) ;
#39671=EDGE_CURVE ( 'NONE', #37113, #36574, #18640, .T. ) ;
#39672=CARTESIAN_POINT ( 'NONE',  ( 47.13393739769619373, -38.26167638829240047, -54.64999999999999858 ) ) ;
#39681=VECTOR ( 'NONE', #3104, 1000.000000000000000 ) ;
#39688=EDGE_LOOP ( 'NONE', ( #13336, #5963, #7674, #41433 ) ) ;
#39702=DIRECTION ( 'NONE',  ( 0.000000000000000000, 0.000000000000000000, -1.000000000000000000 ) ) ;
#39703=VERTEX_POINT ( 'NONE', #10792 ) ;
#39704=ADVANCED_FACE ( 'NONE', ( #26752 ), #27018, .F. ) ;
#39706=EDGE_LOOP ( 'NONE', ( #35228, #17599, #48199, #31279, #42347, #51370, #47832, #29198 ) ) ;
#39716=PLANE ( 'NONE',  #41788 ) ;
#39718=DIRECTION ( 'NONE',  ( 0.9805806756909202226, 0.000000000000000000, -0.1961161351381840445 ) ) ;
#39726=CARTESIAN_POINT ( 'NONE',  ( 42.28005749516919565, -39.79447665039643312, -74.97844900094325737 ) ) ;
#39733=EDGE_CURVE ( 'NONE', #51582, #14157, #3920, .T. ) ;
#39740=( BOUNDED_CURVE ( )  B_SPLINE_CURVE ( 3, ( #37901, #26081, #42088, #29505 ),
 .UNSPECIFIED., .F., .T. ) 
 B_SPLINE_CURVE_WITH_KNOTS ( ( 4, 4 ),
 ( -9.769962616701377556E-15, 0.7853981633974057575 ),
 .UNSPECIFIED. ) 
 CURVE ( )  GEOMETRIC_REPRESENTATION_ITEM ( )  RATIONAL_B_SPLINE_CURVE ( ( 1.000000000000000000, 0.9492530216741954519, 0.9492530216741954519, 1.000000000000000000 ) ) 
 REPRESENTATION_ITEM ( '' )  );
#39742=VERTEX_POINT ( 'NONE', #48751 ) ;
#39747=CARTESIAN_POINT ( 'NONE',  ( 41.94533325028437076, 8.526340366768270229, -76.59527892131112026 ) ) ;
#39751=ORIENTED_EDGE ( 'NONE', *, *, #9284, .T. ) ;
#39752=CARTESIAN_POINT ( 'NONE',  ( 0.06588876110915349582, 19.86606076565430001, -34.93030904342190013 ) ) ;
#39760=ADVANCED_FACE ( 'NONE', ( #20175 ), #35911, .T. ) ;
#39761=CARTESIAN_POINT ( 'NONE',  ( -0.4123484725610440105, 14.05881538531380137, -35.12503119152799513 ) ) ;
#39762=DIRECTION ( 'NONE',  ( 0.000000000000000000, 0.000000000000000000, 1.000000000000000000 ) ) ;
#39764=AXIS2_PLACEMENT_3D ( 'NONE', #38183, #2277, #50497 ) ;
#39778=CARTESIAN_POINT ( 'NONE',  ( 3.633937397696210159, -8.399310579809009525, -34.64999999999999858 ) ) ;
#39781=DIRECTION ( 'NONE',  ( 0.000000000000000000, -1.000000000000000000, 0.000000000000000000 ) ) ;
#39783=CARTESIAN_POINT ( 'NONE',  ( 46.95755860539310333, -39.50979427423180113, -54.16316400158059707 ) ) ;
#39785=CONICAL_SURFACE ( 'NONE', #1296, 0.7350000000000003197, 0.06981317007977388966 ) ;
#39793=CARTESIAN_POINT ( 'NONE',  ( 43.34604152446959802, 4.883811055320659733, -58.29242082535468938 ) ) ;
#39794=CARTESIAN_POINT ( 'NONE',  ( 0.6045892726184427524, -8.790618991491967904, -34.79644291222913921 ) ) ;
#39803=CARTESIAN_POINT ( 'NONE',  ( 45.84105415622519786, 7.939782908946126483, -61.60406984308864509 ) ) ;
#39804=CARTESIAN_POINT ( 'NONE',  ( 14.28038400710293487, -41.76263555408612405, -34.79644660940672907 ) ) ;
#39810=DIRECTION ( 'NONE',  ( 0.000000000000000000, -1.000000000000000000, 0.000000000000000000 ) ) ;
#39821=CARTESIAN_POINT ( 'NONE',  ( 12.95491128060869990, -49.88685839599860117, -82.14319696191608955 ) ) ;
#39828=VERTEX_POINT ( 'NONE', #12858 ) ;
#39833=LINE ( 'NONE', #31424, #42184 ) ;
#39848=CARTESIAN_POINT ( 'NONE',  ( 11.63393739769600010, 10.38381105532060111, -35.14999999999999858 ) ) ;
#39859=CARTESIAN_POINT ( 'NONE',  ( 12.95491128060830022, 18.65448050664010182, -82.14319696191608955 ) ) ;
#39873=EDGE_CURVE ( 'NONE', #43147, #4357, #20050, .T. ) ;
#39877=CARTESIAN_POINT ( 'NONE',  ( -0.4410626023037830246, -8.356009309619699010, -35.14999999999999858 ) ) ;
#39884=CARTESIAN_POINT ( 'NONE',  ( 38.67452568954060155, -36.11618894467930119, -81.65000000000000568 ) ) ;
#39901=DIRECTION ( 'NONE',  ( -0.04040038076619560659, -0.02935259477425090566, 0.9987523388778446476 ) ) ;
#39904=CARTESIAN_POINT ( 'NONE',  ( 42.27050190383921802, 6.434495523153046292, -78.96717512227382940 ) ) ;
#39917=LINE ( 'NONE', #16059, #43481 ) ;
#39922=ORIENTED_EDGE ( 'NONE', *, *, #22346, .T. ) ;
#39927=CARTESIAN_POINT ( 'NONE',  ( 18.13393739769620083, -32.62399965035220362, -35.14999999999999858 ) ) ;
#39938=CARTESIAN_POINT ( 'NONE',  ( 0.1457839871805957643, 14.73018012514992137, -34.68167748489143776 ) ) ;
#39955=EDGE_CURVE ( 'NONE', #21076, #9565, #21465, .T. ) ;
#39961=EDGE_LOOP ( 'NONE', ( #24500, #42662, #42928, #47391, #32898, #12839, #6315 ) ) ;
#39965=EDGE_LOOP ( 'NONE', ( #8676, #46610 ) ) ;
#39966=CARTESIAN_POINT ( 'NONE',  ( 44.66893810599722059, 1.931900683508221306, -44.67038416013655677 ) ) ;
#39967=DIRECTION ( 'NONE',  ( 0.3535533905932736198, -0.6123724356957950254, 0.7071067811865472397 ) ) ;
#39969=VECTOR ( 'NONE', #29498, 1000.000000000000000 ) ;
#39976=CARTESIAN_POINT ( 'NONE',  ( 0.6045892726184849408, -22.44175889786657763, -34.79644291222908237 ) ) ;
#39985=CARTESIAN_POINT ( 'NONE',  ( 43.36319213471767853, -39.89965443588339156, -69.74287559708298545 ) ) ;
#39999=ORIENTED_EDGE ( 'NONE', *, *, #38516, .T. ) ;
#40000=DIRECTION ( 'NONE',  ( 0.5516667872527449834, -0.8340645993220396903, -3.885780586188043947E-16 ) ) ;
#40004=DIRECTION ( 'NONE',  ( -0.5877852522924744694, -0.8090169943749464521, 0.000000000000000000 ) ) ;
#40005=CARTESIAN_POINT ( 'NONE',  ( 42.20273094283171389, 8.553841343497502692, -75.35254198661807834 ) ) ;
#40006=CARTESIAN_POINT ( 'NONE',  ( 19.40270147970570136, 17.88381105532069881, -34.64999999999999858 ) ) ;
#40020=CARTESIAN_POINT ( 'NONE',  ( 1.058369240368480124, -8.644356418428410294, -34.64999999999999858 ) ) ;
#40021=DIRECTION ( 'NONE',  ( 1.000000000000000000, 0.000000000000000000, 0.000000000000000000 ) ) ;
#40026=EDGE_LOOP ( 'NONE', ( #28525, #47745, #10176, #25223 ) ) ;
#40030=DIRECTION ( 'NONE',  ( 0.000000000000000000, 0.000000000000000000, -1.000000000000000000 ) ) ;
#40032=ADVANCED_FACE ( 'NONE', ( #38502 ), #2603, .T. ) ;
#40036=EDGE_CURVE ( 'NONE', #33273, #13585, #6340, .T. ) ;
#40038=CARTESIAN_POINT ( 'NONE',  ( 8.942935310824500661, 18.10006093832389951, -34.64999999999999858 ) ) ;
#40040=AXIS2_PLACEMENT_3D ( 'NONE', #48670, #37383, #441 ) ;
#40043=EDGE_LOOP ( 'NONE', ( #39546, #4613, #20793, #30398, #4085 ) ) ;
#40047=DIRECTION ( 'NONE',  ( 0.000000000000000000, -1.000000000000000000, 0.000000000000000000 ) ) ;
#40051=EDGE_CURVE ( 'NONE', #4357, #23707, #35101, .T. ) ;
#40060=CARTESIAN_POINT ( 'NONE',  ( 44.67636077250357118, 7.841592789065577662, -67.36726970128053438 ) ) ;
#40068=PLANE ( 'NONE',  #29796 ) ;
#40069=ORIENTED_EDGE ( 'NONE', *, *, #32482, .F. ) ;
#40079=AXIS2_PLACEMENT_3D ( 'NONE', #41513, #1683, #6400 ) ;
#40090=VERTEX_POINT ( 'NONE', #27722 ) ;
#40091=DIRECTION ( 'NONE',  ( 1.000000000000000000, 0.000000000000000000, 0.000000000000000000 ) ) ;
#40099=ORIENTED_EDGE ( 'NONE', *, *, #18275, .F. ) ;
#40108=AXIS2_PLACEMENT_3D ( 'NONE', #34677, #30744, #2208 ) ;
#40113=DIRECTION ( 'NONE',  ( -0.3535533905932768950, -0.6123724356957934711, 0.7071067811865469066 ) ) ;
#40114=CARTESIAN_POINT ( 'NONE',  ( 40.59195266416351444, -39.62822065711511499, -83.00040738963430442 ) ) ;
#40141=ORIENTED_EDGE ( 'NONE', *, *, #40384, .T. ) ;
#40148=CIRCLE ( 'NONE', #38589, 5.461610137242767671 ) ;
#40149=VECTOR ( 'NONE', #20806, 1000.000000000000114 ) ;
#40151=CARTESIAN_POINT ( 'NONE',  ( -0.4123484725610440105, 14.05881538531380137, -35.12503119152799513 ) ) ;
#40171=VERTEX_POINT ( 'NONE', #30033 ) ;
#40182=CONICAL_SURFACE ( 'NONE', #1690, 3.567506086244480734, 0.04995839572194331335 ) ;
#40184=CARTESIAN_POINT ( 'NONE',  ( 17.18674513269237991, 18.38376737894684254, -83.21862149193310643 ) ) ;
#40201=DIRECTION ( 'NONE',  ( 0.000000000000000000, 0.000000000000000000, 1.000000000000000000 ) ) ;
#40205=EDGE_LOOP ( 'NONE', ( #12555, #38043, #31110, #23874 ) ) ;
#40211=VECTOR ( 'NONE', #18571, 1000.000000000000114 ) ;
#40212=CARTESIAN_POINT ( 'NONE',  ( -10.98165337464593350, -35.31681881277557977, -44.31573110638452562 ) ) ;
#40215=ORIENTED_EDGE ( 'NONE', *, *, #26416, .T. ) ;
#40217=ADVANCED_FACE ( 'NONE', ( #1247 ), #13061, .T. ) ;
#40220=ORIENTED_EDGE ( 'NONE', *, *, #46627, .F. ) ;
#40224=CARTESIAN_POINT ( 'NONE',  ( 0.3198662801700840053, -10.53391313386299899, -34.64999999999999858 ) ) ;
#40228=AXIS2_PLACEMENT_3D ( 'NONE', #40347, #40859, #4699 ) ;
#40241=EDGE_CURVE ( 'NONE', #50570, #40830, #10536, .T. ) ;
#40242=CARTESIAN_POINT ( 'NONE',  ( 42.58018652930225301, -39.82501111426791596, -73.52906714457603243 ) ) ;
#40246=DIRECTION ( 'NONE',  ( -1.000000000000000000, 0.000000000000000000, 0.000000000000000000 ) ) ;
#40247=CARTESIAN_POINT ( 'NONE',  ( 29.13393739769619728, 1.883811055320659955, -53.85091742636659973 ) ) ;
#40258=CARTESIAN_POINT ( 'NONE',  ( 28.63393739769619728, -26.55370255794280254, -34.64999999999999858 ) ) ;
#40259=CARTESIAN_POINT ( 'NONE',  ( 42.21716448694958501, 8.555370896169934625, -75.28279128881918325 ) ) ;
#40270=VERTEX_POINT ( 'NONE', #2275 ) ;
#40277=CARTESIAN_POINT ( 'NONE',  ( 0.3209249304026170480, -50.71887597443840434, -35.14999999999999858 ) ) ;
#40282=CARTESIAN_POINT ( 'NONE',  ( 43.34604152446959802, 4.883811055320659733, -58.29242082535468938 ) ) ;
#40283=EDGE_CURVE ( 'NONE', #1290, #38545, #37149, .T. ) ;
#40292=CARTESIAN_POINT ( 'NONE',  ( -22.80083709146214233, -13.57305611580116178, -54.72264480988580715 ) ) ;
#40307=CYLINDRICAL_SURFACE ( 'NONE', #8852, 0.4999999999999992784 ) ;
#40328=VERTEX_POINT ( 'NONE', #41331 ) ;
#40329=EDGE_CURVE ( 'NONE', #23421, #12905, #43840, .T. ) ;
#40332=CARTESIAN_POINT ( 'NONE',  ( 46.13393739769619373, 4.883811055320659733, -81.65000000000000568 ) ) ;
#40344=EDGE_LOOP ( 'NONE', ( #20854, #1640 ) ) ;
#40346=CARTESIAN_POINT ( 'NONE',  ( 10.12953414447999911, 22.90954413163299819, -35.04035092416999220 ) ) ;
#40347=CARTESIAN_POINT ( 'NONE',  ( 38.67452568954060155, -37.56081407618430035, -81.65000000000000568 ) ) ;
#40349=EDGE_CURVE ( 'NONE', #10379, #8545, #1324, .T. ) ;
#40356=CARTESIAN_POINT ( 'NONE',  ( 18.13393739769599833, 14.38381105532070059, -62.64999999999999858 ) ) ;
#40361=AXIS2_PLACEMENT_3D ( 'NONE', #44977, #48657, #16946 ) ;
#40362=CIRCLE ( 'NONE', #13630, 2.999999999999999112 ) ;
#40367=CARTESIAN_POINT ( 'NONE',  ( 43.57203457279818082, -40.01153835713891027, -68.34812681792193700 ) ) ;
#40371=ORIENTED_EDGE ( 'NONE', *, *, #46563, .F. ) ;
#40383=CARTESIAN_POINT ( 'NONE',  ( 20.63393739769620083, -41.61618894467930119, -35.14999999999999858 ) ) ;
#40384=EDGE_CURVE ( 'NONE', #34827, #45182, #12560, .T. ) ;
#40385=ORIENTED_EDGE ( 'NONE', *, *, #25195, .T. ) ;
#40395=CYLINDRICAL_SURFACE ( 'NONE', #15122, 0.4999999999999982236 ) ;
#40398=ORIENTED_EDGE ( 'NONE', *, *, #22678, .T. ) ;
#40399=PLANE ( 'NONE',  #7828 ) ;
#40402=DIRECTION ( 'NONE',  ( 0.6339889056055382222, 0.000000000000000000, -0.7733421413379021336 ) ) ;
#40405=EDGE_LOOP ( 'NONE', ( #10709, #2904, #18053, #36075, #33154 ) ) ;
#40407=CARTESIAN_POINT ( 'NONE',  ( 31.13393739769620083, -33.99486860111965569, -83.77132034355965118 ) ) ;
#40408=CARTESIAN_POINT ( 'NONE',  ( 42.31307469794116116, 6.441183479073752771, -78.75431333624337071 ) ) ;
#40412=CARTESIAN_POINT ( 'NONE',  ( -0.4410626023037830246, -8.356009309619699010, -35.14999999999999858 ) ) ;
#40413=CARTESIAN_POINT ( 'NONE',  ( 41.79059739480540259, -37.58975971051863496, -81.36666986503341548 ) ) ;
#40414=ADVANCED_FACE ( 'NONE', ( #14724 ), #32223, .T. ) ;
#40415=ORIENTED_EDGE ( 'NONE', *, *, #22572, .T. ) ;
#40440=DIRECTION ( 'NONE',  ( 0.000000000000000000, -1.000000000000000000, 0.000000000000000000 ) ) ;
#40445=ADVANCED_FACE ( 'NONE', ( #19675 ), #27795, .T. ) ;
#40451=CYLINDRICAL_SURFACE ( 'NONE', #23720, 0.4999999999999982236 ) ;
#40459=AXIS2_PLACEMENT_3D ( 'NONE', #19626, #12036, #15699 ) ;
#40460=ORIENTED_EDGE ( 'NONE', *, *, #48823, .T. ) ;
#40464=FACE_OUTER_BOUND ( 'NONE', #27259, .T. ) ;
#40472=DIRECTION ( 'NONE',  ( -0.05643417272666771678, 0.04100182651872444350, -0.9975640502598241977 ) ) ;
#40473=VERTEX_POINT ( 'NONE', #23586 ) ;
#40477=CONICAL_SURFACE ( 'NONE', #32897, 0.7350000000000003197, 0.06981317007977388966 ) ;
#40483=LINE ( 'NONE', #24988, #3698 ) ;
#40488=VECTOR ( 'NONE', #22624, 1000.000000000000114 ) ;
#40489=CARTESIAN_POINT ( 'NONE',  ( 23.48034592329200265, -49.03431820457670653, -34.71551406240359938 ) ) ;
#40492=CARTESIAN_POINT ( 'NONE',  ( 42.89310467332932575, -39.85583253097592404, -72.01652229824608753 ) ) ;
#40493=PLANE ( 'NONE',  #37368 ) ;
#40514=CARTESIAN_POINT ( 'NONE',  ( 41.50304611168537150, 8.476976521895192462, -78.72953053759411546 ) ) ;
#40517=DIRECTION ( 'NONE',  ( 0.000000000000000000, 0.7071067811865475727, 0.7071067811865475727 ) ) ;
#40520=ORIENTED_EDGE ( 'NONE', *, *, #13223, .T. ) ;
#40521=ORIENTED_EDGE ( 'NONE', *, *, #45729, .F. ) ;
#40531=CARTESIAN_POINT ( 'NONE',  ( -15.34479443485247074, 7.407496050971681179, -48.42068391671703154 ) ) ;
#40533=CIRCLE ( 'NONE', #20422, 22.00000000000000000 ) ;
#40544=CARTESIAN_POINT ( 'NONE',  ( -0.2865249686165656784, -3.826429500511919102, -35.01561944896762668 ) ) ;
#40561=CARTESIAN_POINT ( 'NONE',  ( -0.007164427059776000244, -20.74946784552680157, -34.77269723891829756 ) ) ;
#40569=EDGE_LOOP ( 'NONE', ( #1925, #6072, #47268, #32163 ) ) ;
#40577=EDGE_CURVE ( 'NONE', #6332, #34997, #11363, .T. ) ;
#40591=CARTESIAN_POINT ( 'NONE',  ( 46.25525774125586054, 2.762490711761019568, -54.56299356781535437 ) ) ;
#40603=VECTOR ( 'NONE', #15354, 1000.000000000000000 ) ;
#40608=ORIENTED_EDGE ( 'NONE', *, *, #28206, .F. ) ;
#40612=EDGE_CURVE ( 'NONE', #32835, #36176, #8658, .T. ) ;
#40615=ADVANCED_FACE ( 'NONE', ( #4991 ), #44045, .F. ) ;
#40617=CIRCLE ( 'NONE', #10479, 11.00000000000000000 ) ;
#40619=EDGE_CURVE ( 'NONE', #2348, #12279, #16360, .T. ) ;
#40623=CARTESIAN_POINT ( 'NONE',  ( 44.07452568954059302, -33.11618894467940066, -54.64999999999999858 ) ) ;
#40624=CARTESIAN_POINT ( 'NONE',  ( 41.48201311892960774, -39.75838402827952223, -78.61445045689941935 ) ) ;
#40632=AXIS2_PLACEMENT_3D ( 'NONE', #9112, #5698, #1504 ) ;
#40660=VERTEX_POINT ( 'NONE', #12596 ) ;
#40663=CARTESIAN_POINT ( 'NONE',  ( 40.57649240635721810, -36.11618894467930119, -83.97002642401369599 ) ) ;
#40671=CARTESIAN_POINT ( 'NONE',  ( 43.08604041149931874, -37.79059854641297989, -74.88947594510764816 ) ) ;
#40673=ORIENTED_EDGE ( 'NONE', *, *, #6143, .T. ) ;
#40677=CIRCLE ( 'NONE', #25617, 6.999999999999999112 ) ;
#40680=ADVANCED_FACE ( 'NONE', ( #8147 ), #10055, .T. ) ;
#40692=ORIENTED_EDGE ( 'NONE', *, *, #36989, .F. ) ;
#40695=VECTOR ( 'NONE', #15902, 1000.000000000000114 ) ;
#40698=DIRECTION ( 'NONE',  ( -0.8660254037844379305, 0.5000000000000011102, 0.000000000000000000 ) ) ;
#40713=ORIENTED_EDGE ( 'NONE', *, *, #23919, .T. ) ;
#40714=CARTESIAN_POINT ( 'NONE',  ( 44.13393739769620083, 4.883811055320659733, -35.14999999999999858 ) ) ;
#40717=AXIS2_PLACEMENT_3D ( 'NONE', #28628, #49101, #8734 ) ;
#40719=VERTEX_POINT ( 'NONE', #6806 ) ;
#40734=CARTESIAN_POINT ( 'NONE',  ( 3.987490788289483667, -19.08029055981709732, -34.79644660940672907 ) ) ;
#40735=CARTESIAN_POINT ( 'NONE',  ( 14.13393739769619906, -41.61618894467930119, -54.64999999999999858 ) ) ;
#40736=ORIENTED_EDGE ( 'NONE', *, *, #20877, .T. ) ;
#40745=DIRECTION ( 'NONE',  ( -0.8090169943749478954, -0.5877852522924724710, 0.000000000000000000 ) ) ;
#40750=CARTESIAN_POINT ( 'NONE',  ( 18.07449423817570278, 1.323206481297259929, -34.90839531524139971 ) ) ;
#40753=CARTESIAN_POINT ( 'NONE',  ( 41.18693779094563467, -39.67249569471185566, -80.25382149713556146 ) ) ;
#40771=CARTESIAN_POINT ( 'NONE',  ( 41.14613706618169431, 8.435299800057125097, -80.45036690760321108 ) ) ;
#40775=ORIENTED_EDGE ( 'NONE', *, *, #5103, .F. ) ;
#40781=DIRECTION ( 'NONE',  ( 1.000000000000000000, 0.000000000000000000, 0.000000000000000000 ) ) ;
#40788=CARTESIAN_POINT ( 'NONE',  ( -8.565972701125874167, 14.56525628855416166, -42.60118799329718797 ) ) ;
#40792=DIRECTION ( 'NONE',  ( -1.000000000000000000, 0.000000000000000000, 0.000000000000000000 ) ) ;
#40806=( BOUNDED_CURVE ( )  B_SPLINE_CURVE ( 3, ( #30766, #30509, #34962, #40383 ),
 .UNSPECIFIED., .F., .T. ) 
 B_SPLINE_CURVE_WITH_KNOTS ( ( 4, 4 ),
 ( 2.356194490192344837, 3.141592653589793116 ),
 .UNSPECIFIED. ) 
 CURVE ( )  GEOMETRIC_REPRESENTATION_ITEM ( )  RATIONAL_B_SPLINE_CURVE ( ( 1.000000000000000000, 0.9492530216741911220, 0.9492530216741911220, 1.000000000000000000 ) ) 
 REPRESENTATION_ITEM ( '' )  );
#40824=AXIS2_PLACEMENT_3D ( 'NONE', #48575, #24686, #36755 ) ;
#40828=ORIENTED_EDGE ( 'NONE', *, *, #470, .F. ) ;
#40830=VERTEX_POINT ( 'NONE', #49482 ) ;
#40848=ORIENTED_EDGE ( 'NONE', *, *, #51125, .F. ) ;
#40849=CARTESIAN_POINT ( 'NONE',  ( 0.7611760784153190906, -51.27432484048290462, -34.14606254259449258 ) ) ;
#40851=FACE_OUTER_BOUND ( 'NONE', #29356, .T. ) ;
#40857=CARTESIAN_POINT ( 'NONE',  ( 2.422196078461449797, -25.82482932757800143, -35.02873218748179340 ) ) ;
#40859=DIRECTION ( 'NONE',  ( 0.000000000000000000, 1.000000000000000000, 0.000000000000000000 ) ) ;
#40864=CARTESIAN_POINT ( 'NONE',  ( 0.3209249304026040028, 15.01904124785189865, -34.64999999999999858 ) ) ;
#40868=CARTESIAN_POINT ( 'NONE',  ( 38.67452568954060155, -36.11618894467930119, -84.65000000000000568 ) ) ;
#40870=ADVANCED_FACE ( 'NONE', ( #46319 ), #9886, .T. ) ;
#40879=CARTESIAN_POINT ( 'NONE',  ( 28.71032976354209865, -4.650001368963800452, -34.65450330891889763 ) ) ;
#40880=CARTESIAN_POINT ( 'NONE',  ( 19.13393739769620083, -49.61618894467939356, -83.01107220193038927 ) ) ;
#40882=CARTESIAN_POINT ( 'NONE',  ( 30.38062185377579638, -35.62460461499323827, -84.60948432506590677 ) ) ;
#40885=EDGE_CURVE ( 'NONE', #50266, #9028, #10151, .T. ) ;
#40891=CARTESIAN_POINT ( 'NONE',  ( 16.13393739769620083, -29.64169738395614218, -34.79644660940672907 ) ) ;
#40894=AXIS2_PLACEMENT_3D ( 'NONE', #4487, #44322, #48518 ) ;
#40902=ORIENTED_EDGE ( 'NONE', *, *, #43882, .T. ) ;
#40922=LINE ( 'NONE', #12370, #12771 ) ;
#40925=CARTESIAN_POINT ( 'NONE',  ( 42.34723858680553832, 6.446719989108320448, -78.58349325317209377 ) ) ;
#40929=CARTESIAN_POINT ( 'NONE',  ( 42.59156136795025560, -37.71660974778794895, -77.36181849303467573 ) ) ;
#40936=AXIS2_PLACEMENT_3D ( 'NONE', #213, #48171, #43727 ) ;
#40946=DIRECTION ( 'NONE',  ( -1.000000000000000000, 0.000000000000000000, 0.000000000000000000 ) ) ;
#40950=VERTEX_POINT ( 'NONE', #6999 ) ;
#40957=CARTESIAN_POINT ( 'NONE',  ( 14.13393739769619906, -32.62399965035220362, -35.14999999999999858 ) ) ;
#40967=DIRECTION ( 'NONE',  ( -1.000000000000000000, 0.000000000000000000, 0.000000000000000000 ) ) ;
#40969=FACE_OUTER_BOUND ( 'NONE', #1039, .T. ) ;
#40971=EDGE_CURVE ( 'NONE', #16597, #13585, #25576, .T. ) ;
#40975=VERTEX_POINT ( 'NONE', #11703 ) ;
#40980=CIRCLE ( 'NONE', #15025, 33.00000000000000000 ) ;
#40987=LINE ( 'NONE', #13990, #14224 ) ;
#40991=ORIENTED_EDGE ( 'NONE', *, *, #19032, .T. ) ;
#40994=CARTESIAN_POINT ( 'NONE',  ( 14.13393739769619906, -32.62399965035220362, -35.14999999999999858 ) ) ;
#40996=ORIENTED_EDGE ( 'NONE', *, *, #16744, .T. ) ;
#40997=CARTESIAN_POINT ( 'NONE',  ( 9.894687805641289913, 22.37488585622680048, -34.64999999999999858 ) ) ;
#41005=VECTOR ( 'NONE', #49516, 1000.000000000000000 ) ;
#41006=AXIS2_PLACEMENT_3D ( 'NONE', #49689, #25288, #17196 ) ;
#41012=ORIENTED_EDGE ( 'NONE', *, *, #20030, .F. ) ;
#41021=CARTESIAN_POINT ( 'NONE',  ( 14.30191975431818818, -32.45848243737157901, -34.77490583097449672 ) ) ;
#41022=DIRECTION ( 'NONE',  ( 0.000000000000000000, 1.000000000000000000, 0.000000000000000000 ) ) ;
#41023=ORIENTED_EDGE ( 'NONE', *, *, #28206, .T. ) ;
#41031=CARTESIAN_POINT ( 'NONE',  ( 45.04234838772278948, 8.801119246186837941, -61.60717924809139845 ) ) ;
#41033=DIRECTION ( 'NONE',  ( -0.8660254037844387076, 0.4999999999999998890, 0.000000000000000000 ) ) ;
#41046=DIRECTION ( 'NONE',  ( -0.9304380493636928984, 0.3664492274467039401, 0.000000000000000000 ) ) ;
#41049=ORIENTED_EDGE ( 'NONE', *, *, #10779, .T. ) ;
#41050=CIRCLE ( 'NONE', #4235, 5.251829701412241924 ) ;
#41051=VECTOR ( 'NONE', #28139, 999.9999999999998863 ) ;
#41055=CARTESIAN_POINT ( 'NONE',  ( 29.13393739769619728, 1.883811055320659955, -81.65000000000000568 ) ) ;
#41060=DIRECTION ( 'NONE',  ( 0.000000000000000000, 0.000000000000000000, 1.000000000000000000 ) ) ;
#41062=FACE_OUTER_BOUND ( 'NONE', #9033, .T. ) ;
#41067=CARTESIAN_POINT ( 'NONE',  ( -10.56362341667716187, -35.01310227033097533, -54.64999999999999858 ) ) ;
#41068=EDGE_CURVE ( 'NONE', #27066, #51151, #11962, .T. ) ;
#41091=ORIENTED_EDGE ( 'NONE', *, *, #34292, .F. ) ;
#41100=CARTESIAN_POINT ( 'NONE',  ( 12.86517331568640010, -49.11618894467930829, -34.64999999999999858 ) ) ;
#41101=CARTESIAN_POINT ( 'NONE',  ( 16.13393739769639623, 7.383811055320659733, -84.65000000000000568 ) ) ;
#41117=CARTESIAN_POINT ( 'NONE',  ( 22.35126475695570036, -53.65744759104629935, -34.65028073423250277 ) ) ;
#41135=CARTESIAN_POINT ( 'NONE',  ( -0.007164427059776000244, -22.82436266295209748, -34.77269723891829756 ) ) ;
#41138=DIRECTION ( 'NONE',  ( 1.000000000000000000, 0.000000000000000000, 0.000000000000000000 ) ) ;
#41140=CARTESIAN_POINT ( 'NONE',  ( 30.13393739769619728, -38.61618894467930119, -59.64999999999999147 ) ) ;
#41143=DIRECTION ( 'NONE',  ( 0.9083627212242632032, 0.3704194192529746688, -0.1940789028471167077 ) ) ;
#41164=EDGE_CURVE ( 'NONE', #29628, #6450, #51569, .T. ) ;
#41172=CARTESIAN_POINT ( 'NONE',  ( 2.470463535281269607, -25.59369663964760377, -34.75586992539665232 ) ) ;
#41192=CARTESIAN_POINT ( 'NONE',  ( 35.88493617910660305, 12.02948893129472019, -35.12503119152809461 ) ) ;
#41193=CARTESIAN_POINT ( 'NONE',  ( 41.91508555065757946, -37.61000887859182029, -80.74419515902299338 ) ) ;
#41195=EDGE_LOOP ( 'NONE', ( #19363, #41405, #324, #45111, #48075, #45297 ) ) ;
#41215=CARTESIAN_POINT ( 'NONE',  ( 22.13834065091180037, 22.90954413163309766, -35.04035092416999220 ) ) ;
#41219=CARTESIAN_POINT ( 'NONE',  ( 38.67452568954060155, -37.56081407618430035, -81.65000000000000568 ) ) ;
#41220=DIRECTION ( 'NONE',  ( 0.6339889056055382222, 0.000000000000000000, -0.7733421413379021336 ) ) ;
#41221=DIRECTION ( 'NONE',  ( -1.000000000000000000, 0.000000000000000000, 0.000000000000000000 ) ) ;
#41238=VERTEX_POINT ( 'NONE', #22120 ) ;
#41239=CARTESIAN_POINT ( 'NONE',  ( 16.13393739769620083, -15.61618894467929941, -34.64999999999999858 ) ) ;
#41240=ORIENTED_EDGE ( 'NONE', *, *, #43172, .F. ) ;
#41244=CARTESIAN_POINT ( 'NONE',  ( 44.13393739769620083, 1.883811055320659955, -54.35294145922169662 ) ) ;
#41247=ORIENTED_EDGE ( 'NONE', *, *, #31602, .F. ) ;
#41249=ORIENTED_EDGE ( 'NONE', *, *, #16219, .F. ) ;
#41255=LINE ( 'NONE', #5366, #29991 ) ;
#41263=LINE ( 'NONE', #44677, #50563 ) ;
#41271=CARTESIAN_POINT ( 'NONE',  ( 46.25525774125583922, -33.99486860111965569, -54.56299356781535437 ) ) ;
#41281=SPHERICAL_SURFACE ( 'NONE', #33169, 3.000000000000000000 ) ;
#41290=CARTESIAN_POINT ( 'NONE',  ( 43.26733082018852627, 8.658673373363992454, -70.20620505724502891 ) ) ;
#41297=EDGE_LOOP ( 'NONE', ( #51249, #11971, #20018, #35106 ) ) ;
#41308=CARTESIAN_POINT ( 'NONE',  ( -3.040980549493681906, 18.38569933621215924, -37.85816068168108472 ) ) ;
#41331=CARTESIAN_POINT ( 'NONE',  ( 0.1457840918200039859, -10.50670027737364620, -34.68167776469301344 ) ) ;
#41333=CARTESIAN_POINT ( 'NONE',  ( 16.13393739769620083, -15.61618894467929941, -54.64999999999999858 ) ) ;
#41344=CARTESIAN_POINT ( 'NONE',  ( 2.557755973795389881, -6.043492780141719756, -34.65000333055159842 ) ) ;
#41364=CARTESIAN_POINT ( 'NONE',  ( -22.86606125915950116, -13.70232240041790028, -54.87897021767069106 ) ) ;
#41365=DIRECTION ( 'NONE',  ( -0.9876883405951387696, -0.1564344650402249015, 0.000000000000000000 ) ) ;
#41371=CARTESIAN_POINT ( 'NONE',  ( 22.21935039506121257, -53.95817006707829933, -34.76477869314940961 ) ) ;
#41382=ORIENTED_EDGE ( 'NONE', *, *, #45017, .T. ) ;
#41387=DIRECTION ( 'NONE',  ( -0.3535533905932731202, -0.6123724356957964687, 0.7071067811865462405 ) ) ;
#41393=CARTESIAN_POINT ( 'NONE',  ( 28.81656660489900190, -4.610261985355189829, -34.68308842254609914 ) ) ;
#41398=CARTESIAN_POINT ( 'NONE',  ( 47.18760304122697136, -39.34341269553539178, -54.66681054946693052 ) ) ;
#41405=ORIENTED_EDGE ( 'NONE', *, *, #18614, .T. ) ;
#41429=ORIENTED_EDGE ( 'NONE', *, *, #14057, .T. ) ;
#41430=AXIS2_PLACEMENT_3D ( 'NONE', #23499, #51827, #15927 ) ;
#41433=ORIENTED_EDGE ( 'NONE', *, *, #21013, .T. ) ;
#41434=LINE ( 'NONE', #21507, #7467 ) ;
#41436=CARTESIAN_POINT ( 'NONE',  ( 10.13393739769619906, -54.15188668067469990, -35.14999999999999858 ) ) ;
#41445=CARTESIAN_POINT ( 'NONE',  ( 43.99195235186844144, -37.91623234883149962, -70.35986276463864897 ) ) ;
#41446=VERTEX_POINT ( 'NONE', #47419 ) ;
#41459=VERTEX_POINT ( 'NONE', #7064 ) ;
#41471=CARTESIAN_POINT ( 'NONE',  ( 46.63393739769619373, 4.883811055320659733, -34.64999999999999858 ) ) ;
#41475=DIRECTION ( 'NONE',  ( 0.000000000000000000, 1.000000000000000000, 0.000000000000000000 ) ) ;
#41478=VECTOR ( 'NONE', #23445, 1000.000000000000000 ) ;
#41482=EDGE_CURVE ( 'NONE', #37056, #18491, #7208, .T. ) ;
#41489=CARTESIAN_POINT ( 'NONE',  ( 28.49955684666385025, -22.75548266223732341, -34.64999999999999858 ) ) ;
#41491=CONICAL_SURFACE ( 'NONE', #49072, 0.7349999999999987654, 0.06981317007977388966 ) ;
#41512=ORIENTED_EDGE ( 'NONE', *, *, #1285, .F. ) ;
#41513=CARTESIAN_POINT ( 'NONE',  ( 19.61497263573680172, -40.47764751925419802, -35.14999999999999858 ) ) ;
#41518=FACE_OUTER_BOUND ( 'NONE', #51601, .T. ) ;
#41521=EDGE_CURVE ( 'NONE', #8545, #11667, #8063, .T. ) ;
#41542=VERTEX_POINT ( 'NONE', #31645 ) ;
#41547=CARTESIAN_POINT ( 'NONE',  ( 44.56598291179225413, 8.767012424567191431, -63.91637373492464747 ) ) ;
#41550=DIRECTION ( 'NONE',  ( 0.000000000000000000, 0.000000000000000000, 1.000000000000000000 ) ) ;
#41551=ORIENTED_EDGE ( 'NONE', *, *, #23928, .T. ) ;
#41552=EDGE_LOOP ( 'NONE', ( #24311, #36102, #49768, #17209 ) ) ;
#41560=EDGE_CURVE ( 'NONE', #34524, #31052, #9186, .T. ) ;
#41567=DIRECTION ( 'NONE',  ( 0.000000000000000000, 0.000000000000000000, -1.000000000000000000 ) ) ;
#41575=CARTESIAN_POINT ( 'NONE',  ( 14.13393739769640156, 10.38381105532060111, -35.14999999999999858 ) ) ;
#41591=CIRCLE ( 'NONE', #23978, 33.97624844042359626 ) ;
#41602=AXIS2_PLACEMENT_3D ( 'NONE', #6185, #13279, #25553 ) ;
#41610=CARTESIAN_POINT ( 'NONE',  ( 8.643872352929088620, -48.75656286698969666, -35.12503119152809461 ) ) ;
#41611=ORIENTED_EDGE ( 'NONE', *, *, #44817, .F. ) ;
#41612=ORIENTED_EDGE ( 'NONE', *, *, #50472, .F. ) ;
#41616=DIRECTION ( 'NONE',  ( 1.000000000000000000, 0.000000000000000000, 0.000000000000000000 ) ) ;
#41618=ORIENTED_EDGE ( 'NONE', *, *, #32140, .F. ) ;
#41619=CARTESIAN_POINT ( 'NONE',  ( -20.84783344275790284, -28.76004404052860153, -53.00251837860739101 ) ) ;
#41620=DIRECTION ( 'NONE',  ( 0.000000000000000000, 0.000000000000000000, -1.000000000000000000 ) ) ;
#41639=ORIENTED_EDGE ( 'NONE', *, *, #25277, .T. ) ;
#41651=CARTESIAN_POINT ( 'NONE',  ( 16.13393739769620083, -1.759782484128330049, -47.64999999999999858 ) ) ;
#41655=CARTESIAN_POINT ( 'NONE',  ( 28.93686911782399918, -4.565436177846480703, -34.75221567031820058 ) ) ;
#41656=CARTESIAN_POINT ( 'NONE',  ( 17.67958691229047119, -49.61617040957372637, -83.18681078537983353 ) ) ;
#41657=CARTESIAN_POINT ( 'NONE',  ( 0.3209249304026170480, -20.69829881652800196, -34.64999999999999858 ) ) ;
#41659=CARTESIAN_POINT ( 'NONE',  ( 42.32061802937450068, -37.64775053028490248, -78.71596476449020940 ) ) ;
#41665=EDGE_LOOP ( 'NONE', ( #41975, #21815, #16543, #16220, #25247, #30596, #25455 ) ) ;
#41670=CARTESIAN_POINT ( 'NONE',  ( 28.96098294488680125, -26.67590919638950098, -34.77057949856859409 ) ) ;
#41683=DIRECTION ( 'NONE',  ( 0.000000000000000000, 1.000000000000000000, 0.000000000000000000 ) ) ;
#41693=DIRECTION ( 'NONE',  ( 0.5112408204145798551, -0.8594375041513067082, 0.000000000000000000 ) ) ;
#41703=CARTESIAN_POINT ( 'NONE',  ( 43.66604041426285931, -37.87226800533215254, -71.98948473448078289 ) ) ;
#41711=ADVANCED_FACE ( 'NONE', ( #48699 ), #8923, .F. ) ;
#41720=ORIENTED_EDGE ( 'NONE', *, *, #41560, .T. ) ;
#41729=( BOUNDED_CURVE ( )  B_SPLINE_CURVE ( 3, ( #51034, #31093, #23226, #47623 ),
 .UNSPECIFIED., .F., .T. ) 
 B_SPLINE_CURVE_WITH_KNOTS ( ( 4, 4 ),
 ( 4.712388980384688786, 5.070260775219134430 ),
 .UNSPECIFIED. ) 
 CURVE ( )  GEOMETRIC_REPRESENTATION_ITEM ( )  RATIONAL_B_SPLINE_CURVE ( ( 1.000000000000000000, 0.9893557610490355536, 0.9893557610490355536, 1.000000000000000000 ) ) 
 REPRESENTATION_ITEM ( '' )  );
#41745=EDGE_LOOP ( 'NONE', ( #29500, #9360, #222, #22508 ) ) ;
#41748=CARTESIAN_POINT ( 'NONE',  ( 45.14832757675640096, 2.060512883921409966, -35.14999999999999858 ) ) ;
#41752=ORIENTED_EDGE ( 'NONE', *, *, #27247, .F. ) ;
#41759=CARTESIAN_POINT ( 'NONE',  ( -0.1295185695944109927, -31.87964491196989414, -84.65000000000000568 ) ) ;
#41761=EDGE_LOOP ( 'NONE', ( #7161, #17279, #45602, #43937 ) ) ;
#41762=VECTOR ( 'NONE', #31053, 1000.000000000000114 ) ;
#41763=CARTESIAN_POINT ( 'NONE',  ( 46.87892044299400141, 7.006504445231336753, -55.92504309812742491 ) ) ;
#41770=CARTESIAN_POINT ( 'NONE',  ( 16.13393739769620083, -15.61618894467929941, -47.64999999999999858 ) ) ;
#41771=VERTEX_POINT ( 'NONE', #49222 ) ;
#41772=CARTESIAN_POINT ( 'NONE',  ( 29.13393739769619728, -35.78776181993320193, -84.63196841427449613 ) ) ;
#41788=AXIS2_PLACEMENT_3D ( 'NONE', #11170, #47840, #27137 ) ;
#41794=CARTESIAN_POINT ( 'NONE',  ( 9.995687254861159943, -53.83794553065769861, -34.69483829921999529 ) ) ;
#41797=CARTESIAN_POINT ( 'NONE',  ( 16.13393739769620083, -1.182432214938700099, -34.64999999999999858 ) ) ;
#41798=ORIENTED_EDGE ( 'NONE', *, *, #44852, .F. ) ;
#41801=ORIENTED_EDGE ( 'NONE', *, *, #46107, .T. ) ;
#41806=CARTESIAN_POINT ( 'NONE',  ( 44.69989113218067445, 8.776768675800711961, -63.26780307294824013 ) ) ;
#41813=ORIENTED_EDGE ( 'NONE', *, *, #28477, .F. ) ;
#41814=CARTESIAN_POINT ( 'NONE',  ( -22.75275928769006839, -18.47887437259823429, -54.69860443186151855 ) ) ;
#41819=EDGE_CURVE ( 'NONE', #16471, #1290, #991, .T. ) ;
#41822=ORIENTED_EDGE ( 'NONE', *, *, #23177, .T. ) ;
#41826=CARTESIAN_POINT ( 'NONE',  ( 3.633937397696210159, -22.83306730954970121, -34.64999999999999858 ) ) ;
#41828=VERTEX_POINT ( 'NONE', #5452 ) ;
#41837=VECTOR ( 'NONE', #51103, 1000.000000000000000 ) ;
#41849=CARTESIAN_POINT ( 'NONE',  ( 46.38959050561425812, -40.11466081036353160, -55.06739743959177247 ) ) ;
#41865=DIRECTION ( 'NONE',  ( 0.8340645993220398013, -0.5516667872527448724, 0.000000000000000000 ) ) ;
#41876=CARTESIAN_POINT ( 'NONE',  ( 8.653191590476110306, -48.77463972988229557, -35.01184033120630090 ) ) ;
#41878=ORIENTED_EDGE ( 'NONE', *, *, #21267, .F. ) ;
#41883=( BOUNDED_CURVE ( )  B_SPLINE_CURVE ( 3, ( #9852, #14042, #30003, #46025 ),
 .UNSPECIFIED., .F., .T. ) 
 B_SPLINE_CURVE_WITH_KNOTS ( ( 4, 4 ),
 ( 4.712388980384689674, 5.497787143782005614 ),
 .UNSPECIFIED. ) 
 CURVE ( )  GEOMETRIC_REPRESENTATION_ITEM ( )  RATIONAL_B_SPLINE_CURVE ( ( 1.000000000000000000, 0.9492530216742079974, 0.9492530216742079974, 1.000000000000000000 ) ) 
 REPRESENTATION_ITEM ( '' )  );
#41888=CARTESIAN_POINT ( 'NONE',  ( -22.36136842496640043, -21.42584896580819986, -54.21115099506850044 ) ) ;
#41910=VECTOR ( 'NONE', #9477, 1000.000000000000000 ) ;
#41924=CARTESIAN_POINT ( 'NONE',  ( -9.412135025327549087, 14.13484241487110005, -42.98138733652569954 ) ) ;
#41925=CARTESIAN_POINT ( 'NONE',  ( 14.14886614762370165, 1.362847559348080217, -35.02873218748179340 ) ) ;
#41926=CARTESIAN_POINT ( 'NONE',  ( 44.17224985740909915, -39.08504712336350195, -69.61925960810538072 ) ) ;
#41933=CARTESIAN_POINT ( 'NONE',  ( 46.37276178491875811, 9.011627554650393890, -54.63167819045965246 ) ) ;
#41957=ADVANCED_FACE ( 'NONE', ( #48832 ), #33073, .T. ) ;
#41963=PLANE ( 'NONE',  #35050 ) ;
#41974=CARTESIAN_POINT ( 'NONE',  ( 45.48467495382262626, -38.09807257052023743, -62.89625465325211451 ) ) ;
#41975=ORIENTED_EDGE ( 'NONE', *, *, #1070, .F. ) ;
#41989=EDGE_CURVE ( 'NONE', #9028, #16471, #12935, .T. ) ;
#41993=CARTESIAN_POINT ( 'NONE',  ( 41.24914385796110139, -39.67975193718725535, -79.95434115774115469 ) ) ;
#42013=CARTESIAN_POINT ( 'NONE',  ( 18.13393739769639978, 10.38381105532070059, -35.14999999999999858 ) ) ;
#42032=CARTESIAN_POINT ( 'NONE',  ( 46.44895917027370302, 6.966159365888272781, -58.07489105607155011 ) ) ;
#42042=CARTESIAN_POINT ( 'NONE',  ( 28.63393739769619728, -12.15208732954159920, -35.14999999999999858 ) ) ;
#42050=EDGE_CURVE ( 'NONE', #23386, #44397, #29467, .T. ) ;
#42052=FACE_OUTER_BOUND ( 'NONE', #43476, .T. ) ;
#42064=DIRECTION ( 'NONE',  ( 0.000000000000000000, 1.000000000000000000, 0.000000000000000000 ) ) ;
#42065=VERTEX_POINT ( 'NONE', #28368 ) ;
#42070=CARTESIAN_POINT ( 'NONE',  ( 40.79482532997379707, 8.392676044869128660, -82.14319696191608955 ) ) ;
#42073=CARTESIAN_POINT ( 'NONE',  ( 43.63607212596370033, 8.691589028069600431, -68.42176024395821798 ) ) ;
#42083=LINE ( 'NONE', #29233, #33254 ) ;
#42084=DIRECTION ( 'NONE',  ( 0.000000000000000000, -1.000000000000000000, 0.000000000000000000 ) ) ;
#42088=CARTESIAN_POINT ( 'NONE',  ( 28.18536260820836148, -8.658295355271512506, -34.89146800830130957 ) ) ;
#42089=DIRECTION ( 'NONE',  ( -1.000000000000000000, 0.000000000000000000, 0.000000000000000000 ) ) ;
#42092=CARTESIAN_POINT ( 'NONE',  ( 46.47536507427530239, 8.886826513564159313, -54.64999999999999858 ) ) ;
#42104=DIRECTION ( 'NONE',  ( 0.000000000000000000, 0.000000000000000000, -1.000000000000000000 ) ) ;
#42105=VERTEX_POINT ( 'NONE', #44894 ) ;
#42107=AXIS2_PLACEMENT_3D ( 'NONE', #43279, #51391, #15489 ) ;
#42111=EDGE_CURVE ( 'NONE', #35016, #12167, #8999, .T. ) ;
#42125=AXIS2_PLACEMENT_3D ( 'NONE', #34001, #10179, #34526 ) ;
#42128=DIRECTION ( 'NONE',  ( 0.7071067811865475727, 0.000000000000000000, 0.7071067811865475727 ) ) ;
#42139=CARTESIAN_POINT ( 'NONE',  ( 8.645706001916300565, -48.76012022032579551, -35.08633291502829366 ) ) ;
#42140=ORIENTED_EDGE ( 'NONE', *, *, #49523, .T. ) ;
#42148=EDGE_LOOP ( 'NONE', ( #23423, #5927, #15217 ) ) ;
#42149=CARTESIAN_POINT ( 'NONE',  ( -22.86617264519300008, -18.55609227334679900, -54.83108237264280405 ) ) ;
#42170=AXIS2_PLACEMENT_3D ( 'NONE', #45489, #25541, #1977 ) ;
#42184=VECTOR ( 'NONE', #43263, 1000.000000000000000 ) ;
#42185=CARTESIAN_POINT ( 'NONE',  ( -21.86809497655350043, -6.965125899114559260, -53.78175932259858882 ) ) ;
#42187=CARTESIAN_POINT ( 'NONE',  ( 47.36600735767230930, -39.35907597182351481, -53.77478896724066715 ) ) ;
#42189=DIRECTION ( 'NONE',  ( 1.000000000000000000, 0.000000000000000000, 0.000000000000000000 ) ) ;
#42192=( BOUNDED_CURVE ( )  B_SPLINE_CURVE ( 3, ( #14066, #30293, #10657, #30027 ),
 .UNSPECIFIED., .F., .T. ) 
 B_SPLINE_CURVE_WITH_KNOTS ( ( 4, 4 ),
 ( 2.356194490192073943, 3.141592653589802886 ),
 .UNSPECIFIED. ) 
 CURVE ( )  GEOMETRIC_REPRESENTATION_ITEM ( )  RATIONAL_B_SPLINE_CURVE ( ( 1.000000000000000000, 0.9492530216741552618, 0.9492530216741552618, 1.000000000000000000 ) ) 
 REPRESENTATION_ITEM ( '' )  );
#42195=CARTESIAN_POINT ( 'NONE',  ( 47.21631652332737872, 8.040122714078041355, -54.78327235947799068 ) ) ;
#42216=ORIENTED_EDGE ( 'NONE', *, *, #30093, .F. ) ;
#42229=EDGE_CURVE ( 'NONE', #33944, #14108, #36506, .T. ) ;
#42231=CARTESIAN_POINT ( 'NONE',  ( 44.86124405867887077, -38.02577711452058651, -66.01342731499525485 ) ) ;
#42239=CIRCLE ( 'NONE', #20476, 2.999999999999998668 ) ;
#42251=CARTESIAN_POINT ( 'NONE',  ( 42.22066838722344073, -39.78807865986343018, -75.26602574004256496 ) ) ;
#42273=DIRECTION ( 'NONE',  ( 0.7071067811865487940, 0.000000000000000000, 0.7071067811865462405 ) ) ;
#42276=EDGE_LOOP ( 'NONE', ( #36698, #49370, #5305, #39499, #9659 ) ) ;
#42278=ORIENTED_EDGE ( 'NONE', *, *, #22969, .T. ) ;
#42287=FACE_OUTER_BOUND ( 'NONE', #34228, .T. ) ;
#42291=CARTESIAN_POINT ( 'NONE',  ( 46.40541215375579043, 6.961926829937682193, -58.29262626224165444 ) ) ;
#42292=DIRECTION ( 'NONE',  ( 0.3863301728269249447, 0.9223605572461988089, -3.330669073875469621E-16 ) ) ;
#42298=DIRECTION ( 'NONE',  ( -1.000000000000000000, 0.000000000000000000, 0.000000000000000000 ) ) ;
#42305=CARTESIAN_POINT ( 'NONE',  ( 14.13393739769640156, 10.38381105532060111, -35.14999999999999858 ) ) ;
#42319=CARTESIAN_POINT ( 'NONE',  ( 13.13393739769600010, 18.38381105532060289, -83.01107220193038927 ) ) ;
#42324=CARTESIAN_POINT ( 'NONE',  ( 0.3209249304026170480, -8.218592747557250888, -34.64999999999999858 ) ) ;
#42334=DIRECTION ( 'NONE',  ( 1.000000000000000000, 0.000000000000000000, 0.000000000000000000 ) ) ;
#42337=CARTESIAN_POINT ( 'NONE',  ( 45.76530515845411884, 8.847626787123020975, -58.09878025211985886 ) ) ;
#42339=LINE ( 'NONE', #38926, #29284 ) ;
#42340=CARTESIAN_POINT ( 'NONE',  ( 10.13393739769630031, -54.15188668067469990, -35.09469305598949518 ) ) ;
#42342=EDGE_LOOP ( 'NONE', ( #32611, #12371, #46677, #34867 ) ) ;
#42345=CARTESIAN_POINT ( 'NONE',  ( -20.77565199683915154, -28.32022799467020491, -53.08356737070175058 ) ) ;
#42347=ORIENTED_EDGE ( 'NONE', *, *, #31196, .T. ) ;
#42352=VERTEX_POINT ( 'NONE', #45874 ) ;
#42365=CARTESIAN_POINT ( 'NONE',  ( 27.22499013618942598, -28.04647486959190417, -34.79644660940672907 ) ) ;
#42366=B_SPLINE_CURVE_WITH_KNOTS ( 'NONE', 3,
 ( #15679, #26947, #7051, #39783, #35593, #19085, #11239, #43461, #51836, #19855, #34807, #10983, #19346, #39022, #30865, #35845, #35061, #12012, #15935 ),
 .UNSPECIFIED., .F., .F.,
 ( 4, 3, 3, 3, 3, 3, 4 ),
 ( 0.000000000000000000, 0.04742532092110129938, 0.07033534312137200428, 0.1033624735406969974, 0.1094063869444049930, 0.1257965922736820064, 0.1407742777448500182 ),
 .UNSPECIFIED. ) ;
#42371=VECTOR ( 'NONE', #33234, 1000.000000000000000 ) ;
#42375=CARTESIAN_POINT ( 'NONE',  ( 46.13154385501714216, -40.10099849830307761, -56.32029921020890839 ) ) ;
#42389=DIRECTION ( 'NONE',  ( 0.000000000000000000, 1.000000000000000000, 0.000000000000000000 ) ) ;
#42410=ORIENTED_EDGE ( 'NONE', *, *, #1668, .T. ) ;
#42422=EDGE_CURVE ( 'NONE', #11667, #37038, #1436, .T. ) ;
#42438=DIRECTION ( 'NONE',  ( 1.000000000000000000, 0.000000000000000000, 0.000000000000000000 ) ) ;
#42445=CARTESIAN_POINT ( 'NONE',  ( 29.09106731080629871, -4.508242673544909707, -34.94555596725388824 ) ) ;
#42449=CARTESIAN_POINT ( 'NONE',  ( 0.3976851907049809842, 20.06812262159460047, -34.91005868551109614 ) ) ;
#42451=CARTESIAN_POINT ( 'NONE',  ( 45.32011839866689229, -39.20707424017311382, -63.91252006199604097 ) ) ;
#42454=ORIENTED_EDGE ( 'NONE', *, *, #30602, .F. ) ;
#42458=CARTESIAN_POINT ( 'NONE',  ( 46.39461793029816761, 9.013153168876611332, -54.52405409598588193 ) ) ;
#42474=CARTESIAN_POINT ( 'NONE',  ( 46.98749078828947034, -15.61618894467929941, -34.79644660940672907 ) ) ;
#42482=DIRECTION ( 'NONE',  ( -0.3502816565540492477, 0.000000000000000000, 0.9366444154970182678 ) ) ;
#42483=ORIENTED_EDGE ( 'NONE', *, *, #48750, .F. ) ;
#42491=CARTESIAN_POINT ( 'NONE',  ( 44.08684091409431005, 1.883811055320659511, -54.64999999999999858 ) ) ;
#42493=TOROIDAL_SURFACE ( 'NONE', #8174, 38.50000000000000000, 0.5000000000000000000 ) ;
#42495=EDGE_CURVE ( 'NONE', #677, #34827, #2870, .T. ) ;
#42498=CARTESIAN_POINT ( 'NONE',  ( 44.17290358208205703, -37.93974571477343716, -69.45512797184353815 ) ) ;
#42516=CARTESIAN_POINT ( 'NONE',  ( 41.23058856492793467, -39.67759845120787787, -80.04365382965534081 ) ) ;
#42522=EDGE_CURVE ( 'NONE', #37113, #27066, #39088, .T. ) ;
#42524=CARTESIAN_POINT ( 'NONE',  ( 2.404741263826640107, -5.380232784273969671, -35.14999999999999858 ) ) ;
#42532=AXIS2_PLACEMENT_3D ( 'NONE', #45155, #9269, #41221 ) ;
#42533=CARTESIAN_POINT ( 'NONE',  ( 17.63393739769620083, -32.58675169315650066, -35.14999999999999858 ) ) ;
#42539=CYLINDRICAL_SURFACE ( 'NONE', #10042, 0.4999999999999991118 ) ;
#42554=CARTESIAN_POINT ( 'NONE',  ( 45.09935103916460264, 6.822007087868398933, -64.82292987203024381 ) ) ;
#42559=B_SPLINE_CURVE_WITH_KNOTS ( 'NONE', 3,
 ( #12108, #28065, #44069, #8172, #17332, #20982, #29365, #41172, #24116, #9212 ),
 .UNSPECIFIED., .F., .F.,
 ( 4, 2, 2, 2, 4 ),
 ( -0.1857717838172110170, -0.1853436703576350209, -0.1652145016252450083, -0.1459149143060420040, -0.1350635247397186933 ),
 .UNSPECIFIED. ) ;
#42573=LINE ( 'NONE', #17933, #397 ) ;
#42579=CARTESIAN_POINT ( 'NONE',  ( 46.98749078828947034, -15.61618894467929941, -34.79644660940672907 ) ) ;
#42585=CARTESIAN_POINT ( 'NONE',  ( 10.06369629473941352, -53.99262654158863484, -34.79644414665150975 ) ) ;
#42592=ORIENTED_EDGE ( 'NONE', *, *, #1285, .T. ) ;
#42600=CARTESIAN_POINT ( 'NONE',  ( 45.40454100101857904, 8.825245881843775564, -59.84982165534362508 ) ) ;
#42605=ORIENTED_EDGE ( 'NONE', *, *, #20877, .F. ) ;
#42609=DIRECTION ( 'NONE',  ( 3.757729999999999984E-12, -1.000000000000000000, 1.557061999999999974E-12 ) ) ;
#42614=ORIENTED_EDGE ( 'NONE', *, *, #34935, .T. ) ;
#42626=AXIS2_PLACEMENT_3D ( 'NONE', #5118, #33384, #9040 ) ;
#42628=CARTESIAN_POINT ( 'NONE',  ( -13.73674066540299954, -0.6797460008306699386, -46.71145918530370267 ) ) ;
#42629=CIRCLE ( 'NONE', #50184, 2.999999999999999112 ) ;
#42632=ORIENTED_EDGE ( 'NONE', *, *, #37018, .F. ) ;
#42635=AXIS2_PLACEMENT_3D ( 'NONE', #27294, #22835, #38856 ) ;
#42636=UNCERTAINTY_MEASURE_WITH_UNIT (LENGTH_MEASURE( 1.000000000000000082E-05 ), #11360, 'distance_accuracy_value', 'NONE');
#42638=CARTESIAN_POINT ( 'NONE',  ( 45.77958804137001891, -40.08084910885633434, -58.02946520578011302 ) ) ;
#42644=EDGE_CURVE ( 'NONE', #12279, #45483, #30976, .T. ) ;
#42647=ORIENTED_EDGE ( 'NONE', *, *, #21655, .F. ) ;
#42649=VERTEX_POINT ( 'NONE', #34969 ) ;
#42652=DIRECTION ( 'NONE',  ( 1.130501000000000083E-17, -8.343543999999999066E-19, -1.000000000000000000 ) ) ;
#42654=CARTESIAN_POINT ( 'NONE',  ( 14.58123197128210080, 0.9736865341423419640, -34.65032322548069743 ) ) ;
#42656=CARTESIAN_POINT ( 'NONE',  ( -13.73674066540309902, -30.55263188852779876, -46.71145918530379504 ) ) ;
#42657=DIRECTION ( 'NONE',  ( -1.000000000000000000, 0.000000000000000000, 0.000000000000000000 ) ) ;
#42662=ORIENTED_EDGE ( 'NONE', *, *, #4402, .T. ) ;
#42664=AXIS2_PLACEMENT_3D ( 'NONE', #3903, #19869, #47926 ) ;
#42674=DIRECTION ( 'NONE',  ( -1.000000000000000000, 0.000000000000000000, 0.000000000000000000 ) ) ;
#42682=DIRECTION ( 'NONE',  ( 0.000000000000000000, 0.000000000000000000, 1.000000000000000000 ) ) ;
#42690=B_SPLINE_CURVE_WITH_KNOTS ( 'NONE', 3,
 ( #45053, #24071, #4184, #20160, #48213, #9156, #36151, #32193 ),
 .UNSPECIFIED., .F., .F.,
 ( 4, 2, 2, 4 ),
 ( -0.1350635247397783956, -0.1243669311589359894, -0.1075965482636560000, -0.1052074838081859948 ),
 .UNSPECIFIED. ) ;
#42718=CARTESIAN_POINT ( 'NONE',  ( 47.88935567426931073, 8.085927491590410909, -51.43431970325507763 ) ) ;
#42719=CARTESIAN_POINT ( 'NONE',  ( 40.57649240635721100, -15.61618894467929941, -83.97002642401369599 ) ) ;
#42739=VERTEX_POINT ( 'NONE', #26583 ) ;
#42741=ORIENTED_EDGE ( 'NONE', *, *, #19092, .T. ) ;
#42752=AXIS2_PLACEMENT_3D ( 'NONE', #50722, #22404, #47070 ) ;
#42754=CARTESIAN_POINT ( 'NONE',  ( 17.63499105033369929, -32.15889263939740772, -34.64999999999999858 ) ) ;
#42766=DIRECTION ( 'NONE',  ( 0.000000000000000000, 0.000000000000000000, 1.000000000000000000 ) ) ;
#42777=ORIENTED_EDGE ( 'NONE', *, *, #1104, .F. ) ;
#42779=EDGE_CURVE ( 'NONE', #6345, #6332, #24823, .T. ) ;
#42790=CARTESIAN_POINT ( 'NONE',  ( 46.63393739769619373, -36.11618894467930119, -35.14999999999999858 ) ) ;
#42794=LINE ( 'NONE', #19700, #33709 ) ;
#42795=DIRECTION ( 'NONE',  ( -0.8660254037844387076, -0.4999999999999998890, 1.110223024625155678E-16 ) ) ;
#42802=ORIENTED_EDGE ( 'NONE', *, *, #24642, .T. ) ;
#42804=DIRECTION ( 'NONE',  ( 0.000000000000000000, 0.000000000000000000, -1.000000000000000000 ) ) ;
#42812=DIRECTION ( 'NONE',  ( 0.1961161351381840723, -2.713878504639270283E-16, 0.9805806756909202226 ) ) ;
#42815=CARTESIAN_POINT ( 'NONE',  ( 44.79206433993918779, 6.785388388300961360, -66.35931098130210160 ) ) ;
#42824=( BOUNDED_CURVE ( )  B_SPLINE_CURVE ( 3, ( #41797, #49679, #13770, #38389 ),
 .UNSPECIFIED., .F., .T. ) 
 B_SPLINE_CURVE_WITH_KNOTS ( ( 4, 4 ),
 ( 1.570796326794896558, 2.356194490192377700 ),
 .UNSPECIFIED. ) 
 CURVE ( )  GEOMETRIC_REPRESENTATION_ITEM ( )  RATIONAL_B_SPLINE_CURVE ( ( 1.000000000000000000, 0.9492530216741870142, 0.9492530216741870142, 1.000000000000000000 ) ) 
 REPRESENTATION_ITEM ( '' )  );
#42832=DIRECTION ( 'NONE',  ( 0.000000000000000000, 0.000000000000000000, 1.000000000000000000 ) ) ;
#42839=FACE_OUTER_BOUND ( 'NONE', #30533, .T. ) ;
#42840=DIRECTION ( 'NONE',  ( -0.3535533905932768950, -0.6123724356957934711, 0.7071067811865469066 ) ) ;
#42857=ORIENTED_EDGE ( 'NONE', *, *, #26740, .F. ) ;
#42866=ORIENTED_EDGE ( 'NONE', *, *, #16186, .T. ) ;
#42873=ORIENTED_EDGE ( 'NONE', *, *, #1368, .T. ) ;
#42876=ORIENTED_EDGE ( 'NONE', *, *, #41989, .T. ) ;
#42887=CIRCLE ( 'NONE', #31958, 34.41780050634729804 ) ;
#42888=VECTOR ( 'NONE', #8677, 1000.000000000000114 ) ;
#42897=CARTESIAN_POINT ( 'NONE',  ( 45.11971453824414624, -40.03891821604290158, -61.23139901406670305 ) ) ;
#42915=CARTESIAN_POINT ( 'NONE',  ( 44.43741329154635622, -33.13124401929711382, -48.95770300930330166 ) ) ;
#42927=VECTOR ( 'NONE', #45836, 1000.000000000000000 ) ;
#42928=ORIENTED_EDGE ( 'NONE', *, *, #41482, .T. ) ;
#42932=CARTESIAN_POINT ( 'NONE',  ( -1.453061824043200501, -7.771731286528777538, -43.67210485546797827 ) ) ;
#42936=CARTESIAN_POINT ( 'NONE',  ( 16.13393739769620083, -15.61618894467929941, -44.64999999999999858 ) ) ;
#42954=ORIENTED_EDGE ( 'NONE', *, *, #1873, .T. ) ;
#42958=CARTESIAN_POINT ( 'NONE',  ( 23.61468320491609774, 17.54226184052379978, -35.01184033120630090 ) ) ;
#42960=CARTESIAN_POINT ( 'NONE',  ( -0.007164427059776000244, -10.48291004383190028, -34.77269723891829756 ) ) ;
#42967=CARTESIAN_POINT ( 'NONE',  ( 0.09557987621370379883, 19.93481762610629815, -35.07694834390559890 ) ) ;
#42977=CARTESIAN_POINT ( 'NONE',  ( 47.66931075806890306, 8.074467705775857596, -52.52531625216943922 ) ) ;
#42988=ORIENTED_EDGE ( 'NONE', *, *, #23964, .F. ) ;
#42992=DIRECTION ( 'NONE',  ( 0.000000000000000000, 0.000000000000000000, 1.000000000000000000 ) ) ;
#43010=FACE_OUTER_BOUND ( 'NONE', #49957, .T. ) ;
#43018=CARTESIAN_POINT ( 'NONE',  ( -22.71090128286022036, -12.19468477084010871, -54.67917393425321393 ) ) ;
#43021=LINE ( 'NONE', #39848, #9935 ) ;
#43022=CIRCLE ( 'NONE', #26273, 0.4934432871681592725 ) ;
#43034=ADVANCED_FACE ( 'NONE', ( #12823 ), #17266, .T. ) ;
#43035=CARTESIAN_POINT ( 'NONE',  ( 47.13393739769619373, -36.11618894467930119, -35.14999999999999858 ) ) ;
#43037=CARTESIAN_POINT ( 'NONE',  ( 23.36719009671439906, 16.90943255703749770, -48.24693239604849992 ) ) ;
#43045=CARTESIAN_POINT ( 'NONE',  ( 16.13393739769620083, -15.61618894467929941, -643.2998782751060389 ) ) ;
#43059=CONICAL_SURFACE ( 'NONE', #37207, 3.506677339277151084, 0.04995839572194331335 ) ;
#43065=DIRECTION ( 'NONE',  ( 0.7071067811865461294, -0.7071067811865490160, 0.000000000000000000 ) ) ;
#43068=CARTESIAN_POINT ( 'NONE',  ( -0.3016046179078940015, -20.31737465961040101, -35.02873218748179340 ) ) ;
#43069=CARTESIAN_POINT ( 'NONE',  ( 44.57438173209401810, 6.759042111859073110, -67.44773831433604983 ) ) ;
#43091=CIRCLE ( 'NONE', #30531, 38.50000000000001421 ) ;
#43097=CARTESIAN_POINT ( 'NONE',  ( 14.25914812751967098, 1.264432139860236060, -34.81767276520688625 ) ) ;
#43102=CARTESIAN_POINT ( 'NONE',  ( 0.6920486002283754434, -37.06681587484604279, -59.64999999999999147 ) ) ;
#43116=CARTESIAN_POINT ( 'NONE',  ( 46.09098740009942219, 8.866406348324682440, -56.51717585894476770 ) ) ;
#43122=EDGE_LOOP ( 'NONE', ( #49188, #46882, #10225, #25323 ) ) ;
#43124=ORIENTED_EDGE ( 'NONE', *, *, #203, .F. ) ;
#43127=( BOUNDED_CURVE ( )  B_SPLINE_CURVE ( 3, ( #36942, #17037, #32989, #41135 ),
 .UNSPECIFIED., .F., .T. ) 
 B_SPLINE_CURVE_WITH_KNOTS ( ( 4, 4 ),
 ( 5.070260775219124660, 5.428132570053652906 ),
 .UNSPECIFIED. ) 
 CURVE ( )  GEOMETRIC_REPRESENTATION_ITEM ( )  RATIONAL_B_SPLINE_CURVE ( ( 1.000000000000000000, 0.9893557610490306686, 0.9893557610490306686, 1.000000000000000000 ) ) 
 REPRESENTATION_ITEM ( '' )  );
#43128=DIRECTION ( 'NONE',  ( 0.8090169943749472292, -0.5877852522924734702, 0.000000000000000000 ) ) ;
#43129=ORIENTED_EDGE ( 'NONE', *, *, #39277, .T. ) ;
#43134=LINE ( 'NONE', #23178, #25121 ) ;
#43147=VERTEX_POINT ( 'NONE', #13339 ) ;
#43152=EDGE_CURVE ( 'NONE', #51582, #9877, #22200, .T. ) ;
#43153=CARTESIAN_POINT ( 'NONE',  ( 44.70959683697221720, -40.00980781633823113, -63.22093828018593342 ) ) ;
#43155=FILL_AREA_STYLE ('',( #35005 ) ) ;
#43159=AXIS2_PLACEMENT_3D ( 'NONE', #47542, #25586, #42840 ) ;
#43165=ORIENTED_EDGE ( 'NONE', *, *, #46807, .T. ) ;
#43172=EDGE_CURVE ( 'NONE', #9063, #11865, #51645, .T. ) ;
#43177=CARTESIAN_POINT ( 'NONE',  ( -0.03447620312152738231, -22.81072779144790275, -34.79644660940672907 ) ) ;
#43178=ADVANCED_FACE ( 'NONE', ( #14096 ), #1530, .T. ) ;
#43199=DIRECTION ( 'NONE',  ( -0.3502816565540492477, 0.000000000000000000, 0.9366444154970182678 ) ) ;
#43205=VECTOR ( 'NONE', #7198, 1000.000000000000114 ) ;
#43207=CARTESIAN_POINT ( 'NONE',  ( 14.13393739769619906, -37.52509124488599923, -54.64999999999999858 ) ) ;
#43216=CARTESIAN_POINT ( 'NONE',  ( 3.277530937145240131, -5.884138137110399569, -34.64999999999999858 ) ) ;
#43218=CARTESIAN_POINT ( 'NONE',  ( 22.21935039506094967, 22.72579217771971827, -34.76477869314942382 ) ) ;
#43220=CIRCLE ( 'NONE', #1356, 2.999999999999999112 ) ;
#43231=ORIENTED_EDGE ( 'NONE', *, *, #3266, .T. ) ;
#43232=CARTESIAN_POINT ( 'NONE',  ( 45.14469185402641926, 7.879481261360513855, -65.05625649667543087 ) ) ;
#43248=ADVANCED_FACE ( 'NONE', ( #2832 ), #7311, .T. ) ;
#43263=DIRECTION ( 'NONE',  ( 0.000000000000000000, 0.000000000000000000, 1.000000000000000000 ) ) ;
#43264=EDGE_LOOP ( 'NONE', ( #17052, #26791, #37181, #38390 ) ) ;
#43275=CARTESIAN_POINT ( 'NONE',  ( -22.73277434335082603, -12.47272083566619649, -54.68865740790490548 ) ) ;
#43277=AXIS2_PLACEMENT_3D ( 'NONE', #40332, #20144, #48719 ) ;
#43279=CARTESIAN_POINT ( 'NONE',  ( 16.13393739769620083, -15.61618894467929941, -35.14999999999999858 ) ) ;
#43290=CARTESIAN_POINT ( 'NONE',  ( 31.59596111684529518, -35.98598576688283401, -84.65000000000001990 ) ) ;
#43303=DIRECTION ( 'NONE',  ( 8.462868000000000073E-18, -1.066343000000000058E-17, 1.000000000000000000 ) ) ;
#43304=EDGE_CURVE ( 'NONE', #23386, #26529, #19320, .T. ) ;
#43321=CARTESIAN_POINT ( 'NONE',  ( 0.9261640637176550284, -8.686430247967809493, -34.65800258959620095 ) ) ;
#43323=VERTEX_POINT ( 'NONE', #3859 ) ;
#43325=CARTESIAN_POINT ( 'NONE',  ( 42.99776018868912075, 6.545124476837784755, -75.33088594088501111 ) ) ;
#43328=EDGE_CURVE ( 'NONE', #39742, #37859, #20742, .T. ) ;
#43337=FACE_OUTER_BOUND ( 'NONE', #4469, .T. ) ;
#43342=AXIS2_PLACEMENT_3D ( 'NONE', #32318, #20533, #8765 ) ;
#43351=CARTESIAN_POINT ( 'NONE',  ( 2.419685150592632006, -5.395387223103724317, -35.06583844469683697 ) ) ;
#43379=LINE ( 'NONE', #15074, #14330 ) ;
#43387=EDGE_CURVE ( 'NONE', #31052, #32053, #12359, .T. ) ;
#43389=ORIENTED_EDGE ( 'NONE', *, *, #25958, .T. ) ;
#43403=CARTESIAN_POINT ( 'NONE',  ( 44.78235668084641219, -40.01503934400871287, -62.86839404953338573 ) ) ;
#43415=VERTEX_POINT ( 'NONE', #38735 ) ;
#43417=( BOUNDED_CURVE ( )  B_SPLINE_CURVE ( 3, ( #47859, #32604, #28949, #16645 ),
 .UNSPECIFIED., .F., .T. ) 
 B_SPLINE_CURVE_WITH_KNOTS ( ( 4, 4 ),
 ( 3.141592653589793116, 3.487830450619280320 ),
 .UNSPECIFIED. ) 
 CURVE ( )  GEOMETRIC_REPRESENTATION_ITEM ( )  RATIONAL_B_SPLINE_CURVE ( ( 1.000000000000000000, 0.9900348743600094759, 0.9900348743600094759, 1.000000000000000000 ) ) 
 REPRESENTATION_ITEM ( '' )  );
#43419=ORIENTED_EDGE ( 'NONE', *, *, #38896, .T. ) ;
#43425=CARTESIAN_POINT ( 'NONE',  ( 14.63183004845009982, 0.9274771370715009233, -34.65000333055159842 ) ) ;
#43430=CARTESIAN_POINT ( 'NONE',  ( -0.4410626023037970689, -22.87636857973879856, -35.14999999999999858 ) ) ;
#43432=VERTEX_POINT ( 'NONE', #16948 ) ;
#43437=ORIENTED_EDGE ( 'NONE', *, *, #37388, .T. ) ;
#43438=ORIENTED_EDGE ( 'NONE', *, *, #49883, .T. ) ;
#43440=CARTESIAN_POINT ( 'NONE',  ( -21.26982224466123839, -4.540630827726737095, -53.50719499581953897 ) ) ;
#43461=CARTESIAN_POINT ( 'NONE',  ( 46.81105700171560358, -39.69772926811019431, -54.41163925913020449 ) ) ;
#43473=CARTESIAN_POINT ( 'NONE',  ( 47.13098424738270609, -38.11658957897590483, -54.64686075001500143 ) ) ;
#43476=EDGE_LOOP ( 'NONE', ( #6588, #19742, #14673, #23109, #3147 ) ) ;
#43481=VECTOR ( 'NONE', #11372, 1000.000000000000000 ) ;
#43482=CARTESIAN_POINT ( 'NONE',  ( 47.12305569550148476, 6.751649648232654677, -54.63870115556262874 ) ) ;
#43490=EDGE_CURVE ( 'NONE', #2299, #25155, #596, .T. ) ;
#43494=CIRCLE ( 'NONE', #11695, 5.251829701412229490 ) ;
#43496=ORIENTED_EDGE ( 'NONE', *, *, #41819, .F. ) ;
#43500=CARTESIAN_POINT ( 'NONE',  ( 19.13393739769600188, 18.38381105532069881, -35.14999999999999858 ) ) ;
#43503=EDGE_LOOP ( 'NONE', ( #39588, #31610, #8246, #33629 ) ) ;
#43504=CARTESIAN_POINT ( 'NONE',  ( 44.11147024075970080, -33.11640768660669920, -54.64999999999999858 ) ) ;
#43511=ORIENTED_EDGE ( 'NONE', *, *, #45336, .F. ) ;
#43515=DIRECTION ( 'NONE',  ( 0.3863301728269248891, -0.9223605572461988089, 0.000000000000000000 ) ) ;
#43519=CARTESIAN_POINT ( 'NONE',  ( 46.42406059160111198, -38.19600863765170828, -58.19938352928596714 ) ) ;
#43533=CARTESIAN_POINT ( 'NONE',  ( 18.14758755231450493, -4.788411538692897373, -34.79644660940672907 ) ) ;
#43535=CARTESIAN_POINT ( 'NONE',  ( 9.937051593247810288, 22.47179399159399793, -34.65604926186119172 ) ) ;
#43545=DIRECTION ( 'NONE',  ( 0.000000000000000000, 0.000000000000000000, -1.000000000000000000 ) ) ;
#43546=ORIENTED_EDGE ( 'NONE', *, *, #6084, .F. ) ;
#43555=EDGE_CURVE ( 'NONE', #50266, #38136, #45502, .T. ) ;
#43558=CARTESIAN_POINT ( 'NONE',  ( 16.13393739769620083, -15.61618894467919816, -82.14319696191608955 ) ) ;
#43559=VECTOR ( 'NONE', #46500, 1000.000000000000000 ) ;
#43565=CARTESIAN_POINT ( 'NONE',  ( 16.13393739769620083, -1.700401765863659209, -34.89146800830129536 ) ) ;
#43571=ORIENTED_EDGE ( 'NONE', *, *, #15221, .T. ) ;
#43579=CARTESIAN_POINT ( 'NONE',  ( 43.43225333442439506, 6.607470992752627836, -73.15836440129699270 ) ) ;
#43583=DIRECTION ( 'NONE',  ( 0.8660254037844379305, -0.5000000000000011102, 0.000000000000000000 ) ) ;
#43585=LINE ( 'NONE', #14511, #43559 ) ;
#43592=ADVANCED_FACE ( 'NONE', ( #13789 ), #10116, .T. ) ;
#43600=ORIENTED_EDGE ( 'NONE', *, *, #19045, .T. ) ;
#43607=EDGE_LOOP ( 'NONE', ( #25189, #1375, #6902, #26676 ) ) ;
#43615=ADVANCED_FACE ( 'NONE', ( #5673 ), #42493, .T. ) ;
#43616=CARTESIAN_POINT ( 'NONE',  ( 0.2602139982834061338, 14.91936600910487343, -34.65037388166341259 ) ) ;
#43618=CARTESIAN_POINT ( 'NONE',  ( -0.2133638169075534607, -20.52615564361606815, -34.95200341233793750 ) ) ;
#43621=EDGE_CURVE ( 'NONE', #11158, #12367, #41883, .T. ) ;
#43625=VERTEX_POINT ( 'NONE', #45762 ) ;
#43629=DIRECTION ( 'NONE',  ( 0.000000000000000000, 0.000000000000000000, 1.000000000000000000 ) ) ;
#43634=ORIENTED_EDGE ( 'NONE', *, *, #16093, .F. ) ;
#43637=CARTESIAN_POINT ( 'NONE',  ( -110.3642515470889975, -33.11618894529460277, -112.3286729284269967 ) ) ;
#43641=ORIENTED_EDGE ( 'NONE', *, *, #3144, .F. ) ;
#43644=ORIENTED_EDGE ( 'NONE', *, *, #16834, .F. ) ;
#43648=CARTESIAN_POINT ( 'NONE',  ( 44.66728565622769054, 1.931601751605777073, -44.70166766796090485 ) ) ;
#43651=EDGE_CURVE ( 'NONE', #46747, #17157, #42083, .T. ) ;
#43660=CARTESIAN_POINT ( 'NONE',  ( 44.31273514806447622, -39.97978406752861247, -65.14464952758170568 ) ) ;
#43677=CARTESIAN_POINT ( 'NONE',  ( 18.70688454841999970, -48.06418385137889970, -35.14999999999999858 ) ) ;
#43681=CARTESIAN_POINT ( 'NONE',  ( 41.49957317341533525, 8.476577171076462136, -78.74628940708531388 ) ) ;
#43684=CARTESIAN_POINT ( 'NONE',  ( 18.13393739769620083, -41.61618894467930119, -35.14999999999999858 ) ) ;
#43686=CARTESIAN_POINT ( 'NONE',  ( 0.1124364628814909922, 19.94096921249579779, -35.13980537375690005 ) ) ;
#43693=CARTESIAN_POINT ( 'NONE',  ( 19.31296351478360052, 18.65448050664020130, -82.14319696191608955 ) ) ;
#43700=ORIENTED_EDGE ( 'NONE', *, *, #6371, .T. ) ;
#43704=CARTESIAN_POINT ( 'NONE',  ( 1.058369240368409958, -22.58802147093010149, -34.64999999999999858 ) ) ;
#43719=ORIENTED_EDGE ( 'NONE', *, *, #1668, .F. ) ;
#43724=( BOUNDED_CURVE ( )  B_SPLINE_CURVE ( 3, ( #10452, #39259, #22734, #3107 ),
 .UNSPECIFIED., .F., .T. ) 
 B_SPLINE_CURVE_WITH_KNOTS ( ( 4, 4 ),
 ( 0.07448749837916979200, 0.3185623355031764192 ),
 .UNSPECIFIED. ) 
 CURVE ( )  GEOMETRIC_REPRESENTATION_ITEM ( )  RATIONAL_B_SPLINE_CURVE ( ( 1.000000000000000000, 0.9950417810258930240, 0.9950417810258930240, 1.000000000000000000 ) ) 
 REPRESENTATION_ITEM ( '' )  );
#43727=DIRECTION ( 'NONE',  ( -0.7071067811865475727, 0.000000000000000000, 0.7071067811865475727 ) ) ;
#43738=CARTESIAN_POINT ( 'NONE',  ( 43.29114022628257885, 7.693946413374631810, -74.22886101434919226 ) ) ;
#43740=CARTESIAN_POINT ( 'NONE',  ( 16.13393739769639623, 7.383811055320659733, -84.65000000000000568 ) ) ;
#43745=DIRECTION ( 'NONE',  ( 0.000000000000000000, 0.000000000000000000, -1.000000000000000000 ) ) ;
#43771=CARTESIAN_POINT ( 'NONE',  ( 46.75053292986431330, -38.22714621137214408, -56.56697207775517455 ) ) ;
#43772=ORIENTED_EDGE ( 'NONE', *, *, #22315, .T. ) ;
#43782=DIRECTION ( 'NONE',  ( -0.3863301728269312174, 0.9223605572461961444, 1.110223024625156294E-16 ) ) ;
#43783=DIRECTION ( 'NONE',  ( 0.000000000000000000, 1.000000000000000000, 0.000000000000000000 ) ) ;
#43791=DIRECTION ( 'NONE',  ( 0.7071067811865475727, 0.000000000000000000, 0.7071067811865475727 ) ) ;
#43797=VERTEX_POINT ( 'NONE', #24935 ) ;
#43805=CARTESIAN_POINT ( 'NONE',  ( 0.3209249304026170480, -4.754491132419490285, -34.64999999999999858 ) ) ;
#43806=DIRECTION ( 'NONE',  ( 1.000000000000000000, 0.000000000000000000, 0.000000000000000000 ) ) ;
#43808=CIRCLE ( 'NONE', #21192, 22.00000000000000000 ) ;
#43809=CARTESIAN_POINT ( 'NONE',  ( -11.39236625349550103, 2.585530954890270294, -54.64999999999999858 ) ) ;
#43816=CARTESIAN_POINT ( 'NONE',  ( -0.4123484725610440105, -45.29119327467250145, -35.12503119152799513 ) ) ;
#43824=DIRECTION ( 'NONE',  ( 0.000000000000000000, 0.000000000000000000, -1.000000000000000000 ) ) ;
#43826=EDGE_LOOP ( 'NONE', ( #18024, #25445, #6542, #16039, #45755 ) ) ;
#43831=CARTESIAN_POINT ( 'NONE',  ( 43.79971744381874998, 6.658519618423869524, -71.32108293267019405 ) ) ;
#43840=B_SPLINE_CURVE_WITH_KNOTS ( 'NONE', 3,
 ( #5445, #21402, #41849, #37403, #45791, #9880, #5953, #21911, #14326, #23451, #42375, #30809, #26621, #51010, #34743, #51270, #47347, #11445, #26888, #35271, #19290, #42638, #14586, #27402, #39476, #6472, #50751, #46576, #15368, #35002, #6735, #19026, #22690, #15107, #38709, #14846, #50495, #50239, #2800, #7503, #23195, #31067, #42897, #47094, #18250, #11182, #3312, #39211, #38963, #27148, #46837, #30552, #31322, #10665, #3056, #43403, #30297, #46315, #18771, #34219, #43153, #6992, #10405, #26357, #10923, #7247, #22428, #38438, #2537, #22945, #18516, #34492, #43660, #31834, #16126, #32602, #28165, #23713, #43915, #12728, #20301, #23965, #4333, #51524, #32343, #19803, #35537, #4585, #48362, #27659, #15625, #32087, #35793, #401, #8790, #20556, #3576, #12206, #39985, #8010, #48107, #51776, #44170, #16640, #48628, #657, #20049, #28684, #12458, #44686, #44430, #4077, #36291, #8535, #36553, #40492, #8264, #24743, #36040, #16387, #148, #7765, #24217, #11957, #28427, #40242, #19544, #31577, #47597, #24479, #11697, #39726, #3830, #15880, #47851, #27914, #36817, #22566, #22047, #42251, #10281, #13950, #6350, #45927, #22308, #10017, #38060, #21794, #20820, #25979, #30694, #46456, #33845, #922, #13697, #30431, #10544, #10801, #26243, #46716, #4854, #2155, #1897, #26500, #49861, #38316, #18649, #16916, #32861, #41993, #42516, #34361, #40753, #38582, #50378, #50627, #2676, #48894, #30177 ),
 .UNSPECIFIED., .F., .F.,
 ( 4, 2, 2, 2, 1, 1, 2, 2, 2, 2, 1, 2, 2, 2, 2, 2, 2, 2, 1, 1, 2, 2, 2, 2, 1, 2, 1, 2, 2, 2, 2, 2, 1, 2, 2, 2, 2, 1, 2, 2, 2, 2, 2, 2, 1, 2, 2, 2, 2, 1, 1, 2, 2, 2, 2, 2, 1, 2, 2, 2, 2, 1, 2, 2, 2, 2, 2, 2, 1, 1, 2, 2, 2, 2, 1, 2, 2, 2, 2, 2, 2, 2, 1, 1, 2, 2, 2, 2, 1, 2, 2, 2, 2, 2, 2, 2, 1, 2, 2, 4 ),
 ( 0.000000000000000000, 0.03124999999998254174, 0.04687499999997373629, 0.05468749999996957295, 0.05859374999996754679, 0.06054687499996654065, 0.06152343749996577044, 0.06249999999996499328, 0.09374999999994663991, 0.1093749999999377581, 0.1171874999999337197, 0.1210937499999317768, 0.1230468749999313466, 0.1240234374999307637, 0.1249999999999301947, 0.1562499999999337474, 0.1718749999999354960, 0.1796874999999364675, 0.1835937499999372446, 0.1855468749999378275, 0.1865234374999381883, 0.1874999999999385214, 0.2187499999999658606, 0.2343749999999794609, 0.2421874999999861777, 0.2460937499999892031, 0.2480468749999906741, 0.2490234374999909794, 0.2499999999999912847, 0.2812499999999738542, 0.2968749999999648059, 0.3046874999999603650, 0.3085937499999580891, 0.3105468749999574785, 0.3124999999999568123, 0.3437499999999511502, 0.3593749999999475975, 0.3671874999999458766, 0.3710937499999448774, 0.3730468749999434896, 0.3749999999999420464, 0.4062499999999429345, 0.4218749999999433786, 0.4296874999999437117, 0.4335937499999432676, 0.4355468749999431011, 0.4374999999999428790, 0.4687499999999381051, 0.4843749999999358291, 0.4921874999999355516, 0.4960937499999345524, 0.4980468749999351630, 0.4999999999999357181, 0.5312499999999212852, 0.5468749999999139577, 0.5546874999999096278, 0.5585937499999079625, 0.5605468749999077405, 0.5624999999999075184, 0.5937499999999158451, 0.6093749999999200639, 0.6171874999999220623, 0.6210937499999231726, 0.6230468749999237277, 0.6249999999999242828, 0.6562499999999480416, 0.6718749999999598099, 0.6796874999999658051, 0.6835937499999686917, 0.6855468749999705791, 0.6865234374999714673, 0.6874999999999723554, 0.7187500000000116573, 0.7343750000000320854, 0.7421875000000422995, 0.7460937500000467404, 0.7480468750000479616, 0.7490234375000487388, 0.7500000000000495159, 0.7812500000000650591, 0.7968750000000727196, 0.8046875000000766054, 0.8085937500000784928, 0.8105468750000793809, 0.8115234375000792699, 0.8125000000000791589, 0.8437500000000712763, 0.8593750000000673905, 0.8671875000000652811, 0.8710937500000650591, 0.8730468750000650591, 0.8740234375000658362, 0.8750000000000666134, 0.9062500000000518474, 0.9218750000000451861, 0.9296875000000413003, 0.9335937500000387468, 0.9355468750000369704, 0.9375000000000351941, 1.000000000000000000 ),
 .UNSPECIFIED. ) ;
#43869=DIRECTION ( 'NONE',  ( 1.000000000000000000, 0.000000000000000000, 0.000000000000000000 ) ) ;
#43874=( BOUNDED_CURVE ( )  B_SPLINE_CURVE ( 3, ( #48839, #44383, #45611, #25670 ),
 .UNSPECIFIED., .F., .T. ) 
 B_SPLINE_CURVE_WITH_KNOTS ( ( 4, 4 ),
 ( 5.497787143782140618, 6.283185307179584456 ),
 .UNSPECIFIED. ) 
 CURVE ( )  GEOMETRIC_REPRESENTATION_ITEM ( )  RATIONAL_B_SPLINE_CURVE ( ( 1.000000000000000000, 0.9492530216741915661, 0.9492530216741915661, 1.000000000000000000 ) ) 
 REPRESENTATION_ITEM ( '' )  );
#43880=VERTEX_POINT ( 'NONE', #39859 ) ;
#43882=EDGE_CURVE ( 'NONE', #26463, #21257, #50863, .T. ) ;
#43890=AXIS2_PLACEMENT_3D ( 'NONE', #43558, #12613, #4480 ) ;
#43897=ORIENTED_EDGE ( 'NONE', *, *, #29898, .F. ) ;
#43899=CARTESIAN_POINT ( 'NONE',  ( 44.67500051388495308, 1.933004323653375156, -44.55553664676357073 ) ) ;
#43907=CARTESIAN_POINT ( 'NONE',  ( 0.8044204053657370013, -22.50679809325820102, -34.68801049095919353 ) ) ;
#43912=CARTESIAN_POINT ( 'NONE',  ( 23.32430482491560042, -49.33365190531349498, -34.64999999999999858 ) ) ;
#43915=CARTESIAN_POINT ( 'NONE',  ( 44.04477319376010769, -39.95831334196088847, -66.44292113288734924 ) ) ;
#43917=FACE_OUTER_BOUND ( 'NONE', #50971, .T. ) ;
#43919=CARTESIAN_POINT ( 'NONE',  ( -0.4410626023037880206, -27.49517073325580085, -35.14999999999999858 ) ) ;
#43932=FACE_OUTER_BOUND ( 'NONE', #2430, .T. ) ;
#43933=CARTESIAN_POINT ( 'NONE',  ( 42.21125607557041803, 8.554746773914486013, -75.31133717877361278 ) ) ;
#43937=ORIENTED_EDGE ( 'NONE', *, *, #48216, .T. ) ;
#43938=CARTESIAN_POINT ( 'NONE',  ( 28.13393739769619728, -22.54439217495490055, -35.14999999999999858 ) ) ;
#43939=CONICAL_SURFACE ( 'NONE', #388, 0.7349999999999987654, 0.06981317007977388966 ) ;
#43947=ORIENTED_EDGE ( 'NONE', *, *, #5512, .T. ) ;
#43948=CARTESIAN_POINT ( 'NONE',  ( -0.1840543581862938427, 14.24433273476873829, -34.92644969713277447 ) ) ;
#43970=ORIENTED_EDGE ( 'NONE', *, *, #40051, .F. ) ;
#43971=AXIS2_PLACEMENT_3D ( 'NONE', #28152, #31823, #19791 ) ;
#43974=CARTESIAN_POINT ( 'NONE',  ( 0.2321907996226789950, 19.54381078690260054, -34.65604112956820160 ) ) ;
#43990=CARTESIAN_POINT ( 'NONE',  ( 41.86227561628311378, 6.227911795772825165, -80.99113711912313818 ) ) ;
#43999=VECTOR ( 'NONE', #48242, 1000.000000000000000 ) ;
#44000=ORIENTED_EDGE ( 'NONE', *, *, #35243, .T. ) ;
#44001=ADVANCED_FACE ( 'NONE', ( #12595 ), #24091, .T. ) ;
#44017=ORIENTED_EDGE ( 'NONE', *, *, #39671, .T. ) ;
#44024=CARTESIAN_POINT ( 'NONE',  ( 16.13393739769620083, -45.61618894467940066, -62.64999999999999858 ) ) ;
#44033=LINE ( 'NONE', #31693, #38112 ) ;
#44045=CYLINDRICAL_SURFACE ( 'NONE', #23042, 1.999999999999998224 ) ;
#44069=CARTESIAN_POINT ( 'NONE',  ( 2.557755973795889926, -25.18888510921449964, -34.65000333055159842 ) ) ;
#44076=ORIENTED_EDGE ( 'NONE', *, *, #50994, .T. ) ;
#44078=CARTESIAN_POINT ( 'NONE',  ( 0.1375253771463843255, -45.94887013623939964, -34.68482877647384299 ) ) ;
#44085=CARTESIAN_POINT ( 'NONE',  ( 17.96595504107426677, 1.226104548012931339, -34.77490583097451804 ) ) ;
#44090=CARTESIAN_POINT ( 'NONE',  ( 45.15012441416580202, 2.064121025657089881, -35.08176457245370017 ) ) ;
#44102=CIRCLE ( 'NONE', #8127, 2.499999999999998668 ) ;
#44117=CARTESIAN_POINT ( 'NONE',  ( 17.50631664302402513, 18.38378960604975632, -83.19923667293778635 ) ) ;
#44161=ADVANCED_FACE ( 'NONE', ( #9947 ), #21725, .T. ) ;
#44166=CARTESIAN_POINT ( 'NONE',  ( 23.32493948456750132, -49.33243882768289978, -34.64999999999999858 ) ) ;
#44169=EDGE_CURVE ( 'NONE', #4309, #46086, #3977, .T. ) ;
#44170=CARTESIAN_POINT ( 'NONE',  ( 43.29584607586762246, -39.89359886923165988, -70.06847773017847203 ) ) ;
#44186=DIRECTION ( 'NONE',  ( 0.000000000000000000, 0.000000000000000000, 1.000000000000000000 ) ) ;
#44187=CARTESIAN_POINT ( 'NONE',  ( 41.70001785874607947, 8.499530765254291964, -77.77813295808087446 ) ) ;
#44189=CARTESIAN_POINT ( 'NONE',  ( 31.79224979287389985, 4.883811055320679273, -84.65000000000000568 ) ) ;
#44192=ORIENTED_EDGE ( 'NONE', *, *, #23964, .T. ) ;
#44196=ORIENTED_EDGE ( 'NONE', *, *, #47943, .F. ) ;
#44198=DIRECTION ( 'NONE',  ( 0.000000000000000000, 0.000000000000000000, -1.000000000000000000 ) ) ;
#44211=DIRECTION ( 'NONE',  ( -1.000000000000000000, 0.000000000000000000, 0.000000000000000000 ) ) ;
#44214=DIRECTION ( 'NONE',  ( 0.000000000000000000, 1.000000000000000000, 0.000000000000000000 ) ) ;
#44218=CARTESIAN_POINT ( 'NONE',  ( -22.70381420151059615, -12.10940840177920563, -54.67624860166066725 ) ) ;
#44221=CARTESIAN_POINT ( 'NONE',  ( 3.987490788289483667, -22.62894316431776787, -34.79644660940672907 ) ) ;
#44222=LINE ( 'NONE', #23769, #35464 ) ;
#44223=AXIS2_PLACEMENT_3D ( 'NONE', #33176, #44211, #25309 ) ;
#44230=DIRECTION ( 'NONE',  ( -1.000000000000000000, 0.000000000000000000, 0.000000000000000000 ) ) ;
#44250=EDGE_CURVE ( 'NONE', #6450, #29628, #39149, .T. ) ;
#44261=CARTESIAN_POINT ( 'NONE',  ( 0.07463975747345250045, -10.49561525072540036, -34.71188928912359728 ) ) ;
#44263=CIRCLE ( 'NONE', #30026, 2.999999999999999112 ) ;
#44267=DIRECTION ( 'NONE',  ( -0.3535533905932738974, 0.6123724356957941373, 0.7071067811865477948 ) ) ;
#44275=CARTESIAN_POINT ( 'NONE',  ( 16.13393739769620083, -38.61618894467930119, -84.65000000000000568 ) ) ;
#44281=ORIENTED_EDGE ( 'NONE', *, *, #10843, .F. ) ;
#44285=LINE ( 'NONE', #28808, #19515 ) ;
#44288=CARTESIAN_POINT ( 'NONE',  ( 14.63393739769630031, 1.354373803797940035, -35.14999999999999858 ) ) ;
#44290=AXIS2_PLACEMENT_3D ( 'NONE', #32505, #48533, #14180 ) ;
#44297=DIRECTION ( 'NONE',  ( -0.8660254037844381525, -0.5000000000000007772, 0.000000000000000000 ) ) ;
#44298=VECTOR ( 'NONE', #27620, 1000.000000000000114 ) ;
#44303=ORIENTED_EDGE ( 'NONE', *, *, #7470, .F. ) ;
#44318=PLANE ( 'NONE',  #37092 ) ;
#44322=DIRECTION ( 'NONE',  ( 0.000000000000000000, -1.000000000000000000, 0.000000000000000000 ) ) ;
#44326=ORIENTED_EDGE ( 'NONE', *, *, #43555, .T. ) ;
#44330=CARTESIAN_POINT ( 'NONE',  ( 0.1457839871805953758, -45.96255801450852374, -34.68167748489142355 ) ) ;
#44331=ORIENTED_EDGE ( 'NONE', *, *, #38684, .F. ) ;
#44332=CARTESIAN_POINT ( 'NONE',  ( 38.67452568954060155, -15.61618894467929941, -81.65000000000000568 ) ) ;
#44334=LINE ( 'NONE', #9225, #51299 ) ;
#44336=CIRCLE ( 'NONE', #47714, 1.999999999999998224 ) ;
#44337=ORIENTED_EDGE ( 'NONE', *, *, #50747, .T. ) ;
#44341=AXIS2_PLACEMENT_3D ( 'NONE', #50457, #2495, #11141 ) ;
#44345=CARTESIAN_POINT ( 'NONE',  ( 41.88850923412460503, -37.60571807051355364, -80.87708175111015407 ) ) ;
#44351=ADVANCED_FACE ( 'NONE', ( #16448 ), #34979, .T. ) ;
#44357=CARTESIAN_POINT ( 'NONE',  ( 0.4371248283888460318, -8.845792823550640449, -35.02873218748179340 ) ) ;
#44365=CARTESIAN_POINT ( 'NONE',  ( 10.13393739769619906, -54.15188668067469990, -35.14999999999999858 ) ) ;
#44367=VERTEX_POINT ( 'NONE', #34720 ) ;
#44370=TOROIDAL_SURFACE ( 'NONE', #23438, 16.60961179679779676, 0.5000000000000000000 ) ;
#44372=CARTESIAN_POINT ( 'NONE',  ( 19.13393739769600188, 18.38381105532069881, -83.01107220193038927 ) ) ;
#44373=AXIS2_PLACEMENT_3D ( 'NONE', #37302, #37553, #49373 ) ;
#44378=CARTESIAN_POINT ( 'NONE',  ( 12.86517331568619937, 17.88381105532060289, -34.64999999999999858 ) ) ;
#44379=CARTESIAN_POINT ( 'NONE',  ( -18.32056709076243450, -10.29233614124584761, -50.69739520735547700 ) ) ;
#44382=DIRECTION ( 'NONE',  ( 0.1961161351368100048, 0.000000000000000000, 0.9805806756911950028 ) ) ;
#44383=CARTESIAN_POINT ( 'NONE',  ( 46.82538613462320143, 3.332619105128364012, -54.61944740401203546 ) ) ;
#44389=CARTESIAN_POINT ( 'NONE',  ( -0.2164510085826325259, -10.71251607911394288, -34.95468620319246611 ) ) ;
#44393=ORIENTED_EDGE ( 'NONE', *, *, #45734, .F. ) ;
#44395=B_SPLINE_CURVE_WITH_KNOTS ( 'NONE', 3,
 ( #23806, #47694, #19385, #39821 ),
 .UNSPECIFIED., .F., .F.,
 ( 4, 4 ),
 ( 0.000000000000000000, 1.000000000000000000 ),
 .UNSPECIFIED. ) ;
#44396=ORIENTED_EDGE ( 'NONE', *, *, #28953, .F. ) ;
#44397=VERTEX_POINT ( 'NONE', #27383 ) ;
#44409=CARTESIAN_POINT ( 'NONE',  ( 14.13393739769619195, -34.76920587678100105, -43.67210485810500842 ) ) ;
#44410=CIRCLE ( 'NONE', #33512, 8.000000000000000000 ) ;
#44419=CARTESIAN_POINT ( 'NONE',  ( 17.63393739769620083, -42.11618894467939356, -34.64999999999999858 ) ) ;
#44428=DIRECTION ( 'NONE',  ( 1.000000000000000000, 0.000000000000000000, 0.000000000000000000 ) ) ;
#44430=CARTESIAN_POINT ( 'NONE',  ( 42.95314063166655671, -39.86164201837387822, -71.72600535252449561 ) ) ;
#44431=( NAMED_UNIT ( * ) SI_UNIT ( $, .STERADIAN. ) SOLID_ANGLE_UNIT ( ) );
#44435=CARTESIAN_POINT ( 'NONE',  ( 18.12828521207283217, 1.371102756008170109, -35.06583844469729172 ) ) ;
#44437=EDGE_CURVE ( 'NONE', #37692, #13888, #8057, .T. ) ;
#44445=DIRECTION ( 'NONE',  ( 1.000000000000000000, 0.000000000000000000, 0.000000000000000000 ) ) ;
#44447=CARTESIAN_POINT ( 'NONE',  ( 42.81535512389526588, 8.615775408760638854, -72.39296071868187710 ) ) ;
#44448=CARTESIAN_POINT ( 'NONE',  ( 0.1457841021255935343, -22.91266753744946527, -34.68167779225149161 ) ) ;
#44454=ORIENTED_EDGE ( 'NONE', *, *, #25836, .F. ) ;
#44460=ORIENTED_EDGE ( 'NONE', *, *, #33825, .F. ) ;
#44464=CARTESIAN_POINT ( 'NONE',  ( 0.6045892726184849408, -22.44175889786657763, -34.79644291222908237 ) ) ;
#44468=CARTESIAN_POINT ( 'NONE',  ( 44.12711257345860361, -33.11618894467940066, -54.38706558040979644 ) ) ;
#44469=LINE ( 'NONE', #48668, #13419 ) ;
#44479=LINE ( 'NONE', #24533, #18176 ) ;
#44480=ADVANCED_FACE ( 'NONE', ( #4562 ), #44661, .T. ) ;
#44489=ORIENTED_EDGE ( 'NONE', *, *, #25958, .F. ) ;
#44497=DIRECTION ( 'NONE',  ( 0.000000000000000000, 0.000000000000000000, -1.000000000000000000 ) ) ;
#44519=AXIS2_PLACEMENT_3D ( 'NONE', #23980, #24233, #40004 ) ;
#44535=CARTESIAN_POINT ( 'NONE',  ( 17.25678305769739751, -43.96113075119600211, -62.64999999999999858 ) ) ;
#44536=CARTESIAN_POINT ( 'NONE',  ( 47.13393739769619373, -39.28050807707779768, -35.14999999999999858 ) ) ;
#44537=CARTESIAN_POINT ( 'NONE',  ( 2.428024600086250206, -25.79661907562860179, -34.95504743437649608 ) ) ;
#44541=SHAPE_DEFINITION_REPRESENTATION ( #14437, #28088 ) ;
#44552=VECTOR ( 'NONE', #2189, 1000.000000000000000 ) ;
#44553=VECTOR ( 'NONE', #7357, 1000.000000000000000 ) ;
#44556=CARTESIAN_POINT ( 'NONE',  ( 14.76155815278458405, -49.61616749541425975, -83.19923667295616099 ) ) ;
#44566=CARTESIAN_POINT ( 'NONE',  ( 28.63393739769619728, -22.83306730954970121, -34.64999999999999858 ) ) ;
#44574=ORIENTED_EDGE ( 'NONE', *, *, #46767, .F. ) ;
#44578=FACE_BOUND ( 'NONE', #48775, .T. ) ;
#44583=CARTESIAN_POINT ( 'NONE',  ( 46.98749101202549383, 7.998570365497442936, -34.79644638567071269 ) ) ;
#44590=EDGE_CURVE ( 'NONE', #10013, #19286, #20019, .T. ) ;
#44597=ORIENTED_EDGE ( 'NONE', *, *, #29453, .F. ) ;
#44599=CARTESIAN_POINT ( 'NONE',  ( 41.97094584064922174, 6.386695846697909573, -80.46488821210131448 ) ) ;
#44603=CARTESIAN_POINT ( 'NONE',  ( 42.96119562966075733, -37.77193556298957589, -75.51370607938744683 ) ) ;
#44623=ORIENTED_EDGE ( 'NONE', *, *, #35057, .T. ) ;
#44632=CARTESIAN_POINT ( 'NONE',  ( -13.73674066540299954, -0.6797460008306699386, -46.71145918530370267 ) ) ;
#44646=ORIENTED_EDGE ( 'NONE', *, *, #10659, .F. ) ;
#44649=ORIENTED_EDGE ( 'NONE', *, *, #49271, .T. ) ;
#44650=EDGE_CURVE ( 'NONE', #12905, #13888, #10718, .T. ) ;
#44655=EDGE_CURVE ( 'NONE', #7182, #1986, #50084, .T. ) ;
#44658=ORIENTED_EDGE ( 'NONE', *, *, #32152, .T. ) ;
#44661=PLANE ( 'NONE',  #43342 ) ;
#44664=DIRECTION ( 'NONE',  ( 0.9752630547764096214, 0.2208726751083120443, 0.008788366098654002215 ) ) ;
#44665=LINE ( 'NONE', #7991, #26816 ) ;
#44677=CARTESIAN_POINT ( 'NONE',  ( 47.13393739769619373, -39.28050807707779768, -35.14999999999999858 ) ) ;
#44681=CARTESIAN_POINT ( 'NONE',  ( 18.02855964079333972, 1.282173023328747608, -34.84133294386911217 ) ) ;
#44683=CARTESIAN_POINT ( 'NONE',  ( 23.43760361721939844, -49.11659379690700433, -34.68023162149790295 ) ) ;
#44686=CARTESIAN_POINT ( 'NONE',  ( 42.97066549866231355, -39.86336681541309446, -71.64106045580271598 ) ) ;
#44687=ADVANCED_FACE ( 'NONE', ( #46687 ), #6579, .T. ) ;
#44688=CARTESIAN_POINT ( 'NONE',  ( -0.1437508118503130761, -27.26413697273960679, -34.89146800830132378 ) ) ;
#44691=AXIS2_PLACEMENT_3D ( 'NONE', #27282, #23330, #31197 ) ;
#44695=VERTEX_POINT ( 'NONE', #13927 ) ;
#44704=CARTESIAN_POINT ( 'NONE',  ( 42.57256523677698112, 8.591912734483669212, -73.56571430690956959 ) ) ;
#44705=CARTESIAN_POINT ( 'NONE',  ( 44.62611405146211752, -33.15679615701111516, -45.47822973459005169 ) ) ;
#44707=CARTESIAN_POINT ( 'NONE',  ( -5.079266037900150188, -4.302480445694469857, -59.64999999999999147 ) ) ;
#44723=CARTESIAN_POINT ( 'NONE',  ( -5.866062602303812490, -15.61618894467929941, -54.64999999999999858 ) ) ;
#44730=DIRECTION ( 'NONE',  ( -6.958217999999999866E-13, 1.000000000000000000, -3.004664999999999799E-13 ) ) ;
#44740=DIRECTION ( 'NONE',  ( -0.8660254037844387076, 0.4999999999999998890, 1.942890293094024439E-16 ) ) ;
#44754=CARTESIAN_POINT ( 'NONE',  ( 29.11900864776890074, -4.497910611074960485, -35.02873218748179340 ) ) ;
#44760=DIRECTION ( 'NONE',  ( 1.000000000000000000, 0.000000000000000000, 0.000000000000000000 ) ) ;
#44768=DIRECTION ( 'NONE',  ( 0.000000000000000000, 0.000000000000000000, -1.000000000000000000 ) ) ;
#44772=FACE_OUTER_BOUND ( 'NONE', #25805, .T. ) ;
#44781=EDGE_CURVE ( 'NONE', #51621, #47003, #48212, .T. ) ;
#44790=CARTESIAN_POINT ( 'NONE',  ( 18.41199818135587307, -48.25922751448980819, -34.79644660940672907 ) ) ;
#44792=CARTESIAN_POINT ( 'NONE',  ( 14.13393739769619906, -41.61618894467930119, -54.64999999999999858 ) ) ;
#44793=( BOUNDED_CURVE ( )  B_SPLINE_CURVE ( 3, ( #39089, #23313, #15232, #33897 ),
 .UNSPECIFIED., .F., .T. ) 
 B_SPLINE_CURVE_WITH_KNOTS ( ( 4, 4 ),
 ( 5.936250502017659691, 6.279745795443859357 ),
 .UNSPECIFIED. ) 
 CURVE ( )  GEOMETRIC_REPRESENTATION_ITEM ( )  RATIONAL_B_SPLINE_CURVE ( ( 1.000000000000000000, 0.9901917273091168648, 0.9901917273091168648, 1.000000000000000000 ) ) 
 REPRESENTATION_ITEM ( '' )  );
#44799=CARTESIAN_POINT ( 'NONE',  ( 0.3209249304026040028, 15.01904124785189865, -34.64999999999999858 ) ) ;
#44805=ORIENTED_EDGE ( 'NONE', *, *, #42422, .T. ) ;
#44808=DIRECTION ( 'NONE',  ( 0.000000000000000000, 0.000000000000000000, -1.000000000000000000 ) ) ;
#44817=EDGE_CURVE ( 'NONE', #45450, #20524, #6690, .T. ) ;
#44840=ORIENTED_EDGE ( 'NONE', *, *, #24673, .F. ) ;
#44852=EDGE_CURVE ( 'NONE', #11156, #37266, #15854, .T. ) ;
#44854=ORIENTED_EDGE ( 'NONE', *, *, #38639, .F. ) ;
#44866=CARTESIAN_POINT ( 'NONE',  ( 42.10651587289341080, 6.408251961395291296, -79.78705605499216347 ) ) ;
#44870=CARTESIAN_POINT ( 'NONE',  ( 42.64634278043503457, -37.72488185585652332, -77.08790612488995464 ) ) ;
#44884=CARTESIAN_POINT ( 'NONE',  ( 16.13393739769620083, -15.61618894467929941, -44.64999999999999858 ) ) ;
#44888=ORIENTED_EDGE ( 'NONE', *, *, #12550, .F. ) ;
#44894=CARTESIAN_POINT ( 'NONE',  ( 18.13393739769599833, 14.38381105532070059, -35.14999999999999858 ) ) ;
#44899=AXIS2_PLACEMENT_3D ( 'NONE', #29859, #14929, #26193 ) ;
#44924=ORIENTED_EDGE ( 'NONE', *, *, #42495, .T. ) ;
#44930=DIRECTION ( 'NONE',  ( 0.3863301728269178947, 0.9223605572462016955, 0.000000000000000000 ) ) ;
#44932=ORIENTED_EDGE ( 'NONE', *, *, #29324, .T. ) ;
#44933=ORIENTED_EDGE ( 'NONE', *, *, #39955, .F. ) ;
#44937=AXIS2_PLACEMENT_3D ( 'NONE', #38379, #2469, #47540 ) ;
#44939=CARTESIAN_POINT ( 'NONE',  ( 29.13393739769619728, -26.76363820448759867, -35.14999999999999858 ) ) ;
#44956=CARTESIAN_POINT ( 'NONE',  ( 14.63393739769620083, -32.15793020853440254, -34.64999999999999858 ) ) ;
#44957=DIRECTION ( 'NONE',  ( 0.000000000000000000, 1.000000000000000000, 0.000000000000000000 ) ) ;
#44958=ORIENTED_EDGE ( 'NONE', *, *, #22963, .T. ) ;
#44961=ORIENTED_EDGE ( 'NONE', *, *, #46447, .T. ) ;
#44964=DIRECTION ( 'NONE',  ( 1.000000000000000000, 0.000000000000000000, 0.000000000000000000 ) ) ;
#44966=CARTESIAN_POINT ( 'NONE',  ( 44.61601407454162427, 8.770664997500155380, -63.67412486887144496 ) ) ;
#44968=B_SPLINE_CURVE_WITH_KNOTS ( 'NONE', 3,
 ( #34837, #6553, #14413, #30381 ),
 .UNSPECIFIED., .F., .F.,
 ( 4, 4 ),
 ( 0.000000000000000000, 1.000000000000000000 ),
 .UNSPECIFIED. ) ;
#44973=ORIENTED_EDGE ( 'NONE', *, *, #45865, .T. ) ;
#44976=ORIENTED_EDGE ( 'NONE', *, *, #7688, .T. ) ;
#44977=CARTESIAN_POINT ( 'NONE',  ( 16.13393739769620083, -15.61618894467929941, -47.64999999999999858 ) ) ;
#44987=CARTESIAN_POINT ( 'NONE',  ( 14.12660287920414959, 18.38375430241896780, -83.14624708882956838 ) ) ;
#44993=DIRECTION ( 'NONE',  ( -1.000000000000000000, 0.000000000000000000, 0.000000000000000000 ) ) ;
#44996=CARTESIAN_POINT ( 'NONE',  ( 14.14886614762350092, -32.59522544870679894, -35.02873218748179340 ) ) ;
#44999=B_SPLINE_CURVE_WITH_KNOTS ( 'NONE', 3,
 ( #33048, #573, #8709, #9496, #28340, #16830, #12644, #40413, #32777, #36467, #44345, #41193, #16559, #25443, #33317, #4253, #32511, #322, #20224, #16306, #37265, #5045, #24919, #25188, #28602, #17352, #29128, #1361, #4506, #835, #20477, #45127, #40929, #48541, #5304, #17097, #44870, #37000, #49330, #13432, #12378, #45391, #36213, #44603, #29388, #32259, #24661, #1098, #48805, #40671, #49074, #48284, #4773, #20739, #36728, #12912, #10782, #1616, #17857, #38298, #30672, #9742, #46695, #41703, #37783, #1877, #34083, #2387, #22291, #41445, #29890, #42498, #45909, #29639, #22547, #17609, #25963, #18362, #37517, #34346, #33577, #33829, #18116, #46435, #46176, #6586, #50357, #50610, #14444, #42231, #38563, #21520, #14186, #30413, #2659, #10525, #49591, #26481, #13681, #18628, #50090, #34607, #5563, #14701, #45645, #30158, #9995, #41974, #2137, #25701, #21777, #5811, #10263, #49841, #13935, #6071, #22031, #26222, #38042, #6330, #35902, #31689, #7877, #11816, #30924, #27006, #19406, #17, #31178, #35384, #43519, #47208, #15482, #47711, #6853, #31946, #15995, #27778, #7112, #11297, #43771, #23062, #22804, #26738, #38825, #23823 ),
 .UNSPECIFIED., .F., .F.,
 ( 4, 2, 2, 2, 2, 2, 1, 2, 2, 2, 2, 1, 1, 1, 2, 2, 2, 2, 1, 1, 1, 2, 2, 2, 2, 1, 1, 2, 2, 2, 2, 1, 1, 2, 2, 2, 2, 2, 2, 2, 2, 2, 2, 2, 2, 2, 2, 2, 2, 2, 2, 2, 1, 2, 2, 2, 2, 2, 2, 2, 2, 2, 1, 2, 2, 2, 2, 2, 2, 2, 2, 1, 2, 2, 2, 2, 2, 2, 2, 4 ),
 ( 0.000000000000000000, 0.007812500000003518019, 0.01562500000000703604, 0.03125000000001407208, 0.04687500000002110812, 0.05468750000002399470, 0.05859375000002597228, 0.06054687500002690903, 0.06250000000002783884, 0.09375000000003770595, 0.1093750000000434236, 0.1171875000000472677, 0.1210937500000481976, 0.1230468750000496547, 0.1240234375000502515, 0.1250000000000508482, 0.1562500000000302258, 0.1718750000000191791, 0.1796875000000143774, 0.1835937500000114353, 0.1855468750000099920, 0.1865234375000099087, 0.1875000000000098255, 0.2187500000000126843, 0.2343750000000148215, 0.2421875000000159039, 0.2460937500000155431, 0.2480468750000153488, 0.2500000000000151545, 0.2812500000000131561, 0.2968750000000121014, 0.3046875000000122125, 0.3085937500000128231, 0.3105468750000131561, 0.3125000000000134892, 0.3437500000000138223, 0.3593750000000133782, 0.3750000000000129341, 0.4062500000000099365, 0.4218750000000083822, 0.4375000000000068279, 0.4687500000000035527, 0.4843750000000026645, 0.4921875000000013878, 0.5000000000000000000, 0.5312500000000000000, 0.5468749999999998890, 0.5546874999999998890, 0.5585937499999998890, 0.5624999999999997780, 0.5937499999999973355, 0.6093749999999962252, 0.6171874999999955591, 0.6210937499999953371, 0.6249999999999951150, 0.6562499999999987788, 0.6718750000000013323, 0.6796875000000027756, 0.6835937500000028866, 0.6875000000000028866, 0.7187500000000064393, 0.7343750000000078826, 0.7421875000000085487, 0.7460937500000093259, 0.7500000000000101030, 0.7812500000000117684, 0.7968750000000125455, 0.8046875000000129896, 0.8125000000000133227, 0.8437500000000145439, 0.8593750000000148770, 0.8671875000000148770, 0.8710937500000145439, 0.8750000000000142109, 0.9062500000000092149, 0.9218750000000069944, 0.9296875000000062172, 0.9335937500000058842, 0.9375000000000054401, 1.000000000000000000 ),
 .UNSPECIFIED. ) ;
#45001=DIRECTION ( 'NONE',  ( 0.3535533905932784493, 0.6123724356957970238, 0.7071067811865430208 ) ) ;
#45017=EDGE_CURVE ( 'NONE', #20864, #37366, #34009, .T. ) ;
#45021=TOROIDAL_SURFACE ( 'NONE', #42532, 34.47562460986249988, 0.5000000000000000000 ) ;
#45028=CARTESIAN_POINT ( 'NONE',  ( 19.16157989668716866, -49.56476373416713699, -34.89146800830127404 ) ) ;
#45029=DIRECTION ( 'NONE',  ( -1.000000000000000000, 0.000000000000000000, 0.000000000000000000 ) ) ;
#45036=ORIENTED_EDGE ( 'NONE', *, *, #22929, .F. ) ;
#45037=ADVANCED_FACE ( 'NONE', ( #14630 ), #46102, .T. ) ;
#45038=VERTEX_POINT ( 'NONE', #45832 ) ;
#45044=ORIENTED_EDGE ( 'NONE', *, *, #33851, .T. ) ;
#45049=DIRECTION ( 'NONE',  ( 0.5897727341282554825, -0.3900873262218120252, 0.7071067811865473507 ) ) ;
#45051=ORIENTED_EDGE ( 'NONE', *, *, #43651, .F. ) ;
#45053=CARTESIAN_POINT ( 'NONE',  ( 17.98749448546710994, -32.47778390180250341, -34.79644291222910368 ) ) ;
#45070=CARTESIAN_POINT ( 'NONE',  ( 47.13393739769619373, -38.26167638829240047, -54.64999999999999858 ) ) ;
#45071=CARTESIAN_POINT ( 'NONE',  ( -11.36606260230380094, -15.61618894467929941, -54.64999999999999858 ) ) ;
#45078=CARTESIAN_POINT ( 'NONE',  ( 30.26695094089093629, -35.61719269261135423, -84.60820949069447749 ) ) ;
#45096=ORIENTED_EDGE ( 'NONE', *, *, #18899, .T. ) ;
#45103=( BOUNDED_CURVE ( )  B_SPLINE_CURVE ( 3, ( #44632, #44379, #3782, #4533 ),
 .UNSPECIFIED., .F., .F. ) 
 B_SPLINE_CURVE_WITH_KNOTS ( ( 4, 4 ),
 ( 2.696998093256683937, 3.586187213922897410 ),
 .UNSPECIFIED. ) 
 CURVE ( )  GEOMETRIC_REPRESENTATION_ITEM ( )  RATIONAL_B_SPLINE_CURVE ( ( 1.000000000000000000, 0.9351900772698563680, 0.9351900772698563680, 1.000000000000000000 ) ) 
 REPRESENTATION_ITEM ( '' )  );
#45111=ORIENTED_EDGE ( 'NONE', *, *, #27493, .F. ) ;
#45114=LINE ( 'NONE', #28590, #36932 ) ;
#45115=ORIENTED_EDGE ( 'NONE', *, *, #16303, .F. ) ;
#45118=LINE ( 'NONE', #29120, #47930 ) ;
#45121=CARTESIAN_POINT ( 'NONE',  ( 41.99526469904490966, 6.390604947338678343, -80.34329386236483117 ) ) ;
#45127=CARTESIAN_POINT ( 'NONE',  ( 42.56729540932941092, -37.71296202124863584, -77.48315337116866885 ) ) ;
#45132=CIRCLE ( 'NONE', #49335, 7.000000000000000000 ) ;
#45137=LINE ( 'NONE', #9248, #17195 ) ;
#45140=EDGE_CURVE ( 'NONE', #13573, #10379, #27445, .T. ) ;
#45143=FACE_OUTER_BOUND ( 'NONE', #13946, .T. ) ;
#45155=CARTESIAN_POINT ( 'NONE',  ( 16.13393739769620083, -15.61618894467929941, -35.14999999999999858 ) ) ;
#45164=CARTESIAN_POINT ( 'NONE',  ( 28.37540540599747274, -22.68380379454831441, -34.70142521051217699 ) ) ;
#45165=VECTOR ( 'NONE', #43782, 999.9999999999998863 ) ;
#45167=AXIS2_PLACEMENT_3D ( 'NONE', #14533, #35218, #19236 ) ;
#45169=ORIENTED_EDGE ( 'NONE', *, *, #38896, .F. ) ;
#45181=DIRECTION ( 'NONE',  ( 0.000000000000000000, 1.000000000000000000, 0.000000000000000000 ) ) ;
#45182=VERTEX_POINT ( 'NONE', #7805 ) ;
#45184=EDGE_LOOP ( 'NONE', ( #23785, #6761, #34549, #37519 ) ) ;
#45189=DIRECTION ( 'NONE',  ( 0.000000000000000000, 0.000000000000000000, -1.000000000000000000 ) ) ;
#45190=ADVANCED_FACE ( 'NONE', ( #4119 ), #47137, .T. ) ;
#45191=ORIENTED_EDGE ( 'NONE', *, *, #14713, .F. ) ;
#45197=DIRECTION ( 'NONE',  ( 0.000000000000000000, -0.7071067811865466846, -0.7071067811865483499 ) ) ;
#45199=AXIS2_PLACEMENT_3D ( 'NONE', #40282, #33174, #4372 ) ;
#45204=AXIS2_PLACEMENT_3D ( 'NONE', #14031, #10364, #14289 ) ;
#45213=DIRECTION ( 'NONE',  ( 0.5516667872527449834, -0.8340645993220396903, -3.885780586188043947E-16 ) ) ;
#45215=FACE_OUTER_BOUND ( 'NONE', #31139, .T. ) ;
#45223=VERTEX_POINT ( 'NONE', #35833 ) ;
#45229=LINE ( 'NONE', #28965, #48003 ) ;
#45231=CARTESIAN_POINT ( 'NONE',  ( 45.05789191074332223, 8.802198375054555157, -61.53174790021666496 ) ) ;
#45235=EDGE_LOOP ( 'NONE', ( #9283, #19260, #47579, #37557 ) ) ;
#45242=CIRCLE ( 'NONE', #37666, 1.999999999999998224 ) ;
#45243=CYLINDRICAL_SURFACE ( 'NONE', #24288, 0.4999999999999992784 ) ;
#45248=ORIENTED_EDGE ( 'NONE', *, *, #9121, .T. ) ;
#45256=CARTESIAN_POINT ( 'NONE',  ( 2.558369240368420172, -25.18609768228349921, -34.64999999999999858 ) ) ;
#45261=CARTESIAN_POINT ( 'NONE',  ( 8.731180243531472485, 17.69319178430564321, -34.79644561402098191 ) ) ;
#45265=CARTESIAN_POINT ( 'NONE',  ( 46.66402864381289817, 8.651351690988509091, -54.57073507588959416 ) ) ;
#45270=ADVANCED_FACE ( 'NONE', ( #12773 ), #16431, .T. ) ;
#45272=DIRECTION ( 'NONE',  ( 1.000000000000000000, 0.000000000000000000, 0.000000000000000000 ) ) ;
#45274=AXIS2_PLACEMENT_3D ( 'NONE', #15056, #23666, #43869 ) ;
#45283=VERTEX_POINT ( 'NONE', #45256 ) ;
#45295=ORIENTED_EDGE ( 'NONE', *, *, #10112, .F. ) ;
#45297=ORIENTED_EDGE ( 'NONE', *, *, #14353, .T. ) ;
#45304=CARTESIAN_POINT ( 'NONE',  ( -1.553653935055010038, -50.14529331550839686, -36.11652824808269457 ) ) ;
#45307=EDGE_CURVE ( 'NONE', #50075, #21125, #26623, .T. ) ;
#45313=VECTOR ( 'NONE', #5265, 1000.000000000000000 ) ;
#45314=ORIENTED_EDGE ( 'NONE', *, *, #31431, .F. ) ;
#45330=EDGE_CURVE ( 'NONE', #36574, #40950, #24099, .T. ) ;
#45336=EDGE_CURVE ( 'NONE', #32200, #38150, #5740, .T. ) ;
#45343=CARTESIAN_POINT ( 'NONE',  ( 46.56087410975415253, -40.27520908467922567, -53.62939914585523127 ) ) ;
#45386=LINE ( 'NONE', #9492, #5071 ) ;
#45391=CARTESIAN_POINT ( 'NONE',  ( 42.90933435587908207, -37.76413940282665749, -75.77300232340927266 ) ) ;
#45424=ADVANCED_FACE ( 'NONE', ( #36866 ), #28993, .T. ) ;
#45444=EDGE_CURVE ( 'NONE', #4837, #33893, #22151, .T. ) ;
#45446=CARTESIAN_POINT ( 'NONE',  ( 2.404741263826560171, -25.85214510508460251, -35.14999999999999858 ) ) ;
#45448=CARTESIAN_POINT ( 'NONE',  ( 46.64226618924153911, 6.984935876691593215, -57.10832150000753415 ) ) ;
#45450=VERTEX_POINT ( 'NONE', #46557 ) ;
#45454=VERTEX_POINT ( 'NONE', #21631 ) ;
#45455=CARTESIAN_POINT ( 'NONE',  ( 28.13393739769619728, -8.687985714403851034, -35.14999999999999858 ) ) ;
#45457=DIRECTION ( 'NONE',  ( 0.000000000000000000, 0.000000000000000000, -1.000000000000000000 ) ) ;
#45459=DIRECTION ( 'NONE',  ( 0.000000000000000000, 1.000000000000000000, 0.000000000000000000 ) ) ;
#45476=EDGE_CURVE ( 'NONE', #32837, #49018, #31962, .T. ) ;
#45481=CARTESIAN_POINT ( 'NONE',  ( 18.13393739769619728, -45.61618894467940066, -49.33749999999999858 ) ) ;
#45483=VERTEX_POINT ( 'NONE', #42092 ) ;
#45489=CARTESIAN_POINT ( 'NONE',  ( 28.13393739769619728, -8.687985714403851034, -47.64999999999999858 ) ) ;
#45491=CARTESIAN_POINT ( 'NONE',  ( 43.25365395683799363, 8.657428456887169332, -70.27234317976126476 ) ) ;
#45496=VERTEX_POINT ( 'NONE', #38691 ) ;
#45498=AXIS2_PLACEMENT_3D ( 'NONE', #16871, #28382, #28640 ) ;
#45502=LINE ( 'NONE', #33424, #39969 ) ;
#45505=VECTOR ( 'NONE', #3483, 1000.000000000000000 ) ;
#45514=DIRECTION ( 'NONE',  ( 0.6339889056055382222, 0.000000000000000000, -0.7733421413379021336 ) ) ;
#45539=CARTESIAN_POINT ( 'NONE',  ( 47.13393739769619373, -15.61618894467929941, -54.64999999999999858 ) ) ;
#45543=ORIENTED_EDGE ( 'NONE', *, *, #40885, .T. ) ;
#45559=( BOUNDED_CURVE ( )  B_SPLINE_CURVE ( 3, ( #22412, #29243, #37902, #29752 ),
 .UNSPECIFIED., .F., .T. ) 
 B_SPLINE_CURVE_WITH_KNOTS ( ( 4, 4 ),
 ( 0.000000000000000000, 0.7853981633974557175 ),
 .UNSPECIFIED. ) 
 CURVE ( )  GEOMETRIC_REPRESENTATION_ITEM ( )  RATIONAL_B_SPLINE_CURVE ( ( 1.000000000000000000, 0.9492530216741901228, 0.9492530216741901228, 1.000000000000000000 ) ) 
 REPRESENTATION_ITEM ( '' )  );
#45563=EDGE_CURVE ( 'NONE', #36574, #2651, #35048, .T. ) ;
#45564=CARTESIAN_POINT ( 'NONE',  ( -13.69310020793190041, -40.86924150905350217, -46.67353371693619835 ) ) ;
#45571=CARTESIAN_POINT ( 'NONE',  ( 22.37218167695519710, -53.60956520270859471, -34.65000333313919612 ) ) ;
#45575=ORIENTED_EDGE ( 'NONE', *, *, #26347, .T. ) ;
#45583=EDGE_LOOP ( 'NONE', ( #51376, #39922, #16743, #31459 ) ) ;
#45588=DIRECTION ( 'NONE',  ( 0.000000000000000000, -1.000000000000000000, 0.000000000000000000 ) ) ;
#45598=CARTESIAN_POINT ( 'NONE',  ( 46.01742420967821801, -39.26550661771518236, -60.45755080081597299 ) ) ;
#45602=ORIENTED_EDGE ( 'NONE', *, *, #17509, .T. ) ;
#45604=ORIENTED_EDGE ( 'NONE', *, *, #22249, .T. ) ;
#45611=CARTESIAN_POINT ( 'NONE',  ( 47.13393739769620794, 4.077527749126597989, -54.64999999999996305 ) ) ;
#45614=ORIENTED_EDGE ( 'NONE', *, *, #42779, .T. ) ;
#45626=ORIENTED_EDGE ( 'NONE', *, *, #22288, .F. ) ;
#45639=CYLINDRICAL_SURFACE ( 'NONE', #15947, 0.4999999999999967248 ) ;
#45641=B_SPLINE_SURFACE_WITH_KNOTS ( 'NONE', 3, 3, ( 
 ( #4688, #36643, #40849, #29303, #38214, #34254 ),
 ( #30331, #45304, #22205, #30067, #33492, #25874 ),
 ( #21687, #46353, #5728, #5986, #5479, #33743 ),
 ( #46094, #21434, #37693, #50012, #21177, #49249 ),
 ( #45564, #29559, #25616, #37956, #2310, #33232 ),
 ( #18033, #1279, #33999, #13345, #9415, #1791 ),
 ( #37436, #2052, #14101, #41619, #10440, #17774 ),
 ( #41888, #10178, #26139, #1536, #37182, #6247 ),
 ( #9660, #13850, #49758, #50277, #42149, #26393 ),
 ( #5225, #18283, #29807, #21945, #45824, #41364 ),
 ( #17523, #9911, #14364, #17271, #25363, #49506 ),
 ( #13596, #42185, #34559, #6804, #34818, #38778 ),
 ( #46389, #21982, #9946, #46127, #30624, #30876 ),
 ( #6284, #50564, #22757, #50822, #2869, #50311 ),
 ( #37992, #25910, #46906, #38249, #10992, #18066 ),
 ( #14396, #34034, #41924, #6536, #26174, #10476 ),
 ( #1829, #50044, #49790, #17807, #13882, #14912 ),
 ( #2610, #26957, #14137, #46648, #2342, #18835 ),
 ( #30107, #10214, #14654, #34295, #42967, #7063 ),
 ( #23013, #18316, #33781, #30364, #26431, #42449 ) ),
 .UNSPECIFIED., .F., .F., .F.,
 ( 4, 2, 2, 2, 2, 2, 2, 2, 2, 4 ),
 ( 4, 1, 1, 4 ),
 ( -1.170155825275029926, -0.9733514710058079888, -0.5765163061072460238, -0.2263816566490509941, 0.000000000000000000, 0.1472167173675059948, 0.3827634651555170131, 0.7338073664531429285, 1.133511627823170054, 1.155436281008310084 ),
 ( -0.007901665929633120908, 0.3333333333333329818, 0.6666666666666670737, 1.002701522820989899 ),
 .UNSPECIFIED. ) ;
#45645=CARTESIAN_POINT ( 'NONE',  ( 45.37135124562947652, -38.08537628155816890, -63.46287384018188504 ) ) ;
#45659=CONICAL_SURFACE ( 'NONE', #36437, 0.7350000000000003197, 0.06981317007977388966 ) ;
#45662=DIRECTION ( 'NONE',  ( 0.000000000000000000, 0.000000000000000000, 1.000000000000000000 ) ) ;
#45668=EDGE_CURVE ( 'NONE', #12820, #33893, #30125, .T. ) ;
#45685=ORIENTED_EDGE ( 'NONE', *, *, #44781, .F. ) ;
#45694=ORIENTED_EDGE ( 'NONE', *, *, #49415, .T. ) ;
#45697=EDGE_CURVE ( 'NONE', #46482, #19317, #47836, .T. ) ;
#45702=ORIENTED_EDGE ( 'NONE', *, *, #50717, .T. ) ;
#45703=CARTESIAN_POINT ( 'NONE',  ( 46.24009931898407189, 6.945389266097389935, -59.11915260907306191 ) ) ;
#45711=ORIENTED_EDGE ( 'NONE', *, *, #23928, .F. ) ;
#45716=CIRCLE ( 'NONE', #49087, 5.251829701412240148 ) ;
#45718=CARTESIAN_POINT ( 'NONE',  ( -0.007164427059776000244, -45.70803162167019451, -34.77269723891829756 ) ) ;
#45720=AXIS2_PLACEMENT_3D ( 'NONE', #14127, #33771, #46635 ) ;
#45724=VECTOR ( 'NONE', #1450, 1000.000000000000000 ) ;
#45727=CARTESIAN_POINT ( 'NONE',  ( 28.18536260820836858, -22.57408253408722132, -34.89146800830129536 ) ) ;
#45728=DIRECTION ( 'NONE',  ( -0.5897727341282554825, -0.3900873262218120252, 0.7071067811865473507 ) ) ;
#45729=EDGE_CURVE ( 'NONE', #2348, #44367, #26870, .T. ) ;
#45731=VECTOR ( 'NONE', #1125, 1000.000000000000000 ) ;
#45734=EDGE_CURVE ( 'NONE', #44367, #43625, #51508, .T. ) ;
#45751=CARTESIAN_POINT ( 'NONE',  ( 43.58840487354246562, 8.687362816293918044, -68.65277826447533016 ) ) ;
#45755=ORIENTED_EDGE ( 'NONE', *, *, #47406, .F. ) ;
#45756=ORIENTED_EDGE ( 'NONE', *, *, #19681, .F. ) ;
#45759=ORIENTED_EDGE ( 'NONE', *, *, #33093, .F. ) ;
#45762=CARTESIAN_POINT ( 'NONE',  ( 47.13393739769619373, 4.883811055320659733, -54.64999999999999858 ) ) ;
#45763=DIRECTION ( 'NONE',  ( -0.3535533905932738974, 0.6123724356957941373, 0.7071067811865477948 ) ) ;
#45769=DIRECTION ( 'NONE',  ( 0.000000000000000000, 0.000000000000000000, -1.000000000000000000 ) ) ;
#45771=CARTESIAN_POINT ( 'NONE',  ( 38.67452568954060155, 6.328436186825659782, -81.65000000000000568 ) ) ;
#45778=DIRECTION ( 'NONE',  ( 0.8660254037844387076, 0.4999999999999998890, 0.000000000000000000 ) ) ;
#45781=EDGE_CURVE ( 'NONE', #31736, #40328, #34486, .T. ) ;
#45791=CARTESIAN_POINT ( 'NONE',  ( 46.26898798325825624, -40.10830698849575526, -55.65325670449188777 ) ) ;
#45793=B_SPLINE_CURVE_WITH_KNOTS ( 'NONE', 3,
 ( #19155, #51650, #31444, #47723, #43535, #7123, #35397, #7633, #35665, #39597 ),
 .UNSPECIFIED., .F., .F.,
 ( 4, 2, 2, 2, 4 ),
 ( -0.0003767167460152949792, 0.000000000000000000, 0.01529901560004469883, 0.03030530679046750109, 0.04513248637254871354 ),
 .UNSPECIFIED. ) ;
#45794=CARTESIAN_POINT ( 'NONE',  ( 16.13393739769620083, -15.61618894467929941, -84.65000000000000568 ) ) ;
#45803=ORIENTED_EDGE ( 'NONE', *, *, #47030, .F. ) ;
#45814=LINE ( 'NONE', #18536, #28608 ) ;
#45817=ORIENTED_EDGE ( 'NONE', *, *, #51125, .T. ) ;
#45821=FACE_OUTER_BOUND ( 'NONE', #21778, .T. ) ;
#45824=CARTESIAN_POINT ( 'NONE',  ( -22.86617264519300008, -13.70436038122300104, -54.83108237264280405 ) ) ;
#45832=CARTESIAN_POINT ( 'NONE',  ( 23.53669455186071602, -48.92556967366427756, -34.79644561402096770 ) ) ;
#45836=DIRECTION ( 'NONE',  ( 1.000000000000000000, 0.000000000000000000, 0.000000000000000000 ) ) ;
#45858=DIRECTION ( 'NONE',  ( 0.8660254037843907460, 0.5000000000000829337, 0.000000000000000000 ) ) ;
#45864=CARTESIAN_POINT ( 'NONE',  ( 41.44407966280440547, -37.52288105733000378, -83.09921727618568355 ) ) ;
#45865=EDGE_CURVE ( 'NONE', #14168, #46682, #41255, .T. ) ;
#45873=CARTESIAN_POINT ( 'NONE',  ( -0.03447620312153643757, -27.09132598751343579, -34.79644660940672907 ) ) ;
#45874=CARTESIAN_POINT ( 'NONE',  ( 20.38275687770182643, -41.70313699072102054, -59.64999999999999147 ) ) ;
#45880=CARTESIAN_POINT ( 'NONE',  ( 38.67452568954060155, 4.883811055320659733, -81.65000000000000568 ) ) ;
#45896=VERTEX_POINT ( 'NONE', #20540 ) ;
#45897=DIRECTION ( 'NONE',  ( 0.000000000000000000, 0.000000000000000000, 1.000000000000000000 ) ) ;
#45908=CARTESIAN_POINT ( 'NONE',  ( 0.03129314105546310287, -20.74349987192420031, -34.73925587533990011 ) ) ;
#45909=CARTESIAN_POINT ( 'NONE',  ( 44.25911907560086433, -37.95088198482868336, -69.02407459214848018 ) ) ;
#45927=CARTESIAN_POINT ( 'NONE',  ( 42.01335208650808539, -39.76583440177442696, -76.26778565571557067 ) ) ;
#45941=CARTESIAN_POINT ( 'NONE',  ( 38.67452568954060155, 6.328436186825659782, -81.65000000000000568 ) ) ;
#45947=ORIENTED_EDGE ( 'NONE', *, *, #32662, .T. ) ;
#45954=ORIENTED_EDGE ( 'NONE', *, *, #5906, .F. ) ;
#45957=VERTEX_POINT ( 'NONE', #40997 ) ;
#45961=CARTESIAN_POINT ( 'NONE',  ( 2.414204846871014887, -25.84668130286647170, -35.10658870009421406 ) ) ;
#45962=ORIENTED_EDGE ( 'NONE', *, *, #9279, .T. ) ;
#45964=CARTESIAN_POINT ( 'NONE',  ( 46.83508469244584660, 7.002556948733312581, -56.14421558670044732 ) ) ;
#45975=DIRECTION ( 'NONE',  ( 1.000000000000000000, 0.000000000000000000, 0.000000000000000000 ) ) ;
#45982=VECTOR ( 'NONE', #16244, 1000.000000000000000 ) ;
#45987=ORIENTED_EDGE ( 'NONE', *, *, #457, .T. ) ;
#46012=FACE_OUTER_BOUND ( 'NONE', #26589, .T. ) ;
#46013=DIRECTION ( 'NONE',  ( 0.000000000000000000, 0.000000000000000000, -1.000000000000000000 ) ) ;
#46015=CARTESIAN_POINT ( 'NONE',  ( 44.23496081612994857, 8.741156191882240023, -65.52195280072128014 ) ) ;
#46017=EDGE_CURVE ( 'NONE', #35078, #7528, #20427, .T. ) ;
#46018=CARTESIAN_POINT ( 'NONE',  ( 19.13393739769600188, 18.38381105532069881, -35.14999999999999858 ) ) ;
#46019=CARTESIAN_POINT ( 'NONE',  ( 10.11211546542419804, -54.10246922935670000, -34.93361312117490058 ) ) ;
#46020=EDGE_LOOP ( 'NONE', ( #41612, #9380, #25339, #10695 ) ) ;
#46022=B_SPLINE_CURVE_WITH_KNOTS ( 'NONE', 3,
 ( #33698, #6460, #1744, #29759, #34474, #46822, #49967, #22418 ),
 .UNSPECIFIED., .F., .F.,
 ( 4, 2, 2, 4 ),
 ( 0.05028014561732388477, 0.06097673919802479997, 0.07774712209307470256, 0.08013618654850850065 ),
 .UNSPECIFIED. ) ;
#46025=CARTESIAN_POINT ( 'NONE',  ( 17.98749078828957337, 10.53025766472752522, -34.79644660940672907 ) ) ;
#46028=VERTEX_POINT ( 'NONE', #45455 ) ;
#46032=VECTOR ( 'NONE', #30276, 1000.000000000000000 ) ;
#46051=LINE ( 'NONE', #14321, #15866 ) ;
#46056=CARTESIAN_POINT ( 'NONE',  ( 44.13393739769620083, 4.883811055320659733, -44.64999999999999858 ) ) ;
#46062=FACE_OUTER_BOUND ( 'NONE', #3633, .T. ) ;
#46080=CARTESIAN_POINT ( 'NONE',  ( 14.13393739769640156, 10.38381105532060111, -54.64999999999999858 ) ) ;
#46083=FACE_OUTER_BOUND ( 'NONE', #43826, .T. ) ;
#46086=VERTEX_POINT ( 'NONE', #25765 ) ;
#46087=ADVANCED_FACE ( 'NONE', ( #10594 ), #37577, .T. ) ;
#46094=CARTESIAN_POINT ( 'NONE',  ( -10.06026339569850059, -44.57856433944859731, -43.51454834703589825 ) ) ;
#46101=ORIENTED_EDGE ( 'NONE', *, *, #447, .T. ) ;
#46102=CYLINDRICAL_SURFACE ( 'NONE', #22430, 39.00000000000000711 ) ;
#46107=EDGE_CURVE ( 'NONE', #34997, #32498, #30225, .T. ) ;
#46112=ORIENTED_EDGE ( 'NONE', *, *, #1045, .F. ) ;
#46125=CARTESIAN_POINT ( 'NONE',  ( 46.25525774125583922, 2.762490711761015572, -35.14999999999999858 ) ) ;
#46127=CARTESIAN_POINT ( 'NONE',  ( -21.18404982641129664, -3.931304892986000166, -53.29316999191859594 ) ) ;
#46129=CARTESIAN_POINT ( 'NONE',  ( 45.67777725554724100, -40.20714941387052477, -57.99046403957294871 ) ) ;
#46135=CARTESIAN_POINT ( 'NONE',  ( 42.88601970632411309, 8.687503640012517181, -71.78374453940418221 ) ) ;
#46140=CARTESIAN_POINT ( 'NONE',  ( 29.02733844998730106, -26.70053505390490400, -34.83948955561429983 ) ) ;
#46148=ADVANCED_FACE ( 'NONE', ( #26292 ), #34147, .T. ) ;
#46163=VERTEX_POINT ( 'NONE', #26028 ) ;
#46164=LINE ( 'NONE', #22277, #4948 ) ;
#46169=DIRECTION ( 'NONE',  ( 1.000000000000000000, 0.000000000000000000, 0.000000000000000000 ) ) ;
#46170=DIRECTION ( 'NONE',  ( -0.000000000000000000, 1.000000000000000000, 0.000000000000000000 ) ) ;
#46176=CARTESIAN_POINT ( 'NONE',  ( 44.67240390351668111, -38.00310740330090908, -66.95760940388875326 ) ) ;
#46179=ORIENTED_EDGE ( 'NONE', *, *, #19681, .T. ) ;
#46180=CARTESIAN_POINT ( 'NONE',  ( 23.13393739769620083, -38.61618894467930119, -59.64999999999999147 ) ) ;
#46197=DIRECTION ( 'NONE',  ( -1.000000000000000000, 0.000000000000000000, 0.000000000000000000 ) ) ;
#46222=ORIENTED_EDGE ( 'NONE', *, *, #30670, .F. ) ;
#46226=ORIENTED_EDGE ( 'NONE', *, *, #20278, .T. ) ;
#46232=AXIS2_PLACEMENT_3D ( 'NONE', #51029, #35025, #51547 ) ;
#46234=CARTESIAN_POINT ( 'NONE',  ( 46.18989734099319122, 6.940418880791806799, -59.37015247182863220 ) ) ;
#46235=CARTESIAN_POINT ( 'NONE',  ( -5.885796488028379514, 16.61635989263051627, -40.29953568053277024 ) ) ;
#46237=EDGE_CURVE ( 'NONE', #29814, #20523, #4907, .T. ) ;
#46242=CARTESIAN_POINT ( 'NONE',  ( 16.13393739769599833, 14.38381105532070059, -35.14999999999999858 ) ) ;
#46244=DIRECTION ( 'NONE',  ( 0.000000000000000000, 0.000000000000000000, 1.000000000000000000 ) ) ;
#46257=PRODUCT_DEFINITION ( 'UNKNOWN', '', #35244, #35791 ) ;
#46261=AXIS2_PLACEMENT_3D ( 'NONE', #2911, #23057, #51381 ) ;
#46270=DIRECTION ( 'NONE',  ( 0.000000000000000000, -1.000000000000000000, 0.000000000000000000 ) ) ;
#46277=CARTESIAN_POINT ( 'NONE',  ( 0.5469381758899513057, -26.92474821800609064, -43.67210485577498957 ) ) ;
#46286=CARTESIAN_POINT ( 'NONE',  ( -22.60072279458010058, -20.15755767129849829, -54.65015892017029842 ) ) ;
#46306=FACE_OUTER_BOUND ( 'NONE', #50912, .T. ) ;
#46308=DIRECTION ( 'NONE',  ( 0.000000000000000000, 0.7071067811865463515, -0.7071067811865487940 ) ) ;
#46309=DIRECTION ( 'NONE',  ( 0.000000000000000000, -1.000000000000000000, 0.000000000000000000 ) ) ;
#46315=CARTESIAN_POINT ( 'NONE',  ( 44.73969310392494947, -40.01199137491765612, -63.07507009560972477 ) ) ;
#46319=FACE_OUTER_BOUND ( 'NONE', #31586, .T. ) ;
#46329=AXIS2_PLACEMENT_3D ( 'NONE', #35825, #11991, #11480 ) ;
#46330=ORIENTED_EDGE ( 'NONE', *, *, #30602, .T. ) ;
#46333=CARTESIAN_POINT ( 'NONE',  ( 17.63393739769629676, -7.616188944679219475, -35.14999999999999858 ) ) ;
#46339=CARTESIAN_POINT ( 'NONE',  ( -0.4123484725610440105, -45.29119327467250145, -35.12503119152799513 ) ) ;
#46343=ORIENTED_EDGE ( 'NONE', *, *, #22315, .F. ) ;
#46352=ORIENTED_EDGE ( 'NONE', *, *, #23410, .F. ) ;
#46353=CARTESIAN_POINT ( 'NONE',  ( -3.783936937370389941, -48.92741940384860300, -38.05596390819669494 ) ) ;
#46365=DIRECTION ( 'NONE',  ( 1.000000000000000000, 0.000000000000000000, 0.000000000000000000 ) ) ;
#46370=TOROIDAL_SURFACE ( 'NONE', #1159, 2.500000000000000000, 0.5000000000000000000 ) ;
#46376=AXIS2_PLACEMENT_3D ( 'NONE', #49193, #13287, #20595 ) ;
#46379=CARTESIAN_POINT ( 'NONE',  ( 13.13393739769615820, -49.61618894467929408, -35.01561944896765510 ) ) ;
#46389=CARTESIAN_POINT ( 'NONE',  ( -21.03465488720650001, -4.042464877597000239, -53.05748812964859695 ) ) ;
#46391=CARTESIAN_POINT ( 'NONE',  ( 56.92451318172422248, -22.90031634167878494, -41.48442968688959098 ) ) ;
#46392=FACE_OUTER_BOUND ( 'NONE', #40569, .T. ) ;
#46394=EDGE_LOOP ( 'NONE', ( #36777, #8105, #25833, #28851 ) ) ;
#46420=ORIENTED_EDGE ( 'NONE', *, *, #39457, .F. ) ;
#46426=VECTOR ( 'NONE', #27958, 1000.000000000000000 ) ;
#46428=VERTEX_POINT ( 'NONE', #29892 ) ;
#46435=CARTESIAN_POINT ( 'NONE',  ( 44.64515780931174760, -37.99980088791255639, -67.09384305938301907 ) ) ;
#46437=CARTESIAN_POINT ( 'NONE',  ( -22.60067283610179700, -11.07416626356550005, -54.64998264227110525 ) ) ;
#46442=CIRCLE ( 'NONE', #35528, 33.00000000000000000 ) ;
#46443=ADVANCED_FACE ( 'NONE', ( #30162 ), #17611, .T. ) ;
#46447=EDGE_CURVE ( 'NONE', #32778, #44695, #34390, .T. ) ;
#46452=VERTEX_POINT ( 'NONE', #24271 ) ;
#46456=CARTESIAN_POINT ( 'NONE',  ( 41.86582274391710001, -39.74996327333580837, -76.97917529163896688 ) ) ;
#46459=ORIENTED_EDGE ( 'NONE', *, *, #40619, .T. ) ;
#46463=LINE ( 'NONE', #42524, #15118 ) ;
#46469=CARTESIAN_POINT ( 'NONE',  ( 28.13393739769619728, -8.687985714403851034, -35.14999999999999858 ) ) ;
#46479=FACE_OUTER_BOUND ( 'NONE', #17262, .T. ) ;
#46482=VERTEX_POINT ( 'NONE', #4384 ) ;
#46493=CARTESIAN_POINT ( 'NONE',  ( -0.007164427059776000244, -45.70803162167019451, -34.77269723891829756 ) ) ;
#46494=CARTESIAN_POINT ( 'NONE',  ( 46.82606541379494303, 7.001739961803058243, -56.18931106192717095 ) ) ;
#46496=EDGE_LOOP ( 'NONE', ( #980, #5813, #43571, #18813 ) ) ;
#46500=DIRECTION ( 'NONE',  ( 0.000000000000000000, 0.000000000000000000, -1.000000000000000000 ) ) ;
#46511=CARTESIAN_POINT ( 'NONE',  ( 16.13393739769639623, 7.383811055320659733, -59.64999999999999147 ) ) ;
#46513=VERTEX_POINT ( 'NONE', #10527 ) ;
#46543=DIRECTION ( 'NONE',  ( -1.000000000000000000, 0.000000000000000000, 0.000000000000000000 ) ) ;
#46545=VERTEX_POINT ( 'NONE', #26483 ) ;
#46547=ORIENTED_EDGE ( 'NONE', *, *, #10779, .F. ) ;
#46548=ORIENTED_EDGE ( 'NONE', *, *, #16617, .F. ) ;
#46552=ORIENTED_EDGE ( 'NONE', *, *, #34203, .F. ) ;
#46555=CARTESIAN_POINT ( 'NONE',  ( 45.32648691190289725, -33.86100112340690771, -34.65030537679119504 ) ) ;
#46557=CARTESIAN_POINT ( 'NONE',  ( 46.25525774125583922, -33.99486860111965569, -54.56299356781535437 ) ) ;
#46563=EDGE_CURVE ( 'NONE', #13523, #51599, #19410, .T. ) ;
#46568=VECTOR ( 'NONE', #47861, 1000.000000000000000 ) ;
#46576=CARTESIAN_POINT ( 'NONE',  ( 45.68290005762235495, -40.07486829699336539, -58.49956670540637305 ) ) ;
#46594=CARTESIAN_POINT ( 'NONE',  ( 14.28038030992539476, 1.245406012443915467, -34.79644291222909658 ) ) ;
#46598=PLANE ( 'NONE',  #26966 ) ;
#46599=ORIENTED_EDGE ( 'NONE', *, *, #41989, .F. ) ;
#46601=AXIS2_PLACEMENT_3D ( 'NONE', #45880, #2359, #38530 ) ;
#46602=VERTEX_POINT ( 'NONE', #51388 ) ;
#46610=ORIENTED_EDGE ( 'NONE', *, *, #34203, .T. ) ;
#46621=CYLINDRICAL_SURFACE ( 'NONE', #29369, 0.4999999999999967248 ) ;
#46622=DIRECTION ( 'NONE',  ( -1.000000000000000000, 0.000000000000000000, 0.000000000000000000 ) ) ;
#46627=EDGE_CURVE ( 'NONE', #50035, #31436, #23065, .T. ) ;
#46635=DIRECTION ( 'NONE',  ( 0.7071067811865487940, 0.000000000000000000, 0.7071067811865462405 ) ) ;
#46648=CARTESIAN_POINT ( 'NONE',  ( -0.2318988266004489984, 19.75091050890950228, -35.18657710974959230 ) ) ;
#46650=CARTESIAN_POINT ( 'NONE',  ( 46.21341081811389984, -38.04634951012319988, -59.23843942165659371 ) ) ;
#46657=CARTESIAN_POINT ( 'NONE',  ( 42.41448987238078416, 8.636218628778827622, -74.08055508994929994 ) ) ;
#46666=ORIENTED_EDGE ( 'NONE', *, *, #32723, .T. ) ;
#46669=CARTESIAN_POINT ( 'NONE',  ( 46.63393739769619373, -15.61618894467929941, -35.14999999999999858 ) ) ;
#46677=ORIENTED_EDGE ( 'NONE', *, *, #2588, .T. ) ;
#46682=VERTEX_POINT ( 'NONE', #19534 ) ;
#46683=DIRECTION ( 'NONE',  ( 0.000000000000000000, 0.000000000000000000, 1.000000000000000000 ) ) ;
#46687=FACE_OUTER_BOUND ( 'NONE', #46394, .T. ) ;
#46695=CARTESIAN_POINT ( 'NONE',  ( 43.64524006940550294, -37.86935080219515015, -72.09348446035122038 ) ) ;
#46697=ORIENTED_EDGE ( 'NONE', *, *, #36784, .F. ) ;
#46703=ADVANCED_FACE ( 'NONE', ( #47081 ), #39716, .T. ) ;
#46716=CARTESIAN_POINT ( 'NONE',  ( 41.52316232194336010, -39.71166745791303754, -78.63244444805715716 ) ) ;
#46717=CARTESIAN_POINT ( 'NONE',  ( 14.13393739769619906, -32.61307204591476250, -35.10658870008958843 ) ) ;
#46747=VERTEX_POINT ( 'NONE', #23185 ) ;
#46752=CYLINDRICAL_SURFACE ( 'NONE', #3052, 3.000000000000003997 ) ;
#46757=CARTESIAN_POINT ( 'NONE',  ( 42.91198480261937931, 6.532264137049844877, -75.75975149268437292 ) ) ;
#46767=EDGE_CURVE ( 'NONE', #43323, #39742, #15355, .T. ) ;
#46775=B_SPLINE_CURVE_WITH_KNOTS ( 'NONE', 3,
 ( #7725, #30313, #33979, #26120, #27617, #3791, #7971, #23413 ),
 .UNSPECIFIED., .F., .F.,
 ( 4, 2, 2, 4 ),
 ( 0.04082353370410345822, 0.04299190937466709772, 0.06210110413228960013, 0.08070042245434939920 ),
 .UNSPECIFIED. ) ;
#46778=CARTESIAN_POINT ( 'NONE',  ( 14.28038030992539476, 1.245406012443915467, -34.79644291222909658 ) ) ;
#46784=FACE_OUTER_BOUND ( 'NONE', #29550, .T. ) ;
#46789=ORIENTED_EDGE ( 'NONE', *, *, #38602, .F. ) ;
#46803=EDGE_LOOP ( 'NONE', ( #45169, #5794, #36809, #49950, #12230 ) ) ;
#46805=CARTESIAN_POINT ( 'NONE',  ( 29.13393739769619017, -1.673960226304022969, -42.42700139135352089 ) ) ;
#46807=EDGE_CURVE ( 'NONE', #13573, #42105, #4122, .T. ) ;
#46808=FACE_OUTER_BOUND ( 'NONE', #29799, .T. ) ;
#46809=( BOUNDED_CURVE ( )  B_SPLINE_CURVE ( 3, ( #1331, #13396, #20195, #12347 ),
 .UNSPECIFIED., .F., .T. ) 
 B_SPLINE_CURVE_WITH_KNOTS ( ( 4, 4 ),
 ( 0.3752708228560562298, 1.160668986253397872 ),
 .UNSPECIFIED. ) 
 CURVE ( )  GEOMETRIC_REPRESENTATION_ITEM ( )  RATIONAL_B_SPLINE_CURVE ( ( 1.000000000000000000, 0.9492530216742047777, 0.9492530216742047777, 1.000000000000000000 ) ) 
 REPRESENTATION_ITEM ( '' )  );
#46810=CARTESIAN_POINT ( 'NONE',  ( -2.938890781262444296, -49.79850883445518406, -37.77204286592886717 ) ) ;
#46811=ORIENTED_EDGE ( 'NONE', *, *, #3957, .T. ) ;
#46815=CARTESIAN_POINT ( 'NONE',  ( 45.34326386872739789, -33.92578000960650542, -34.65000321691689322 ) ) ;
#46817=CARTESIAN_POINT ( 'NONE',  ( 44.85820924768243856, 1.972254910232243752, -41.02118509755829479 ) ) ;
#46821=EDGE_CURVE ( 'NONE', #51151, #18993, #36732, .T. ) ;
#46822=CARTESIAN_POINT ( 'NONE',  ( 2.423250969874890082, -5.412656893201930330, -35.01387690002259490 ) ) ;
#46829=LINE ( 'NONE', #51518, #22196 ) ;
#46830=CARTESIAN_POINT ( 'NONE',  ( 59.13393739769620083, 1.883811055320659955, -34.64999999999999858 ) ) ;
#46837=CARTESIAN_POINT ( 'NONE',  ( 45.02188872858284441, -40.03205829299434271, -61.70655696423168735 ) ) ;
#46854=CARTESIAN_POINT ( 'NONE',  ( 40.81680904382810837, 8.394903995891963788, -82.03934974883871689 ) ) ;
#46855=CARTESIAN_POINT ( 'NONE',  ( 44.21750825437292320, -33.11618894467930119, -52.85396186151582754 ) ) ;
#46856=CARTESIAN_POINT ( 'NONE',  ( 0.4394934780714550016, -22.38736998951459967, -35.02127583263639821 ) ) ;
#46857=DIRECTION ( 'NONE',  ( 0.000000000000000000, -1.000000000000000000, 0.000000000000000000 ) ) ;
#46861=EDGE_CURVE ( 'NONE', #27066, #38190, #15834, .T. ) ;
#46865=AXIS2_PLACEMENT_3D ( 'NONE', #26109, #22699, #51016 ) ;
#46870=VECTOR ( 'NONE', #14090, 1000.000000000000114 ) ;
#46882=ORIENTED_EDGE ( 'NONE', *, *, #51515, .F. ) ;
#46888=EDGE_CURVE ( 'NONE', #41446, #23485, #4321, .T. ) ;
#46891=CARTESIAN_POINT ( 'NONE',  ( 8.737696419500521117, 17.70577807492154321, -34.78557451168259718 ) ) ;
#46894=VERTEX_POINT ( 'NONE', #4844 ) ;
#46898=CARTESIAN_POINT ( 'NONE',  ( 23.57448381426044293, 17.62014253445614287, -34.86893418027934644 ) ) ;
#46903=CIRCLE ( 'NONE', #5882, 134.6233317251269739 ) ;
#46906=CARTESIAN_POINT ( 'NONE',  ( -15.88273178560489818, 6.935963212412289636, -48.60151163369399541 ) ) ;
#46908=CARTESIAN_POINT ( 'NONE',  ( 45.05991370691160824, -37.95321327874120243, -65.01221274611590673 ) ) ;
#46909=CARTESIAN_POINT ( 'NONE',  ( 18.13393739769620083, -45.61618894467940066, -62.64999999999999858 ) ) ;
#46914=CARTESIAN_POINT ( 'NONE',  ( 44.75967145671651082, 8.877769785130974256, -62.58944400151567322 ) ) ;
#46922=ORIENTED_EDGE ( 'NONE', *, *, #42111, .T. ) ;
#46925=VERTEX_POINT ( 'NONE', #44419 ) ;
#46951=CARTESIAN_POINT ( 'NONE',  ( 17.96595504107422059, -32.45848243737152217, -34.77490583097451093 ) ) ;
#46953=AXIS2_PLACEMENT_3D ( 'NONE', #37385, #2723, #50423 ) ;
#46956=CARTESIAN_POINT ( 'NONE',  ( 27.13393739769620083, -38.61618894467930119, -84.65000000000000568 ) ) ;
#46957=ORIENTED_EDGE ( 'NONE', *, *, #3370, .T. ) ;
#46960=CARTESIAN_POINT ( 'NONE',  ( -22.84309005266754511, -14.77827754098507818, -54.74605632281347312 ) ) ;
#46968=B_SPLINE_CURVE_WITH_KNOTS ( 'NONE', 3,
 ( #49022, #8653, #20685, #8922, #24868, #40879, #13125, #30359, #41393, #5509, #49787, #30102, #41655, #21717, #18063, #49537, #10472, #22496, #26427, #33778, #42445, #13631, #25905, #29589, #5758 ),
 .UNSPECIFIED., .F., .F.,
 ( 4, 3, 3, 3, 3, 3, 3, 3, 4 ),
 ( -0.0003379885557460000044, 0.000000000000000000, 0.01174556080967900130, 0.02341952721554300260, 0.03417459637594329885, 0.04370164535764300279, 0.05433935653199269827, 0.06272590451755999386, 0.06880987158481699506 ),
 .UNSPECIFIED. ) ;
#46977=CARTESIAN_POINT ( 'NONE',  ( 44.13393739769620083, 4.883811055320659733, -35.14999999999999858 ) ) ;
#46978=ORIENTED_EDGE ( 'NONE', *, *, #13021, .T. ) ;
#46980=AXIS2_PLACEMENT_3D ( 'NONE', #35508, #50466, #30525 ) ;
#46997=ADVANCED_FACE ( 'NONE', ( #41518 ), #50165, .T. ) ;
#47001=CARTESIAN_POINT ( 'NONE',  ( 31.13393739769620083, -36.11618894467930119, -81.65000000000000568 ) ) ;
#47003=VERTEX_POINT ( 'NONE', #22102 ) ;
#47011=ORIENTED_EDGE ( 'NONE', *, *, #30064, .T. ) ;
#47013=CARTESIAN_POINT ( 'NONE',  ( 43.03331702636307199, 6.550456568673448388, -75.15310059331962123 ) ) ;
#47017=CARTESIAN_POINT ( 'NONE',  ( 16.13393739769620083, -15.61618894467929941, -54.64999999999999858 ) ) ;
#47019=EDGE_CURVE ( 'NONE', #8526, #23591, #50996, .T. ) ;
#47030=EDGE_CURVE ( 'NONE', #40270, #2647, #13736, .T. ) ;
#47034=EDGE_CURVE ( 'NONE', #47312, #25918, #38426, .T. ) ;
#47038=DIRECTION ( 'NONE',  ( -1.000000000000000000, -5.465567116091310088E-15, 0.000000000000000000 ) ) ;
#47046=CARTESIAN_POINT ( 'NONE',  ( -6.434040441868821958, -15.02156145381371388, 4.943674098299959851 ) ) ;
#47061=EDGE_CURVE ( 'NONE', #13116, #35078, #18185, .T. ) ;
#47062=ORIENTED_EDGE ( 'NONE', *, *, #51700, .F. ) ;
#47065=ORIENTED_EDGE ( 'NONE', *, *, #51156, .F. ) ;
#47070=DIRECTION ( 'NONE',  ( -1.000000000000000000, 0.000000000000000000, 0.000000000000000000 ) ) ;
#47074=DIRECTION ( 'NONE',  ( 0.000000000000000000, 1.000000000000000000, 0.000000000000000000 ) ) ;
#47081=FACE_OUTER_BOUND ( 'NONE', #40205, .T. ) ;
#47085=CARTESIAN_POINT ( 'NONE',  ( 33.13393739769620083, -38.61618894467930119, -72.14999999999999147 ) ) ;
#47093=EDGE_CURVE ( 'NONE', #11926, #30658, #26034, .T. ) ;
#47094=CARTESIAN_POINT ( 'NONE',  ( 45.10073672284692492, -40.03758267129227022, -61.32363707965989619 ) ) ;
#47096=CARTESIAN_POINT ( 'NONE',  ( 22.27218754053109961, 22.60556764129909979, -34.69483829921999529 ) ) ;
#47097=SURFACE_STYLE_FILL_AREA ( #43155 ) ;
#47106=( BOUNDED_CURVE ( )  B_SPLINE_CURVE ( 3, ( #21339, #20821, #5128, #17430 ),
 .UNSPECIFIED., .F., .T. ) 
 B_SPLINE_CURVE_WITH_KNOTS ( ( 4, 4 ),
 ( 4.712388980384782045, 5.497787143782128183 ),
 .UNSPECIFIED. ) 
 CURVE ( )  GEOMETRIC_REPRESENTATION_ITEM ( )  RATIONAL_B_SPLINE_CURVE ( ( 1.000000000000000000, 0.9492530216742041116, 0.9492530216742041116, 1.000000000000000000 ) ) 
 REPRESENTATION_ITEM ( '' )  );
#47119=CARTESIAN_POINT ( 'NONE',  ( 0.06741163554565170191, 19.71662681832729902, -34.75842043174770168 ) ) ;
#47120=ORIENTED_EDGE ( 'NONE', *, *, #15240, .T. ) ;
#47121=ORIENTED_EDGE ( 'NONE', *, *, #42111, .F. ) ;
#47128=VERTEX_POINT ( 'NONE', #18440 ) ;
#47135=CARTESIAN_POINT ( 'NONE',  ( 0.1457841021255935343, -15.61618894467929941, -34.68167779225149161 ) ) ;
#47137=PLANE ( 'NONE',  #32445 ) ;
#47149=CARTESIAN_POINT ( 'NONE',  ( 46.98749101202549383, 7.998570365497442936, -34.79644638567071269 ) ) ;
#47155=CARTESIAN_POINT ( 'NONE',  ( 23.55667557762233244, 17.65459752315667430, -34.82978046822307761 ) ) ;
#47158=CARTESIAN_POINT ( 'NONE',  ( 8.942300673233280150, -49.33122573608360284, -34.65000333295999724 ) ) ;
#47163=CARTESIAN_POINT ( 'NONE',  ( 44.83365995299240581, -37.92676521017259716, -66.14348151571169865 ) ) ;
#47170=CARTESIAN_POINT ( 'NONE',  ( 44.36630888106301995, 6.521024588956093382, -68.44974023162843935 ) ) ;
#47171=CARTESIAN_POINT ( 'NONE',  ( 19.13393739769620083, -49.61618894467939356, -83.01107220193038927 ) ) ;
#47173=CARTESIAN_POINT ( 'NONE',  ( 47.04404845359660214, -39.25010480764659349, -34.85732842610099880 ) ) ;
#47180=ORIENTED_EDGE ( 'NONE', *, *, #48401, .T. ) ;
#47182=EDGE_CURVE ( 'NONE', #31436, #45896, #39917, .T. ) ;
#47208=CARTESIAN_POINT ( 'NONE',  ( 46.43430893930594294, -38.19702260607925837, -58.14814218777431165 ) ) ;
#47252=CARTESIAN_POINT ( 'NONE',  ( 20.30127474080349970, -42.11618894467939356, -34.64999999999999858 ) ) ;
#47261=DIRECTION ( 'NONE',  ( 1.000000000000000000, 0.000000000000000000, 0.000000000000000000 ) ) ;
#47265=CARTESIAN_POINT ( 'NONE',  ( 44.76553362146206894, 6.782212060689038147, -66.49196124640384653 ) ) ;
#47268=ORIENTED_EDGE ( 'NONE', *, *, #3625, .T. ) ;
#47295=CARTESIAN_POINT ( 'NONE',  ( 16.13393739769620083, -38.61618894467930119, -84.65000000000000568 ) ) ;
#47304=VECTOR ( 'NONE', #7510, 1000.000000000000114 ) ;
#47312=VERTEX_POINT ( 'NONE', #10854 ) ;
#47316=CARTESIAN_POINT ( 'NONE',  ( 46.11904533366443104, 8.867946641963873944, -56.38094778067191726 ) ) ;
#47327=ORIENTED_EDGE ( 'NONE', *, *, #17194, .T. ) ;
#47332=CARTESIAN_POINT ( 'NONE',  ( 44.66807317952414991, 1.931744143413151038, -44.68675940148178682 ) ) ;
#47347=CARTESIAN_POINT ( 'NONE',  ( 45.86929072264158691, -40.08640120534250428, -57.59292921774597573 ) ) ;
#47350=SURFACE_SIDE_STYLE ('',( #47097 ) ) ;
#47353=CIRCLE ( 'NONE', #29742, 5.251829701412240148 ) ;
#47358=ORIENTED_EDGE ( 'NONE', *, *, #16521, .F. ) ;
#47366=CARTESIAN_POINT ( 'NONE',  ( 14.30191975431828411, 1.226104548012949325, -34.77490583097451093 ) ) ;
#47369=ORIENTED_EDGE ( 'NONE', *, *, #45336, .T. ) ;
#47371=ORIENTED_EDGE ( 'NONE', *, *, #1368, .F. ) ;
#47390=CARTESIAN_POINT ( 'NONE',  ( 19.22157560178254698, 18.51631118994118808, -82.73668660645967066 ) ) ;
#47391=ORIENTED_EDGE ( 'NONE', *, *, #9648, .T. ) ;
#47394=DIRECTION ( 'NONE',  ( 0.000000000000000000, -1.000000000000000000, 0.000000000000000000 ) ) ;
#47395=DIRECTION ( 'NONE',  ( 0.000000000000000000, 0.000000000000000000, -1.000000000000000000 ) ) ;
#47400=LINE ( 'NONE', #39778, #32586 ) ;
#47402=CARTESIAN_POINT ( 'NONE',  ( 8.942300673232759678, 18.09884784672440006, -34.65000333295999724 ) ) ;
#47405=DIRECTION ( 'NONE',  ( -0.4999999999999995004, 0.8660254037844390407, 0.000000000000000000 ) ) ;
#47406=EDGE_CURVE ( 'NONE', #47961, #48439, #33079, .T. ) ;
#47412=( BOUNDED_CURVE ( )  B_SPLINE_CURVE ( 3, ( #2037, #33983, #30050, #2561 ),
 .UNSPECIFIED., .F., .T. ) 
 B_SPLINE_CURVE_WITH_KNOTS ( ( 4, 4 ),
 ( 1.570796326794901665, 2.356194490192332403 ),
 .UNSPECIFIED. ) 
 CURVE ( )  GEOMETRIC_REPRESENTATION_ITEM ( )  RATIONAL_B_SPLINE_CURVE ( ( 1.000000000000000000, 0.9492530216741933424, 0.9492530216741933424, 1.000000000000000000 ) ) 
 REPRESENTATION_ITEM ( '' )  );
#47416=VECTOR ( 'NONE', #11527, 1000.000000000000000 ) ;
#47419=CARTESIAN_POINT ( 'NONE',  ( 38.67452568954060155, -37.56081407618430035, -84.65000000000000568 ) ) ;
#47425=ORIENTED_EDGE ( 'NONE', *, *, #7986, .T. ) ;
#47426=CARTESIAN_POINT ( 'NONE',  ( 47.12223953835182755, 6.751577964446205726, -54.64278194131097166 ) ) ;
#47434=CARTESIAN_POINT ( 'NONE',  ( 46.63393739769619373, -36.11618894467930119, -34.64999999999999858 ) ) ;
#47435=ORIENTED_EDGE ( 'NONE', *, *, #28683, .T. ) ;
#47437=EDGE_LOOP ( 'NONE', ( #17565, #22304 ) ) ;
#47443=LINE ( 'NONE', #10759, #41837 ) ;
#47448=CARTESIAN_POINT ( 'NONE',  ( 20.13393739769620083, -28.89524513604070322, -39.64999999999999858 ) ) ;
#47449=ORIENTED_EDGE ( 'NONE', *, *, #10112, .T. ) ;
#47464=ORIENTED_EDGE ( 'NONE', *, *, #14713, .T. ) ;
#47465=CARTESIAN_POINT ( 'NONE',  ( -22.84941414684771388, -15.61618224896967355, -54.74986855478772441 ) ) ;
#47469=CARTESIAN_POINT ( 'NONE',  ( 29.13393739769619728, -35.78776181993320193, -84.65000000000000568 ) ) ;
#47473=CARTESIAN_POINT ( 'NONE',  ( 0.1375253771463928743, 14.71649224688080082, -34.68482877647384299 ) ) ;
#47493=CARTESIAN_POINT ( 'NONE',  ( -0.1963508450805951933, -45.46408278790535462, -34.93716512309965339 ) ) ;
#47506=ORIENTED_EDGE ( 'NONE', *, *, #7969, .T. ) ;
#47508=EDGE_CURVE ( 'NONE', #51808, #11818, #19154, .T. ) ;
#47516=CARTESIAN_POINT ( 'NONE',  ( 44.64206215848041381, 6.767191847450578557, -67.10931550608336238 ) ) ;
#47535=CARTESIAN_POINT ( 'NONE',  ( 4.133937397696209715, -8.687985714403833271, -35.01561944896766221 ) ) ;
#47540=DIRECTION ( 'NONE',  ( 0.5198294763375396199, 0.8542087557464956848, -0.01023313914021957947 ) ) ;
#47542=CARTESIAN_POINT ( 'NONE',  ( 15.31199894099709979, -16.87369336301570044, -35.14999999999999858 ) ) ;
#47544=DIRECTION ( 'NONE',  ( 0.000000000000000000, 0.000000000000000000, 1.000000000000000000 ) ) ;
#47551=CARTESIAN_POINT ( 'NONE',  ( -0.1944835411611390841, -20.56321558487172751, -34.93556154945131453 ) ) ;
#47560=CARTESIAN_POINT ( 'NONE',  ( 22.13393739769619728, -54.15188668067469990, -35.09469305598949518 ) ) ;
#47567=ORIENTED_EDGE ( 'NONE', *, *, #38110, .F. ) ;
#47579=ORIENTED_EDGE ( 'NONE', *, *, #50624, .T. ) ;
#47580=FACE_OUTER_BOUND ( 'NONE', #36565, .T. ) ;
#47583=CARTESIAN_POINT ( 'NONE',  ( 45.06234682331504615, 2.029620634295568937, -36.93999394477614828 ) ) ;
#47597=CARTESIAN_POINT ( 'NONE',  ( 42.43635952588410731, -39.81067629326607005, -74.22320020691999787 ) ) ;
#47598=DIRECTION ( 'NONE',  ( -1.000000000000000000, -1.006844464268868150E-16, 0.000000000000000000 ) ) ;
#47602=LINE ( 'NONE', #31327, #47304 ) ;
#47615=CARTESIAN_POINT ( 'NONE',  ( 42.72653070048255586, 8.607061861151045434, -72.82242792000907627 ) ) ;
#47616=LINE ( 'NONE', #15127, #33137 ) ;
#47617=FACE_OUTER_BOUND ( 'NONE', #10080, .T. ) ;
#47618=CARTESIAN_POINT ( 'NONE',  ( 38.67452568954060155, 4.883811055320659733, -81.65000000000000568 ) ) ;
#47623=CARTESIAN_POINT ( 'NONE',  ( 0.1457841021255935343, -26.78123956999450428, -34.68167779225149161 ) ) ;
#47630=CARTESIAN_POINT ( 'NONE',  ( -20.29802031372836524, -1.697423245748443943, -52.67334128422192663 ) ) ;
#47647=ADVANCED_FACE ( 'NONE', ( #8397 ), #12080, .T. ) ;
#47650=CARTESIAN_POINT ( 'NONE',  ( 8.787528872099951371, 17.80194031521759968, -34.71551406240389781 ) ) ;
#47654=EDGE_LOOP ( 'NONE', ( #25436, #44597, #43644, #14780, #9075 ) ) ;
#47656=DIRECTION ( 'NONE',  ( -1.000000000000000000, 0.000000000000000000, 0.000000000000000000 ) ) ;
#47662=CARTESIAN_POINT ( 'NONE',  ( 47.13393739769619373, -36.11618894467930119, -54.64999999999999858 ) ) ;
#47664=EDGE_CURVE ( 'NONE', #19127, #46545, #33129, .T. ) ;
#47666=CARTESIAN_POINT ( 'NONE',  ( 0.4420762188774280399, -8.844152220602129688, -35.01387690002259490 ) ) ;
#47677=CARTESIAN_POINT ( 'NONE',  ( 46.20542188648048665, 6.681296133090609324, -59.23417205188202672 ) ) ;
#47691=EDGE_CURVE ( 'NONE', #51177, #46163, #33439, .T. ) ;
#47694=CARTESIAN_POINT ( 'NONE',  ( 13.04629919360955448, -49.74868907930030559, -82.73668660645857642 ) ) ;
#47705=ORIENTED_EDGE ( 'NONE', *, *, #1281, .F. ) ;
#47711=CARTESIAN_POINT ( 'NONE',  ( 46.48050859836360615, -38.20152441653880260, -57.91714385711884461 ) ) ;
#47713=ORIENTED_EDGE ( 'NONE', *, *, #31267, .F. ) ;
#47714=AXIS2_PLACEMENT_3D ( 'NONE', #31621, #39520, #22989 ) ;
#47717=DIRECTION ( 'NONE',  ( 0.3863301728269245006, -0.9223605572461989199, -3.608224830031755305E-16 ) ) ;
#47718=VECTOR ( 'NONE', #42674, 1000.000000000000000 ) ;
#47723=CARTESIAN_POINT ( 'NONE',  ( 9.916610038436060037, 22.42506970168800251, -34.65028073423250277 ) ) ;
#47734=EDGE_CURVE ( 'NONE', #38545, #24575, #6277, .T. ) ;
#47745=ORIENTED_EDGE ( 'NONE', *, *, #5067, .T. ) ;
#47747=TOROIDAL_SURFACE ( 'NONE', #5061, 2.500000000000000000, 0.5000000000000000000 ) ;
#47749=CARTESIAN_POINT ( 'NONE',  ( 0.1155610841158959956, 19.94237700917059897, -35.14999985728680088 ) ) ;
#47751=CARTESIAN_POINT ( 'NONE',  ( 12.95491128060830022, 18.65448050664010182, -82.14319696191608955 ) ) ;
#47756=VECTOR ( 'NONE', #20721, 1000.000000000000114 ) ;
#47759=DIRECTION ( 'NONE',  ( 1.000000000000000000, 0.000000000000000000, 0.000000000000000000 ) ) ;
#47760=ORIENTED_EDGE ( 'NONE', *, *, #43328, .F. ) ;
#47761=ORIENTED_EDGE ( 'NONE', *, *, #49918, .F. ) ;
#47770=CARTESIAN_POINT ( 'NONE',  ( 44.39412272499598799, 6.736181560341522712, -68.34907281161095227 ) ) ;
#47790=EDGE_CURVE ( 'NONE', #6571, #43625, #43874, .T. ) ;
#47795=ORIENTED_EDGE ( 'NONE', *, *, #5638, .F. ) ;
#47796=CARTESIAN_POINT ( 'NONE',  ( 26.93010376912529935, -27.85143120648099924, -35.14999999999999858 ) ) ;
#47803=DIRECTION ( 'NONE',  ( -1.000000000000000000, 0.000000000000000000, 0.000000000000000000 ) ) ;
#47807=CARTESIAN_POINT ( 'NONE',  ( 20.47328261930400473, -41.85765695298069033, -34.70142521051216988 ) ) ;
#47815=CARTESIAN_POINT ( 'NONE',  ( 38.67452568954050207, 4.883811055320659733, -81.65000000000000568 ) ) ;
#47825=DIRECTION ( 'NONE',  ( 0.7165155114351267063, -0.6975711590030502229, 0.000000000000000000 ) ) ;
#47828=AXIS2_PLACEMENT_3D ( 'NONE', #3283, #39187, #27631 ) ;
#47832=ORIENTED_EDGE ( 'NONE', *, *, #32140, .T. ) ;
#47834=ORIENTED_EDGE ( 'NONE', *, *, #2592, .T. ) ;
#47836=LINE ( 'NONE', #14828, #7430 ) ;
#47839=DIRECTION ( 'NONE',  ( 0.3863301728269245006, -0.9223605572461989199, -3.608224830031755305E-16 ) ) ;
#47840=DIRECTION ( 'NONE',  ( 1.000000000000000000, 0.000000000000000000, 0.000000000000000000 ) ) ;
#47842=DIRECTION ( 'NONE',  ( 0.000000000000000000, -1.000000000000000000, 0.000000000000000000 ) ) ;
#47845=EDGE_LOOP ( 'NONE', ( #29833, #9797, #9699, #42802, #28488, #38742, #45314 ) ) ;
#47846=CARTESIAN_POINT ( 'NONE',  ( 10.13393739769619906, -54.15188668067469990, -54.64999999999999858 ) ) ;
#47851=CARTESIAN_POINT ( 'NONE',  ( 42.23404623588641016, -39.78951633867036719, -75.20128091132379211 ) ) ;
#47859=CARTESIAN_POINT ( 'NONE',  ( -1.143840380081567076, -15.61618894467929941, -35.76111111111109864 ) ) ;
#47861=DIRECTION ( 'NONE',  ( -1.000000000000000000, 0.000000000000000000, 0.000000000000000000 ) ) ;
#47863=DIRECTION ( 'NONE',  ( -1.000000000000000000, 0.000000000000000000, 0.000000000000000000 ) ) ;
#47868=ORIENTED_EDGE ( 'NONE', *, *, #25470, .T. ) ;
#47873=CARTESIAN_POINT ( 'NONE',  ( 42.43805389010415041, 8.578463427208918191, -74.21497205410845766 ) ) ;
#47874=DIRECTION ( 'NONE',  ( 0.000000000000000000, 1.000000000000000000, 0.000000000000000000 ) ) ;
#47877=ORIENTED_EDGE ( 'NONE', *, *, #27178, .T. ) ;
#47880=EDGE_CURVE ( 'NONE', #26299, #49499, #28416, .T. ) ;
#47886=ORIENTED_EDGE ( 'NONE', *, *, #13964, .T. ) ;
#47887=CARTESIAN_POINT ( 'NONE',  ( -0.1122294247164806885, 14.32548074922725867, -34.86373113243160304 ) ) ;
#47890=CARTESIAN_POINT ( 'NONE',  ( 19.31296351478360052, 18.65448050664020130, -82.14319696191608955 ) ) ;
#47900=CARTESIAN_POINT ( 'NONE',  ( 0.3209249304026170480, -4.754491132419490285, -34.64999999999999858 ) ) ;
#47910=ORIENTED_EDGE ( 'NONE', *, *, #20030, .T. ) ;
#47912=EDGE_CURVE ( 'NONE', #24768, #13283, #10650, .T. ) ;
#47917=LINE ( 'NONE', #42960, #10377 ) ;
#47921=EDGE_CURVE ( 'NONE', #2764, #46028, #22965, .T. ) ;
#47926=DIRECTION ( 'NONE',  ( 1.000000000000000000, 0.000000000000000000, 0.000000000000000000 ) ) ;
#47929=ORIENTED_EDGE ( 'NONE', *, *, #42050, .T. ) ;
#47930=VECTOR ( 'NONE', #39901, 1000.000000000000114 ) ;
#47933=CARTESIAN_POINT ( 'NONE',  ( 45.96971012568268833, 6.673253363729896748, -60.41974218095914040 ) ) ;
#47943=EDGE_CURVE ( 'NONE', #23957, #24198, #38986, .T. ) ;
#47956=ORIENTED_EDGE ( 'NONE', *, *, #29513, .F. ) ;
#47961=VERTEX_POINT ( 'NONE', #3082 ) ;
#47963=CARTESIAN_POINT ( 'NONE',  ( 19.13393739769620083, -49.61618894467939356, -83.01107220193038927 ) ) ;
#47977=DIRECTION ( 'NONE',  ( -0.7071067811865492381, 0.000000000000000000, 0.7071067811865457964 ) ) ;
#47978=CARTESIAN_POINT ( 'NONE',  ( 0.1457840807894888180, 19.59951024407514097, -34.68167773519660813 ) ) ;
#48003=VECTOR ( 'NONE', #44964, 1000.000000000000000 ) ;
#48016=CARTESIAN_POINT ( 'NONE',  ( 16.13393739769599833, 14.38381105532070059, -59.64999999999999147 ) ) ;
#48017=PLANE ( 'NONE',  #13531 ) ;
#48022=CARTESIAN_POINT ( 'NONE',  ( -5.055476499123447098, 11.23874896328612571, -39.16253382332155297 ) ) ;
#48023=CARTESIAN_POINT ( 'NONE',  ( 17.87670698131379865, 1.145880372109089995, -34.70985242058479514 ) ) ;
#48028=EDGE_CURVE ( 'NONE', #19317, #8526, #26873, .T. ) ;
#48051=CARTESIAN_POINT ( 'NONE',  ( 33.13393739769620083, 7.383811055320659733, -72.14999999999999147 ) ) ;
#48055=CARTESIAN_POINT ( 'NONE',  ( 16.38470059807072943, 18.38381071981026693, -83.24417156243271165 ) ) ;
#48063=AXIS2_PLACEMENT_3D ( 'NONE', #17530, #36923, #33499 ) ;
#48069=CARTESIAN_POINT ( 'NONE',  ( -0.1114929980067364962, -10.52519485297225366, -34.86345228575846988 ) ) ;
#48075=ORIENTED_EDGE ( 'NONE', *, *, #50747, .F. ) ;
#48084=ORIENTED_EDGE ( 'NONE', *, *, #49341, .T. ) ;
#48090=FACE_OUTER_BOUND ( 'NONE', #10952, .T. ) ;
#48096=CARTESIAN_POINT ( 'NONE',  ( 0.6320745533423832718, -22.45076187167874338, -34.77490583097448962 ) ) ;
#48107=CARTESIAN_POINT ( 'NONE',  ( 43.32052231349704385, -39.89583416345196554, -69.94913773093004750 ) ) ;
#48119=FACE_OUTER_BOUND ( 'NONE', #4151, .T. ) ;
#48122=CYLINDRICAL_SURFACE ( 'NONE', #25239, 39.00000000000000711 ) ;
#48123=CARTESIAN_POINT ( 'NONE',  ( 41.84854853683915366, 8.515723429679729506, -77.06240910697275126 ) ) ;
#48130=EDGE_LOOP ( 'NONE', ( #8247, #44649, #25792, #11343, #40991, #14304, #5889, #46420 ) ) ;
#48141=ADVANCED_FACE ( 'NONE', ( #47617 ), #44370, .T. ) ;
#48142=CARTESIAN_POINT ( 'NONE',  ( 14.13393739769640156, 10.38381105532060111, -35.14999999999999858 ) ) ;
#48145=B_SPLINE_CURVE_WITH_KNOTS ( 'NONE', 3,
 ( #23912, #11645, #15821, #43616, #15316, #39938 ),
 .UNSPECIFIED., .F., .F.,
 ( 4, 2, 4 ),
 ( -0.0006077122342960819372, 0.000000000000000000, 0.03318971727292711893 ),
 .UNSPECIFIED. ) ;
#48146=EDGE_LOOP ( 'NONE', ( #35443, #2257, #36786, #32414, #17751 ) ) ;
#48154=CARTESIAN_POINT ( 'NONE',  ( -0.007164427059776000244, -27.04615419348650107, -34.77269723891829756 ) ) ;
#48156=( BOUNDED_CURVE ( )  B_SPLINE_CURVE ( 2, ( #36190, #15521, #47751 ),
 .UNSPECIFIED., .F., .T. ) 
 B_SPLINE_CURVE_WITH_KNOTS ( ( 3, 3 ),
 ( 1.923142637335169880, 4.853851569642519515 ),
 .UNSPECIFIED. ) 
 CURVE ( )  GEOMETRIC_REPRESENTATION_ITEM ( )  RATIONAL_B_SPLINE_CURVE ( ( 1.003436844930660099, 1.004455541116340056, 1.000597593688439924 ) ) 
 REPRESENTATION_ITEM ( '' )  );
#48167=TOROIDAL_SURFACE ( 'NONE', #25554, 31.45861873485090143, 3.000000000000000000 ) ;
#48171=DIRECTION ( 'NONE',  ( 0.000000000000000000, -1.000000000000000000, 0.000000000000000000 ) ) ;
#48174=AXIS2_PLACEMENT_3D ( 'NONE', #35794, #3832, #11185 ) ;
#48180=CARTESIAN_POINT ( 'NONE',  ( 45.61405083969839325, 7.915465039487636467, -62.73908642572272498 ) ) ;
#48181=CARTESIAN_POINT ( 'NONE',  ( 14.13393739769619906, -41.61618894467930119, -35.14999999999999858 ) ) ;
#48198=AXIS2_PLACEMENT_3D ( 'NONE', #37927, #21919, #22176 ) ;
#48199=ORIENTED_EDGE ( 'NONE', *, *, #3370, .F. ) ;
#48204=CARTESIAN_POINT ( 'NONE',  ( 41.61626771661330082, 6.328436186825659782, -82.23834840541459812 ) ) ;
#48208=ADVANCED_FACE ( 'NONE', ( #33152 ), #13783, .T. ) ;
#48212=LINE ( 'NONE', #15726, #11581 ) ;
#48213=CARTESIAN_POINT ( 'NONE',  ( 18.09749211374579758, -32.57607267493840197, -34.95504743437649608 ) ) ;
#48216=EDGE_CURVE ( 'NONE', #25427, #41238, #29738, .T. ) ;
#48223=VECTOR ( 'NONE', #22816, 1000.000000000000114 ) ;
#48224=EDGE_CURVE ( 'NONE', #32046, #26382, #1016, .T. ) ;
#48225=CARTESIAN_POINT ( 'NONE',  ( 0.08961746015897878448, -8.352138177767987059, -34.70268271585497644 ) ) ;
#48239=CARTESIAN_POINT ( 'NONE',  ( 41.95231199169119662, -39.81623677285271867, -76.32572085277173812 ) ) ;
#48242=DIRECTION ( 'NONE',  ( 0.000000000000000000, 0.000000000000000000, -1.000000000000000000 ) ) ;
#48255=ORIENTED_EDGE ( 'NONE', *, *, #18160, .F. ) ;
#48262=CARTESIAN_POINT ( 'NONE',  ( 46.70917532059600319, 7.904099119542530083, -34.65437117444129456 ) ) ;
#48265=DIRECTION ( 'NONE',  ( 0.8445834565878902467, -0.5331027592246893043, -0.04980193736265902532 ) ) ;
#48269=FACE_OUTER_BOUND ( 'NONE', #9017, .T. ) ;
#48272=DIRECTION ( 'NONE',  ( -0.1961161351381831008, 1.073215590470984393E-15, -0.9805806756909204447 ) ) ;
#48284=CARTESIAN_POINT ( 'NONE',  ( 43.20303852803674971, -37.80742877201157626, -74.30445077681486055 ) ) ;
#48302=ORIENTED_EDGE ( 'NONE', *, *, #36134, .F. ) ;
#48305=AXIS2_PLACEMENT_3D ( 'NONE', #7535, #39244, #10954 ) ;
#48307=CARTESIAN_POINT ( 'NONE',  ( 15.63241099694714542, 18.38381172634125704, -83.24416995785023232 ) ) ;
#48309=CARTESIAN_POINT ( 'NONE',  ( 18.13393739769620083, -41.61618894467939356, -35.01561944896766221 ) ) ;
#48311=DIRECTION ( 'NONE',  ( 0.000000000000000000, 0.000000000000000000, -1.000000000000000000 ) ) ;
#48315=CARTESIAN_POINT ( 'NONE',  ( -0.2246626217552654958, -20.50318462115538765, -34.96184000430482541 ) ) ;
#48322=ORIENTED_EDGE ( 'NONE', *, *, #13025, .F. ) ;
#48323=CARTESIAN_POINT ( 'NONE',  ( -0.3016046179078940015, -10.91500322974829906, -35.02873218748179340 ) ) ;
#48330=ORIENTED_EDGE ( 'NONE', *, *, #13223, .F. ) ;
#48334=CYLINDRICAL_SURFACE ( 'NONE', #35670, 0.4999999999999990008 ) ;
#48335=DIRECTION ( 'NONE',  ( -1.000000000000000000, 0.000000000000000000, 0.000000000000000000 ) ) ;
#48351=AXIS2_PLACEMENT_3D ( 'NONE', #6360, #18659, #37813 ) ;
#48354=DIRECTION ( 'NONE',  ( -0.1961161351381840445, -2.837236618486509954E-16, -0.9805806756909201116 ) ) ;
#48359=CARTESIAN_POINT ( 'NONE',  ( 23.52343111712058032, -48.95118247924429511, -34.77532226276708371 ) ) ;
#48362=CARTESIAN_POINT ( 'NONE',  ( 43.68052723063104281, -39.92785622281377300, -68.20639724664832215 ) ) ;
#48366=CARTESIAN_POINT ( 'NONE',  ( 16.13393739769620083, -45.61618894467940066, -34.64999999999999858 ) ) ;
#48367=EDGE_CURVE ( 'NONE', #18539, #3226, #6178, .T. ) ;
#48371=EDGE_CURVE ( 'NONE', #8235, #39828, #42339, .T. ) ;
#48378=CARTESIAN_POINT ( 'NONE',  ( 23.34813653593170102, 18.05571844226370004, -34.65024031912469837 ) ) ;
#48381=CARTESIAN_POINT ( 'NONE',  ( 41.49123592270440497, 8.475614001362112404, -78.78653678967756946 ) ) ;
#48382=CARTESIAN_POINT ( 'NONE',  ( 0.2019507440921957664, -22.94509536330835786, -34.66067286864802099 ) ) ;
#48383=CARTESIAN_POINT ( 'NONE',  ( 31.39802437502155286, 4.622311496553142440, -84.65000000000000568 ) ) ;
#48384=CARTESIAN_POINT ( 'NONE',  ( 37.88393739769619373, -42.11618894467939356, -35.14999999999999858 ) ) ;
#48390=PLANE ( 'NONE',  #40361 ) ;
#48395=ORIENTED_EDGE ( 'NONE', *, *, #5169, .F. ) ;
#48396=EDGE_CURVE ( 'NONE', #18232, #36393, #16776, .T. ) ;
#48399=CARTESIAN_POINT ( 'NONE',  ( 13.13393739769600010, 18.38381105532060289, -83.01107220193038927 ) ) ;
#48401=EDGE_CURVE ( 'NONE', #46428, #51503, #15912, .T. ) ;
#48416=CARTESIAN_POINT ( 'NONE',  ( -0.1295185695944109927, -31.87964491196989414, -59.64999999999999147 ) ) ;
#48437=ORIENTED_EDGE ( 'NONE', *, *, #42229, .T. ) ;
#48439=VERTEX_POINT ( 'NONE', #17960 ) ;
#48440=CARTESIAN_POINT ( 'NONE',  ( 2.470463535281291367, -5.638681249711038568, -34.75586992539663811 ) ) ;
#48459=VECTOR ( 'NONE', #9152, 1000.000000000000000 ) ;
#48463=CARTESIAN_POINT ( 'NONE',  ( 40.00893739769619373, -16.26570799751769769, -35.14999999999999858 ) ) ;
#48468=( BOUNDED_CURVE ( )  B_SPLINE_CURVE ( 3, ( #1673, #21831, #7416, #3225 ),
 .UNSPECIFIED., .F., .T. ) 
 B_SPLINE_CURVE_WITH_KNOTS ( ( 4, 4 ),
 ( 5.070260775219133542, 5.428132570053642247 ),
 .UNSPECIFIED. ) 
 CURVE ( )  GEOMETRIC_REPRESENTATION_ITEM ( )  RATIONAL_B_SPLINE_CURVE ( ( 1.000000000000000000, 0.9893557610490317789, 0.9893557610490317789, 1.000000000000000000 ) ) 
 REPRESENTATION_ITEM ( '' )  );
#48481=DIRECTION ( 'NONE',  ( -0.5000000000000003331, -0.8660254037844384856, 0.000000000000000000 ) ) ;
#48487=CARTESIAN_POINT ( 'NONE',  ( 0.1457841021255935343, -15.61618894467929941, -34.68167779225149161 ) ) ;
#48489=CARTESIAN_POINT ( 'NONE',  ( 15.26510710965380113, -49.61613877435842568, -83.22678919103138639 ) ) ;
#48490=LINE ( 'NONE', #41657, #975 ) ;
#48511=ORIENTED_EDGE ( 'NONE', *, *, #36959, .F. ) ;
#48518=DIRECTION ( 'NONE',  ( -0.7071067811865475727, 0.000000000000000000, 0.7071067811865475727 ) ) ;
#48522=ORIENTED_EDGE ( 'NONE', *, *, #20200, .T. ) ;
#48527=EDGE_CURVE ( 'NONE', #33944, #12367, #12690, .T. ) ;
#48530=DIRECTION ( 'NONE',  ( 0.000000000000000000, -1.000000000000000000, 0.000000000000000000 ) ) ;
#48533=DIRECTION ( 'NONE',  ( 3.302498000000000159E-18, -1.533299999999999999E-17, -1.000000000000000000 ) ) ;
#48541=CARTESIAN_POINT ( 'NONE',  ( 42.62079769550818042, -37.72101637537727470, -77.21563321993323825 ) ) ;
#48559=CARTESIAN_POINT ( 'NONE',  ( 16.13393739769620083, -15.61618894467929941, -35.12503119152809461 ) ) ;
#48568=DIRECTION ( 'NONE',  ( 0.000000000000000000, 0.000000000000000000, 1.000000000000000000 ) ) ;
#48569=AXIS2_PLACEMENT_3D ( 'NONE', #12689, #21558, #37042 ) ;
#48575=CARTESIAN_POINT ( 'NONE',  ( 20.63393739769620083, -41.61618894467930119, -34.64999999999999858 ) ) ;
#48592=EDGE_LOOP ( 'NONE', ( #41247, #12754, #28982, #33720, #41551, #44489, #3279, #4118 ) ) ;
#48593=ORIENTED_EDGE ( 'NONE', *, *, #10787, .T. ) ;
#48600=ORIENTED_EDGE ( 'NONE', *, *, #49341, .F. ) ;
#48601=ORIENTED_EDGE ( 'NONE', *, *, #6621, .T. ) ;
#48605=CARTESIAN_POINT ( 'NONE',  ( 14.63393739769640156, 10.88381105532070059, -34.64999999999999858 ) ) ;
#48610=DIRECTION ( 'NONE',  ( 0.9083627212242635363, -0.3704194192529762786, -0.1940789028471121280 ) ) ;
#48623=ORIENTED_EDGE ( 'NONE', *, *, #9876, .T. ) ;
#48625=CARTESIAN_POINT ( 'NONE',  ( 23.37006864188879973, -49.24610395064770074, -34.65445009297679491 ) ) ;
#48628=CARTESIAN_POINT ( 'NONE',  ( 43.21150532606133510, -39.88589448485808475, -70.47653842715691042 ) ) ;
#48647=CARTESIAN_POINT ( 'NONE',  ( 42.13187174340301766, 8.546205365918842389, -75.69530005827525088 ) ) ;
#48648=CARTESIAN_POINT ( 'NONE',  ( 44.66545912666861540, -33.16365024224258917, -44.73623550635601731 ) ) ;
#48656=VERTEX_POINT ( 'NONE', #3989 ) ;
#48657=DIRECTION ( 'NONE',  ( 0.000000000000000000, 0.000000000000000000, 1.000000000000000000 ) ) ;
#48661=ORIENTED_EDGE ( 'NONE', *, *, #25274, .T. ) ;
#48662=ORIENTED_EDGE ( 'NONE', *, *, #45668, .F. ) ;
#48663=LINE ( 'NONE', #40020, #2520 ) ;
#48664=DIRECTION ( 'NONE',  ( -0.000000000000000000, 1.000000000000000000, 0.000000000000000000 ) ) ;
#48668=CARTESIAN_POINT ( 'NONE',  ( 11.63393739769600010, 10.38381105532060111, -54.64999999999999858 ) ) ;
#48670=CARTESIAN_POINT ( 'NONE',  ( 25.43010376912519988, -1.113097814880039893, -35.14999999999999858 ) ) ;
#48694=CARTESIAN_POINT ( 'NONE',  ( 41.61626771661330082, -37.56081407618439982, -82.23834840541459812 ) ) ;
#48699=FACE_OUTER_BOUND ( 'NONE', #31801, .T. ) ;
#48707=DIRECTION ( 'NONE',  ( 0.000000000000000000, -0.7071067811865492381, 0.7071067811865457964 ) ) ;
#48708=CARTESIAN_POINT ( 'NONE',  ( 16.13393739769620083, -15.61618894467929941, -35.14999999999999858 ) ) ;
#48719=DIRECTION ( 'NONE',  ( 0.000000000000000000, -0.7071067811865466846, -0.7071067811865483499 ) ) ;
#48723=VECTOR ( 'NONE', #6758, 1000.000000000000000 ) ;
#48749=CARTESIAN_POINT ( 'NONE',  ( 47.13393739769619373, -38.94772025634554780, -54.35302954682959609 ) ) ;
#48750=EDGE_CURVE ( 'NONE', #43415, #26981, #39377, .T. ) ;
#48751=CARTESIAN_POINT ( 'NONE',  ( 29.13393739769619728, -4.468739684871080087, -35.14999999999999858 ) ) ;
#48753=AXIS2_PLACEMENT_3D ( 'NONE', #10453, #10192, #14634 ) ;
#48754=LINE ( 'NONE', #48487, #12702 ) ;
#48756=ADVANCED_FACE ( 'NONE', ( #23612 ), #40182, .F. ) ;
#48759=CARTESIAN_POINT ( 'NONE',  ( 0.4047412638265869833, -22.38804348994680282, -35.14999999999999858 ) ) ;
#48761=EDGE_CURVE ( 'NONE', #50288, #6764, #46903, .T. ) ;
#48764=ORIENTED_EDGE ( 'NONE', *, *, #30074, .T. ) ;
#48775=EDGE_LOOP ( 'NONE', ( #2254, #48623 ) ) ;
#48781=( BOUNDED_CURVE ( )  B_SPLINE_CURVE ( 3, ( #8792, #44688, #12208, #43919 ),
 .UNSPECIFIED., .F., .T. ) 
 B_SPLINE_CURVE_WITH_KNOTS ( ( 4, 4 ),
 ( 1.195525503939052436, 1.980923667336377703 ),
 .UNSPECIFIED. ) 
 CURVE ( )  GEOMETRIC_REPRESENTATION_ITEM ( )  RATIONAL_B_SPLINE_CURVE ( ( 1.000000000000000000, 0.9492530216742067761, 0.9492530216742067761, 1.000000000000000000 ) ) 
 REPRESENTATION_ITEM ( '' )  );
#48783=CARTESIAN_POINT ( 'NONE',  ( 46.94631559364368911, 7.984621261935255454, -34.75526898281330546 ) ) ;
#48798=VECTOR ( 'NONE', #17474, 1000.000000000000227 ) ;
#48803=EDGE_CURVE ( 'NONE', #51503, #15968, #20458, .T. ) ;
#48805=CARTESIAN_POINT ( 'NONE',  ( 43.03680859621228905, -37.78309590381571326, -75.13564474923592229 ) ) ;
#48814=CARTESIAN_POINT ( 'NONE',  ( 16.13393739769620083, -29.47259540523039689, -47.64999999999999858 ) ) ;
#48823=EDGE_CURVE ( 'NONE', #13190, #34524, #306, .T. ) ;
#48826=ORIENTED_EDGE ( 'NONE', *, *, #21347, .T. ) ;
#48832=FACE_OUTER_BOUND ( 'NONE', #32497, .T. ) ;
#48834=DIRECTION ( 'NONE',  ( 1.000000000000000000, 0.000000000000000000, 0.000000000000000000 ) ) ;
#48839=CARTESIAN_POINT ( 'NONE',  ( 46.25525774125586054, 2.762490711761019568, -54.56299356781535437 ) ) ;
#48845=CARTESIAN_POINT ( 'NONE',  ( 34.13393739769599478, 17.88381105532079829, -35.14999999999999858 ) ) ;
#48847=CYLINDRICAL_SURFACE ( 'NONE', #4195, 0.4999999999999994449 ) ;
#48849=EDGE_LOOP ( 'NONE', ( #34849, #3024, #5851, #1992, #39576, #45711, #5834, #3599 ) ) ;
#48852=ORIENTED_EDGE ( 'NONE', *, *, #37263, .T. ) ;
#48860=ORIENTED_EDGE ( 'NONE', *, *, #3260, .F. ) ;
#48863=ORIENTED_EDGE ( 'NONE', *, *, #3144, .T. ) ;
#48866=CARTESIAN_POINT ( 'NONE',  ( 19.28172483834588391, 18.60725077530870664, -82.44267625235052321 ) ) ;
#48873=DIRECTION ( 'NONE',  ( 0.000000000000000000, 0.000000000000000000, 1.000000000000000000 ) ) ;
#48876=DIRECTION ( 'NONE',  ( 0.000000000000000000, 1.000000000000000000, 0.000000000000000000 ) ) ;
#48892=ADVANCED_FACE ( 'NONE', ( #8691 ), #40395, .T. ) ;
#48894=CARTESIAN_POINT ( 'NONE',  ( 40.87754521028758603, -39.63528059274995741, -81.74477356559056318 ) ) ;
#48903=CARTESIAN_POINT ( 'NONE',  ( 14.63393739769620083, -42.11618894467930119, -34.64999999999999858 ) ) ;
#48913=CARTESIAN_POINT ( 'NONE',  ( 23.52343111712034585, 17.71880458988573892, -34.77532226276709793 ) ) ;
#48915=CARTESIAN_POINT ( 'NONE',  ( 43.98637686555271387, 8.721229771107395834, -66.72543627791436904 ) ) ;
#48923=ORIENTED_EDGE ( 'NONE', *, *, #51114, .F. ) ;
#48924=VERTEX_POINT ( 'NONE', #1079 ) ;
#48939=CARTESIAN_POINT ( 'NONE',  ( 8.900684698812471041, -48.14181044607449422, -48.24693240290979190 ) ) ;
#48941=CARTESIAN_POINT ( 'NONE',  ( 14.25914812751957506, -32.49681002921884954, -34.81767276520687915 ) ) ;
#48946=CARTESIAN_POINT ( 'NONE',  ( 14.13393739769640156, 10.38381105532060111, -35.14999999999999858 ) ) ;
#48974=CARTESIAN_POINT ( 'NONE',  ( 0.4142048468712421494, -22.38257968772852635, -35.10658870009286403 ) ) ;
#49014=B_SPLINE_CURVE_WITH_KNOTS ( 'NONE', 3,
 ( #37559, #9541, #5609, #21563 ),
 .UNSPECIFIED., .F., .F.,
 ( 4, 4 ),
 ( 0.000000000000000000, 1.000000000000000000 ),
 .UNSPECIFIED. ) ;
#49018=VERTEX_POINT ( 'NONE', #22011 ) ;
#49022=CARTESIAN_POINT ( 'NONE',  ( 28.63393739769619728, -4.678675331415849570, -34.64999999999999858 ) ) ;
#49026=CARTESIAN_POINT ( 'NONE',  ( 43.34618191712553426, -39.98291268152190980, -69.47739009628490692 ) ) ;
#49029=ORIENTED_EDGE ( 'NONE', *, *, #19205, .T. ) ;
#49043=ORIENTED_EDGE ( 'NONE', *, *, #30028, .F. ) ;
#49056=EDGE_LOOP ( 'NONE', ( #8818, #12198, #7164, #33211 ) ) ;
#49060=ORIENTED_EDGE ( 'NONE', *, *, #29699, .F. ) ;
#49063=CYLINDRICAL_SURFACE ( 'NONE', #9442, 0.4999999999999967248 ) ;
#49068=CARTESIAN_POINT ( 'NONE',  ( 41.69553807872770079, 6.341659931880261780, -81.84199659484330880 ) ) ;
#49072=AXIS2_PLACEMENT_3D ( 'NONE', #7382, #35921, #4211 ) ;
#49074=CARTESIAN_POINT ( 'NONE',  ( 43.17225766068933979, -37.80304688360283194, -74.45836467289994687 ) ) ;
#49075=ADVANCED_FACE ( 'NONE', ( #37626 ), #49699, .T. ) ;
#49084=LINE ( 'NONE', #9249, #51588 ) ;
#49086=ORIENTED_EDGE ( 'NONE', *, *, #9506, .T. ) ;
#49087=AXIS2_PLACEMENT_3D ( 'NONE', #46511, #7436, #19477 ) ;
#49089=( GEOMETRIC_REPRESENTATION_CONTEXT ( 3 ) GLOBAL_UNCERTAINTY_ASSIGNED_CONTEXT ( ( #12203 ) ) GLOBAL_UNIT_ASSIGNED_CONTEXT ( ( #16920, #32603, #44431 ) ) REPRESENTATION_CONTEXT ( 'NONE', 'WORKASPACE' ) );
#49095=( BOUNDED_CURVE ( )  B_SPLINE_CURVE ( 3, ( #51680, #35696, #31728, #43816 ),
 .UNSPECIFIED., .F., .T. ) 
 B_SPLINE_CURVE_WITH_KNOTS ( ( 4, 4 ),
 ( 3.744786642406928934, 4.166152881452140022 ),
 .UNSPECIFIED. ) 
 CURVE ( )  GEOMETRIC_REPRESENTATION_ITEM ( )  RATIONAL_B_SPLINE_CURVE ( ( 1.000000000000000000, 0.9852588556718586688, 0.9852588556718586688, 1.000000000000000000 ) ) 
 REPRESENTATION_ITEM ( '' )  );
#49098=VECTOR ( 'NONE', #27346, 1000.000000000000000 ) ;
#49101=DIRECTION ( 'NONE',  ( -0.3863301728269311619, 0.9223605572461961444, 1.110223024625156171E-16 ) ) ;
#49103=PLANE ( 'NONE',  #5186 ) ;
#49109=ADVANCED_FACE ( 'NONE', ( #1732 ), #45243, .T. ) ;
#49113=VERTEX_POINT ( 'NONE', #49954 ) ;
#49114=DIRECTION ( 'NONE',  ( 0.000000000000000000, 0.000000000000000000, -1.000000000000000000 ) ) ;
#49122=ORIENTED_EDGE ( 'NONE', *, *, #14901, .F. ) ;
#49138=ADVANCED_FACE ( 'NONE', ( #21888 ), #1990, .T. ) ;
#49145=EDGE_CURVE ( 'NONE', #31736, #29987, #32666, .T. ) ;
#49148=CARTESIAN_POINT ( 'NONE',  ( 16.13393739769620083, -15.61618894467929941, -643.2998782751060389 ) ) ;
#49156=FACE_OUTER_BOUND ( 'NONE', #41745, .T. ) ;
#49173=CARTESIAN_POINT ( 'NONE',  ( -0.02466850413057549915, -50.78713108147470479, -34.78792709637806979 ) ) ;
#49175=DIRECTION ( 'NONE',  ( 0.000000000000000000, 0.000000000000000000, -1.000000000000000000 ) ) ;
#49177=CARTESIAN_POINT ( 'NONE',  ( 45.15723187293362884, 8.809242139076280509, -61.04885190864924027 ) ) ;
#49179=ADVANCED_FACE ( 'NONE', ( #26594 ), #1733, .F. ) ;
#49181=CARTESIAN_POINT ( 'NONE',  ( 18.13393739769619728, -45.61618894467940066, -62.64999999999999858 ) ) ;
#49182=EDGE_LOOP ( 'NONE', ( #4698, #35821, #4896, #11529 ) ) ;
#49184=ORIENTED_EDGE ( 'NONE', *, *, #39577, .T. ) ;
#49188=ORIENTED_EDGE ( 'NONE', *, *, #7281, .F. ) ;
#49190=DIRECTION ( 'NONE',  ( 0.000000000000000000, 0.000000000000000000, 1.000000000000000000 ) ) ;
#49193=CARTESIAN_POINT ( 'NONE',  ( 30.13393739769619728, 7.383811055320659733, -84.65000000000000568 ) ) ;
#49197=ORIENTED_EDGE ( 'NONE', *, *, #51572, .F. ) ;
#49198=CARTESIAN_POINT ( 'NONE',  ( 33.38393739769599478, 10.88381105532080007, -35.14999999999999858 ) ) ;
#49207=LINE ( 'NONE', #28220, #27372 ) ;
#49222=CARTESIAN_POINT ( 'NONE',  ( 20.30127474080329719, 10.88381105532070059, -34.64999999999999858 ) ) ;
#49224=VECTOR ( 'NONE', #5529, 1000.000000000000114 ) ;
#49237=EDGE_CURVE ( 'NONE', #1956, #35078, #27646, .T. ) ;
#49249=CARTESIAN_POINT ( 'NONE',  ( -10.06940692381879821, -44.95898322470259956, -43.89473864311649720 ) ) ;
#49254=CARTESIAN_POINT ( 'NONE',  ( 26.93010376912529935, -27.85143120648099924, -35.14999999999999858 ) ) ;
#49271=EDGE_CURVE ( 'NONE', #40950, #41828, #12625, .T. ) ;
#49280=FACE_OUTER_BOUND ( 'NONE', #29540, .T. ) ;
#49284=CARTESIAN_POINT ( 'NONE',  ( 46.36052476518712240, -40.25801055237913317, -54.62947754013732293 ) ) ;
#49300=DIRECTION ( 'NONE',  ( 0.000000000000000000, 0.000000000000000000, 1.000000000000000000 ) ) ;
#49303=VECTOR ( 'NONE', #5843, 1000.000000000000000 ) ;
#49311=CARTESIAN_POINT ( 'NONE',  ( 46.67317881810770075, 7.891852522694349226, -34.65023821785899116 ) ) ;
#49316=VERTEX_POINT ( 'NONE', #23172 ) ;
#49319=ORIENTED_EDGE ( 'NONE', *, *, #9279, .F. ) ;
#49325=DIRECTION ( 'NONE',  ( 0.000000000000000000, 0.000000000000000000, 1.000000000000000000 ) ) ;
#49330=CARTESIAN_POINT ( 'NONE',  ( 42.72898525104111656, -37.73742736476912540, -76.67469147134403329 ) ) ;
#49335=AXIS2_PLACEMENT_3D ( 'NONE', #30762, #22381, #26049 ) ;
#49337=CIRCLE ( 'NONE', #45167, 33.00000000000000000 ) ;
#49339=CONICAL_SURFACE ( 'NONE', #26708, 3.567506086244481622, 0.04995839572194331335 ) ;
#49341=EDGE_CURVE ( 'NONE', #3841, #46513, #34279, .T. ) ;
#49367=AXIS2_PLACEMENT_3D ( 'NONE', #17090, #49325, #25437 ) ;
#49370=ORIENTED_EDGE ( 'NONE', *, *, #29343, .F. ) ;
#49373=DIRECTION ( 'NONE',  ( -0.8660254037844384856, 0.5000000000000003331, 0.000000000000000000 ) ) ;
#49392=LINE ( 'NONE', #37322, #37991 ) ;
#49397=CARTESIAN_POINT ( 'NONE',  ( 46.63393739769619373, 4.883811055320659733, -35.14999999999999858 ) ) ;
#49399=ADVANCED_FACE ( 'NONE', ( #40464 ), #8434, .T. ) ;
#49402=CARTESIAN_POINT ( 'NONE',  ( -7.043336953760312547, -0.4477742326702461861, -84.65000000000000568 ) ) ;
#49404=VECTOR ( 'NONE', #15526, 1000.000000000000000 ) ;
#49411=CARTESIAN_POINT ( 'NONE',  ( -0.007164427059776000244, -27.04615419348650107, -34.77269723891829756 ) ) ;
#49415=EDGE_CURVE ( 'NONE', #17858, #31052, #1168, .T. ) ;
#49422=EDGE_CURVE ( 'NONE', #23002, #25882, #18760, .T. ) ;
#49428=CARTESIAN_POINT ( 'NONE',  ( -0.03888451113519723890, -50.92360554050903687, -34.84227938466554519 ) ) ;
#49432=CARTESIAN_POINT ( 'NONE',  ( 43.28072419627158496, 8.659894295519814378, -70.14142403610232179 ) ) ;
#49435=CARTESIAN_POINT ( 'NONE',  ( 10.13393739769619906, -54.15188668067469990, -35.14999999999999858 ) ) ;
#49437=ORIENTED_EDGE ( 'NONE', *, *, #13021, .F. ) ;
#49447=AXIS2_PLACEMENT_3D ( 'NONE', #44275, #12068, #3945 ) ;
#49451=CARTESIAN_POINT ( 'NONE',  ( 13.61748873513634095, 18.38375039377714515, -83.08753104980289095 ) ) ;
#49453=FACE_OUTER_BOUND ( 'NONE', #51555, .T. ) ;
#49468=CARTESIAN_POINT ( 'NONE',  ( 46.93104535293870327, 8.311849618651319105, -54.22205626569730441 ) ) ;
#49476=AXIS2_PLACEMENT_3D ( 'NONE', #17687, #5895, #29469 ) ;
#49482=CARTESIAN_POINT ( 'NONE',  ( 23.62413055734869971, -48.75525398023999912, -35.14999999999999858 ) ) ;
#49491=DIRECTION ( 'NONE',  ( -0.8660254037844390407, -0.4999999999999995004, -5.551115123125774074E-17 ) ) ;
#49499=VERTEX_POINT ( 'NONE', #17810 ) ;
#49502=DIRECTION ( 'NONE',  ( 0.000000000000000000, 0.000000000000000000, -1.000000000000000000 ) ) ;
#49506=CARTESIAN_POINT ( 'NONE',  ( -22.72492714007710291, -11.78847082558010051, -54.75782564465809088 ) ) ;
#49515=CIRCLE ( 'NONE', #49552, 5.251829701412240148 ) ;
#49516=DIRECTION ( 'NONE',  ( 0.000000000000000000, 0.000000000000000000, -1.000000000000000000 ) ) ;
#49518=LINE ( 'NONE', #13609, #8435 ) ;
#49523=EDGE_CURVE ( 'NONE', #50974, #621, #18445, .T. ) ;
#49537=CARTESIAN_POINT ( 'NONE',  ( 29.00424600244190287, -4.540411172299108955, -34.81403640487199880 ) ) ;
#49538=ADVANCED_FACE ( 'NONE', ( #4994 ), #1055, .T. ) ;
#49543=CARTESIAN_POINT ( 'NONE',  ( 41.64150979412020348, -37.55586782839380788, -82.11206661960329711 ) ) ;
#49549=CONICAL_SURFACE ( 'NONE', #13556, 19.50000000000000000, 0.2449786631268651149 ) ;
#49552=AXIS2_PLACEMENT_3D ( 'NONE', #38688, #11674, #11159 ) ;
#49559=CARTESIAN_POINT ( 'NONE',  ( 28.98356459125599827, -26.68429298316319986, -34.79124076679859456 ) ) ;
#49573=PLANE ( 'NONE',  #34298 ) ;
#49580=EDGE_LOOP ( 'NONE', ( #11692, #36458, #11208, #42741 ) ) ;
#49581=DIRECTION ( 'NONE',  ( -1.000000000000000000, 0.000000000000000000, 0.000000000000000000 ) ) ;
#49585=ORIENTED_EDGE ( 'NONE', *, *, #5103, .T. ) ;
#49587=CARTESIAN_POINT ( 'NONE',  ( -0.1295185695942999982, 0.6472670226113349523, -84.65000000000000568 ) ) ;
#49591=CARTESIAN_POINT ( 'NONE',  ( 45.05991202527755490, -38.04955529247586554, -65.02012688996633472 ) ) ;
#49593=ADVANCED_FACE ( 'NONE', ( #2346 ), #35075, .T. ) ;
#49598=AXIS2_PLACEMENT_3D ( 'NONE', #7700, #19977, #12389 ) ;
#49600=ADVANCED_FACE ( 'NONE', ( #46392 ), #30111, .T. ) ;
#49635=CARTESIAN_POINT ( 'NONE',  ( 19.64758755231450849, -22.86272695187545168, -34.79644660940672907 ) ) ;
#49638=ORIENTED_EDGE ( 'NONE', *, *, #25127, .T. ) ;
#49648=CARTESIAN_POINT ( 'NONE',  ( 45.48191705218061998, 6.865434676292834659, -62.91004931326258998 ) ) ;
#49649=ORIENTED_EDGE ( 'NONE', *, *, #50994, .F. ) ;
#49661=DIRECTION ( 'NONE',  ( -0.7071067811865475727, 0.000000000000000000, 0.7071067811865475727 ) ) ;
#49663=CIRCLE ( 'NONE', #30358, 0.5000000000000004441 ) ;
#49667=ORIENTED_EDGE ( 'NONE', *, *, #36989, .T. ) ;
#49679=CARTESIAN_POINT ( 'NONE',  ( 16.13393739769620083, -1.337601509563455471, -34.64999999999999858 ) ) ;
#49687=CARTESIAN_POINT ( 'NONE',  ( 43.90603104686010738, 8.714656956882279815, -67.11423799122562173 ) ) ;
#49689=CARTESIAN_POINT ( 'NONE',  ( 18.11497263573659922, 5.664030231104960400, -35.14999999999999858 ) ) ;
#49694=VERTEX_POINT ( 'NONE', #12276 ) ;
#49695=CARTESIAN_POINT ( 'NONE',  ( -22.84744350781432587, -16.08730834640482854, -54.74874053947917929 ) ) ;
#49697=CARTESIAN_POINT ( 'NONE',  ( 16.13393739769620083, -15.61618894467929941, -35.14999999999999858 ) ) ;
#49699=CYLINDRICAL_SURFACE ( 'NONE', #51121, 0.5000000000000006661 ) ;
#49707=ORIENTED_EDGE ( 'NONE', *, *, #50464, .F. ) ;
#49708=CARTESIAN_POINT ( 'NONE',  ( 0.2602139982833864273, -46.15174389846320224, -34.65037388166341259 ) ) ;
#49712=ADVANCED_FACE ( 'NONE', ( #3646 ), #19618, .T. ) ;
#49714=TOROIDAL_SURFACE ( 'NONE', #32083, 16.60961179679779676, 0.5000000000000000000 ) ;
#49719=DIRECTION ( 'NONE',  ( 1.000000000000000000, 0.000000000000000000, 0.000000000000000000 ) ) ;
#49723=ORIENTED_EDGE ( 'NONE', *, *, #26436, .F. ) ;
#49744=DIRECTION ( 'NONE',  ( 3.302498000000000159E-18, -1.533299999999999999E-17, -1.000000000000000000 ) ) ;
#49758=CARTESIAN_POINT ( 'NONE',  ( -22.79226920359159791, -18.53556694150880091, -54.60327039117859727 ) ) ;
#49765=ORIENTED_EDGE ( 'NONE', *, *, #5257, .T. ) ;
#49768=ORIENTED_EDGE ( 'NONE', *, *, #44655, .F. ) ;
#49769=DIRECTION ( 'NONE',  ( 0.000000000000000000, 0.000000000000000000, 1.000000000000000000 ) ) ;
#49774=ADVANCED_FACE ( 'NONE', ( #31647 ), #13370, .T. ) ;
#49787=CARTESIAN_POINT ( 'NONE',  ( 28.88047141014009966, -4.586426805731299794, -34.71367995918279092 ) ) ;
#49788=B_SPLINE_CURVE_WITH_KNOTS ( 'NONE', 3,
 ( #23009, #43218, #19292, #47096, #23453, #23841, #11576, #31969, #19679, #7381 ),
 .UNSPECIFIED., .F., .F.,
 ( 4, 2, 2, 2, 4 ),
 ( 0.1272047750342873151, 0.1420319546165290103, 0.1570382458071080123, 0.1723372614072689879, 0.1727139781532890106 ),
 .UNSPECIFIED. ) ;
#49790=CARTESIAN_POINT ( 'NONE',  ( -5.194501806656489862, 17.26952857224580384, -39.31824944736199967 ) ) ;
#49792=CARTESIAN_POINT ( 'NONE',  ( 43.93040869676359961, -39.07135447434988862, -70.79477508826258259 ) ) ;
#49795=CARTESIAN_POINT ( 'NONE',  ( 47.13393739769619373, -15.61618894467929941, -54.64999999999999858 ) ) ;
#49800=CARTESIAN_POINT ( 'NONE',  ( 44.28490121901400300, 8.836964955981793324, -64.90668349608083076 ) ) ;
#49801=CARTESIAN_POINT ( 'NONE',  ( 0.3209249304026220440, -50.71887597443840434, -34.64999999999999858 ) ) ;
#49804=CARTESIAN_POINT ( 'NONE',  ( 29.11900864776890074, -26.73446727828369873, -35.02873218748179340 ) ) ;
#49810=ADVANCED_FACE ( 'NONE', ( #12028 ), #37635, .T. ) ;
#49825=ORIENTED_EDGE ( 'NONE', *, *, #22032, .T. ) ;
#49826=VECTOR ( 'NONE', #45778, 1000.000000000000000 ) ;
#49836=CARTESIAN_POINT ( 'NONE',  ( -3.839728563314090071, -24.83858928721370063, -54.64999999999999858 ) ) ;
#49839=CARTESIAN_POINT ( 'NONE',  ( 0.1457840918194806823, -20.72567761198500591, -34.68167776469320529 ) ) ;
#49841=CARTESIAN_POINT ( 'NONE',  ( 45.73379805818350974, -38.12522060878801256, -61.65069626971402528 ) ) ;
#49853=ADVANCED_FACE ( 'NONE', ( #723 ), #4925, .T. ) ;
#49861=CARTESIAN_POINT ( 'NONE',  ( 41.50874094001223114, -39.70998512007497538, -78.70214816491434817 ) ) ;
#49877=DIRECTION ( 'NONE',  ( 1.000000000000000000, 0.000000000000000000, 0.000000000000000000 ) ) ;
#49878=EDGE_LOOP ( 'NONE', ( #39501, #24241, #28392, #20665 ) ) ;
#49883=EDGE_CURVE ( 'NONE', #14340, #40830, #15500, .T. ) ;
#49888=ORIENTED_EDGE ( 'NONE', *, *, #265, .F. ) ;
#49891=ORIENTED_EDGE ( 'NONE', *, *, #13669, .T. ) ;
#49896=EDGE_LOOP ( 'NONE', ( #13076, #33764, #11983, #3291 ) ) ;
#49897=CARTESIAN_POINT ( 'NONE',  ( 45.80601968430718074, 6.900823852999605990, -61.28958453903135251 ) ) ;
#49898=ORIENTED_EDGE ( 'NONE', *, *, #46017, .F. ) ;
#49900=CIRCLE ( 'NONE', #23124, 17.09468304687049667 ) ;
#49918=EDGE_CURVE ( 'NONE', #11156, #14039, #40148, .T. ) ;
#49920=CARTESIAN_POINT ( 'NONE',  ( 47.13393739769619373, -36.11618894467930119, -54.64999999999999858 ) ) ;
#49938=VERTEX_POINT ( 'NONE', #49985 ) ;
#49940=CARTESIAN_POINT ( 'NONE',  ( 17.98749078828957337, 10.53025766472752522, -34.79644660940672907 ) ) ;
#49943=CARTESIAN_POINT ( 'NONE',  ( 43.60551842263911482, 8.688893774213322985, -68.56980346353216760 ) ) ;
#49946=LINE ( 'NONE', #1982, #23580 ) ;
#49947=ADVANCED_FACE ( 'NONE', ( #46062 ), #5961, .T. ) ;
#49950=ORIENTED_EDGE ( 'NONE', *, *, #28704, .T. ) ;
#49953=DIRECTION ( 'NONE',  ( 0.000000000000000000, 0.000000000000000000, -1.000000000000000000 ) ) ;
#49954=CARTESIAN_POINT ( 'NONE',  ( 18.11900864776890074, -32.59522544870679894, -35.02873218748179340 ) ) ;
#49957=EDGE_LOOP ( 'NONE', ( #6899, #32366 ) ) ;
#49962=DIRECTION ( 'NONE',  ( 0.05886216378194202015, 0.000000000000000000, 0.9982661196669493364 ) ) ;
#49967=CARTESIAN_POINT ( 'NONE',  ( 2.422700639432810110, -5.409992334431690253, -35.02127583263639821 ) ) ;
#49985=CARTESIAN_POINT ( 'NONE',  ( 2.458146360389370511, -25.65221394861527671, -34.79644291222910368 ) ) ;
#49987=ORIENTED_EDGE ( 'NONE', *, *, #13250, .F. ) ;
#49992=AXIS2_PLACEMENT_3D ( 'NONE', #20179, #8657, #40113 ) ;
#50008=DIRECTION ( 'NONE',  ( 1.000000000000000000, 0.000000000000000000, 0.000000000000000000 ) ) ;
#50012=CARTESIAN_POINT ( 'NONE',  ( -10.12945549441239912, -44.87173451821930570, -43.73795196952299591 ) ) ;
#50018=ORIENTED_EDGE ( 'NONE', *, *, #27493, .T. ) ;
#50023=CARTESIAN_POINT ( 'NONE',  ( 11.63393739769619906, -41.61618894467930119, -54.64999999999999858 ) ) ;
#50032=VECTOR ( 'NONE', #12970, 1000.000000000000000 ) ;
#50035=VERTEX_POINT ( 'NONE', #19552 ) ;
#50042=DIRECTION ( 'NONE',  ( 0.000000000000000000, 0.000000000000000000, -1.000000000000000000 ) ) ;
#50044=CARTESIAN_POINT ( 'NONE',  ( -5.166791919687259593, 17.14663772333980063, -39.25848487190110347 ) ) ;
#50046=CARTESIAN_POINT ( 'NONE',  ( 47.72980687449361881, -39.38200829285558058, -51.96765182151883522 ) ) ;
#50053=CARTESIAN_POINT ( 'NONE',  ( 41.96502951575018159, 8.570278285162954646, -76.32785687310233413 ) ) ;
#50075=VERTEX_POINT ( 'NONE', #40247 ) ;
#50079=CARTESIAN_POINT ( 'NONE',  ( 3.768317948728551858, -8.476895227121387322, -34.64999999999999858 ) ) ;
#50084=LINE ( 'NONE', #34335, #15729 ) ;
#50086=LINE ( 'NONE', #33823, #50261 ) ;
#50090=CARTESIAN_POINT ( 'NONE',  ( 45.26653699117287033, -38.07366123800876068, -63.98696205713867613 ) ) ;
#50104=AXIS2_PLACEMENT_3D ( 'NONE', #29957, #46244, #45975 ) ;
#50113=CARTESIAN_POINT ( 'NONE',  ( 14.13958958332026583, -32.60348064536626111, -35.06583844469490430 ) ) ;
#50115=ORIENTED_EDGE ( 'NONE', *, *, #10663, .F. ) ;
#50116=CARTESIAN_POINT ( 'NONE',  ( 29.13393739769619728, -33.99486860111965569, -83.77132034355965118 ) ) ;
#50123=DIRECTION ( 'NONE',  ( 0.000000000000000000, -1.000000000000000000, 0.000000000000000000 ) ) ;
#50131=FACE_OUTER_BOUND ( 'NONE', #12836, .T. ) ;
#50132=DIRECTION ( 'NONE',  ( -0.3535533905932731202, -0.6123724356957964687, 0.7071067811865462405 ) ) ;
#50144=CARTESIAN_POINT ( 'NONE',  ( 4.133937397696209715, -8.687985714403829718, -35.14999999999999858 ) ) ;
#50150=CARTESIAN_POINT ( 'NONE',  ( 47.13393739769619373, 7.029298498933709283, -54.64999999999999858 ) ) ;
#50165=CYLINDRICAL_SURFACE ( 'NONE', #20007, 0.4999999999999982236 ) ;
#50169=ADVANCED_FACE ( 'NONE', ( #1709 ), #18489, .F. ) ;
#50179=CARTESIAN_POINT ( 'NONE',  ( 16.81199894099719927, -16.95676073769629610, -35.14999999999999858 ) ) ;
#50184=AXIS2_PLACEMENT_3D ( 'NONE', #21861, #29470, #1446 ) ;
#50188=CARTESIAN_POINT ( 'NONE',  ( 19.97369125467840334, -22.99931529436689814, -35.14999999999999858 ) ) ;
#50190=DIRECTION ( 'NONE',  ( 0.6339889056055382222, 0.000000000000000000, -0.7733421413379021336 ) ) ;
#50200=CARTESIAN_POINT ( 'NONE',  ( 45.68005094484422557, 8.842359151983487209, -58.51315632734830530 ) ) ;
#50203=VERTEX_POINT ( 'NONE', #33662 ) ;
#50212=CYLINDRICAL_SURFACE ( 'NONE', #39451, 2.999999999999999112 ) ;
#50216=CIRCLE ( 'NONE', #10033, 5.251829701412240148 ) ;
#50227=AXIS2_PLACEMENT_3D ( 'NONE', #33229, #18280, #21682 ) ;
#50235=ADVANCED_FACE ( 'NONE', ( #14538 ), #1969, .T. ) ;
#50236=ORIENTED_EDGE ( 'NONE', *, *, #917, .F. ) ;
#50239=CARTESIAN_POINT ( 'NONE',  ( 45.41582150454148348, -40.05831117691089815, -59.79522137358304690 ) ) ;
#50248=( GEOMETRIC_REPRESENTATION_CONTEXT ( 3 ) GLOBAL_UNCERTAINTY_ASSIGNED_CONTEXT ( ( #42636 ) ) GLOBAL_UNIT_ASSIGNED_CONTEXT ( ( #11360, #11618, #27071 ) ) REPRESENTATION_CONTEXT ( 'NONE', 'WORKASPACE' ) );
#50255=DIRECTION ( 'NONE',  ( 1.000000000000000000, 0.000000000000000000, 0.000000000000000000 ) ) ;
#50261=VECTOR ( 'NONE', #26218, 1000.000000000000000 ) ;
#50262=LINE ( 'NONE', #42656, #6144 ) ;
#50266=VERTEX_POINT ( 'NONE', #34699 ) ;
#50277=CARTESIAN_POINT ( 'NONE',  ( -22.85259296468129975, -18.54880656488629853, -54.73566662495469615 ) ) ;
#50288=VERTEX_POINT ( 'NONE', #27356 ) ;
#50300=CYLINDRICAL_SURFACE ( 'NONE', #45720, 0.4999999999999991118 ) ;
#50302=EDGE_CURVE ( 'NONE', #25155, #2299, #2596, .T. ) ;
#50309=DIRECTION ( 'NONE',  ( 0.000000000000000000, 0.000000000000000000, -1.000000000000000000 ) ) ;
#50311=CARTESIAN_POINT ( 'NONE',  ( -18.33921323110770274, 3.183518156266269994, -50.99327864761959717 ) ) ;
#50313=CARTESIAN_POINT ( 'NONE',  ( 45.78987214702719655, -39.24112996349171567, -61.59531111407024895 ) ) ;
#50319=CARTESIAN_POINT ( 'NONE',  ( 45.91115938045514611, 8.982369621444501462, -56.88730701422755942 ) ) ;
#50324=CARTESIAN_POINT ( 'NONE',  ( 28.63710131890649890, -26.55489129076070043, -34.65001001049759566 ) ) ;
#50331=DIRECTION ( 'NONE',  ( 0.000000000000000000, 1.000000000000000000, 0.000000000000000000 ) ) ;
#50337=CIRCLE ( 'NONE', #13525, 38.49999999999999289 ) ;
#50347=DIRECTION ( 'NONE',  ( 1.000000000000000000, 0.000000000000000000, 0.000000000000000000 ) ) ;
#50350=ORIENTED_EDGE ( 'NONE', *, *, #38935, .T. ) ;
#50351=DIRECTION ( 'NONE',  ( 0.000000000000000000, 0.000000000000000000, 1.000000000000000000 ) ) ;
#50354=CARTESIAN_POINT ( 'NONE',  ( 17.98749448546710994, -32.47778390180250341, -34.79644291222910368 ) ) ;
#50356=CARTESIAN_POINT ( 'NONE',  ( 18.13393739769639978, 10.38381105532070059, -54.64999999999999858 ) ) ;
#50357=CARTESIAN_POINT ( 'NONE',  ( 44.70043142015700965, -38.00651179226034060, -66.81746990982490786 ) ) ;
#50365=ADVANCED_FACE ( 'NONE', ( #26099 ), #38957, .T. ) ;
#50378=CARTESIAN_POINT ( 'NONE',  ( 41.16162958179530307, -39.66950744282151931, -80.37574497360704129 ) ) ;
#50385=CARTESIAN_POINT ( 'NONE',  ( 11.63393739769619906, -41.61618894467930119, -54.64999999999999858 ) ) ;
#50391=CARTESIAN_POINT ( 'NONE',  ( 8.731180243531472485, 17.69319178430564321, -34.79644561402098191 ) ) ;
#50417=CARTESIAN_POINT ( 'NONE',  ( 45.11614098616555424, 6.824003222330928153, -64.73897788473527726 ) ) ;
#50418=CARTESIAN_POINT ( 'NONE',  ( 19.97369125467840334, -22.99931529436689814, -35.14999999999999858 ) ) ;
#50419=VERTEX_POINT ( 'NONE', #6209 ) ;
#50423=DIRECTION ( 'NONE',  ( 0.6339889056055382222, 0.000000000000000000, -0.7733421413379021336 ) ) ;
#50457=CARTESIAN_POINT ( 'NONE',  ( 44.13393739769620083, -36.11618894467930119, -44.64999999999999858 ) ) ;
#50459=CARTESIAN_POINT ( 'NONE',  ( 45.65335366086122093, 8.840693443015325670, -58.64289655873446350 ) ) ;
#50464=EDGE_CURVE ( 'NONE', #51808, #16602, #42192, .T. ) ;
#50466=DIRECTION ( 'NONE',  ( 0.000000000000000000, 0.000000000000000000, -1.000000000000000000 ) ) ;
#50468=( BOUNDED_CURVE ( )  B_SPLINE_CURVE ( 3, ( #34338, #38036, #14439, #6326 ),
 .UNSPECIFIED., .F., .T. ) 
 B_SPLINE_CURVE_WITH_KNOTS ( ( 4, 4 ),
 ( 5.070260775219134430, 5.428132570053640471 ),
 .UNSPECIFIED. ) 
 CURVE ( )  GEOMETRIC_REPRESENTATION_ITEM ( )  RATIONAL_B_SPLINE_CURVE ( ( 1.000000000000000000, 0.9893557610490320009, 0.9893557610490320009, 1.000000000000000000 ) ) 
 REPRESENTATION_ITEM ( '' )  );
#50472=EDGE_CURVE ( 'NONE', #38446, #13016, #46051, .T. ) ;
#50477=ORIENTED_EDGE ( 'NONE', *, *, #2977, .T. ) ;
#50495=CARTESIAN_POINT ( 'NONE',  ( 45.41861909476764225, -40.05849041370392172, -59.78164571485964984 ) ) ;
#50497=DIRECTION ( 'NONE',  ( -0.3502816565540492477, 0.000000000000000000, 0.9366444154970182678 ) ) ;
#50509=ORIENTED_EDGE ( 'NONE', *, *, #43555, .F. ) ;
#50511=FACE_OUTER_BOUND ( 'NONE', #49182, .T. ) ;
#50517=CARTESIAN_POINT ( 'NONE',  ( 0.5522155295079038684, -22.42457893558620796, -34.84133294386909796 ) ) ;
#50538=DIRECTION ( 'NONE',  ( 0.000000000000000000, 1.000000000000000000, 0.000000000000000000 ) ) ;
#50540=ORIENTED_EDGE ( 'NONE', *, *, #30360, .T. ) ;
#50541=DIRECTION ( 'NONE',  ( 0.000000000000000000, 0.000000000000000000, -1.000000000000000000 ) ) ;
#50563=VECTOR ( 'NONE', #16632, 1000.000000000000000 ) ;
#50564=CARTESIAN_POINT ( 'NONE',  ( -18.25696898823050063, 2.971788218260359660, -50.64156704142759935 ) ) ;
#50566=CARTESIAN_POINT ( 'NONE',  ( 47.11822937922350718, -38.11590075025419111, -54.71074210669950588 ) ) ;
#50570=VERTEX_POINT ( 'NONE', #29691 ) ;
#50595=CARTESIAN_POINT ( 'NONE',  ( 0.3209249304026170480, -15.61618894467929941, -35.14999999999999858 ) ) ;
#50600=CARTESIAN_POINT ( 'NONE',  ( 0.2609591194317593676, -8.253214024663448001, -34.64999999999999858 ) ) ;
#50604=CARTESIAN_POINT ( 'NONE',  ( 44.11147024075970080, 1.884029797248020000, -54.64999999999999858 ) ) ;
#50610=CARTESIAN_POINT ( 'NONE',  ( 44.71029624102973798, -38.00771234126634113, -66.76814554949260128 ) ) ;
#50624=EDGE_CURVE ( 'NONE', #16095, #4073, #40987, .T. ) ;
#50627=CARTESIAN_POINT ( 'NONE',  ( 41.15616284062399188, -39.66885904924578909, -80.40208926020751790 ) ) ;
#50652=EDGE_CURVE ( 'NONE', #45496, #14025, #22995, .T. ) ;
#50655=VERTEX_POINT ( 'NONE', #37838 ) ;
#50666=CARTESIAN_POINT ( 'NONE',  ( 16.13393739769599833, 14.38381105532070059, -35.14999999999999858 ) ) ;
#50667=CARTESIAN_POINT ( 'NONE',  ( 43.88591490443007359, 6.670162465103853577, -70.89007156030166357 ) ) ;
#50677=VECTOR ( 'NONE', #41138, 1000.000000000000000 ) ;
#50690=CARTESIAN_POINT ( 'NONE',  ( 14.15073023633500071, 1.361188710403610003, -35.02127583263639821 ) ) ;
#50691=DIRECTION ( 'NONE',  ( 0.000000000000000000, 0.000000000000000000, 1.000000000000000000 ) ) ;
#50698=AXIS2_PLACEMENT_3D ( 'NONE', #36174, #43545, #7895 ) ;
#50699=DIRECTION ( 'NONE',  ( 0.000000000000000000, 0.000000000000000000, 1.000000000000000000 ) ) ;
#50706=ORIENTED_EDGE ( 'NONE', *, *, #38110, .T. ) ;
#50708=CYLINDRICAL_SURFACE ( 'NONE', #44341, 2.999999999999999112 ) ;
#50710=CARTESIAN_POINT ( 'NONE',  ( 45.32643724771776306, 8.820270950418585443, -60.22851707904983698 ) ) ;
#50717=EDGE_CURVE ( 'NONE', #49113, #22505, #3342, .T. ) ;
#50721=DIRECTION ( 'NONE',  ( 0.9244418645452657790, 4.067568864690730049E-12, 0.3813230114693739181 ) ) ;
#50722=CARTESIAN_POINT ( 'NONE',  ( -15.32468133715470238, -15.61618894467930296, -81.65000000000000568 ) ) ;
#50723=VERTEX_POINT ( 'NONE', #9802 ) ;
#50744=AXIS2_PLACEMENT_3D ( 'NONE', #7782, #7525, #35556 ) ;
#50747=EDGE_CURVE ( 'NONE', #50419, #45223, #9226, .T. ) ;
#50750=B_SPLINE_CURVE_WITH_KNOTS ( 'NONE', 3,
 ( #34237, #50774, #14864, #30828 ),
 .UNSPECIFIED., .F., .F.,
 ( 4, 4 ),
 ( 0.000000000000000000, 19.53260001885960051 ),
 .UNSPECIFIED. ) ;
#50751=CARTESIAN_POINT ( 'NONE',  ( 45.73065097657321587, -40.07790899994112976, -58.26712722073379069 ) ) ;
#50752=EDGE_CURVE ( 'NONE', #29814, #11667, #13587, .T. ) ;
#50765=ORIENTED_EDGE ( 'NONE', *, *, #44590, .F. ) ;
#50768=AXIS2_PLACEMENT_3D ( 'NONE', #26305, #26563, #47038 ) ;
#50774=CARTESIAN_POINT ( 'NONE',  ( 8.900684698865370947, 16.90943255658890010, -48.24693240561549601 ) ) ;
#50778=CYLINDRICAL_SURFACE ( 'NONE', #2210, 0.4999999999999967248 ) ;
#50789=LINE ( 'NONE', #22723, #39340 ) ;
#50792=CARTESIAN_POINT ( 'NONE',  ( 16.13393739769599833, 14.38381105532070059, -62.64999999999999858 ) ) ;
#50797=DIRECTION ( 'NONE',  ( 1.000000000000000000, 0.000000000000000000, 0.000000000000000000 ) ) ;
#50816=DIRECTION ( 'NONE',  ( -1.000000000000000000, 0.000000000000000000, 0.000000000000000000 ) ) ;
#50820=ADVANCED_FACE ( 'NONE', ( #35892 ), #30984, .T. ) ;
#50822=CARTESIAN_POINT ( 'NONE',  ( -18.35260750266889929, 3.120353346132920258, -50.84549189752459597 ) ) ;
#50829=ORIENTED_EDGE ( 'NONE', *, *, #30464, .T. ) ;
#50830=CARTESIAN_POINT ( 'NONE',  ( 41.02599897614819469, 8.452786747797132350, -80.89672324886578281 ) ) ;
#50837=CARTESIAN_POINT ( 'NONE',  ( 44.13393739769620083, 1.883811055320659955, -54.27132075603810080 ) ) ;
#50863=CIRCLE ( 'NONE', #16503, 34.47562460986249278 ) ;
#50864=CARTESIAN_POINT ( 'NONE',  ( 17.94297559678595988, -32.43785826095941616, -34.75586992539664521 ) ) ;
#50872=ORIENTED_EDGE ( 'NONE', *, *, #21261, .T. ) ;
#50877=CARTESIAN_POINT ( 'NONE',  ( 0.1416488651360941764, 14.72332773530568772, -34.68322412398370602 ) ) ;
#50890=CARTESIAN_POINT ( 'NONE',  ( 28.13393739769619728, -22.54439217495490055, -35.14999999999999858 ) ) ;
#50910=DIRECTION ( 'NONE',  ( 1.000000000000000000, 0.000000000000000000, 0.000000000000000000 ) ) ;
#50911=ORIENTED_EDGE ( 'NONE', *, *, #7026, .F. ) ;
#50912=EDGE_LOOP ( 'NONE', ( #13224, #33285, #49888, #48764, #51712 ) ) ;
#50915=ORIENTED_EDGE ( 'NONE', *, *, #16903, .F. ) ;
#50918=CARTESIAN_POINT ( 'NONE',  ( 46.25525774125583922, -33.99486860111965569, -35.14999999999999858 ) ) ;
#50921=ORIENTED_EDGE ( 'NONE', *, *, #41521, .T. ) ;
#50923=CARTESIAN_POINT ( 'NONE',  ( 43.05104827289743952, 6.553104225060173427, -75.06444201244694625 ) ) ;
#50927=ADVANCED_FACE ( 'NONE', ( #16487 ), #1284, .T. ) ;
#50938=LINE ( 'NONE', #3510, #37365 ) ;
#50941=EDGE_LOOP ( 'NONE', ( #35708, #36002, #21615, #9516 ) ) ;
#50953=CARTESIAN_POINT ( 'NONE',  ( 0.3209249304026170480, -23.01378514180129997, -34.64999999999999858 ) ) ;
#50971=EDGE_LOOP ( 'NONE', ( #28147, #27116, #10113, #10384 ) ) ;
#50974=VERTEX_POINT ( 'NONE', #16168 ) ;
#50977=CARTESIAN_POINT ( 'NONE',  ( 16.13393739769620083, -15.61618894467929941, -34.64999999999999858 ) ) ;
#50978=CARTESIAN_POINT ( 'NONE',  ( -22.10349206065158612, -23.47247094433527792, -54.22342502566657174 ) ) ;
#50979=ORIENTED_EDGE ( 'NONE', *, *, #30074, .F. ) ;
#50984=CARTESIAN_POINT ( 'NONE',  ( 45.30908585303109959, -33.79766069374939974, -34.65739582053399204 ) ) ;
#50986=CARTESIAN_POINT ( 'NONE',  ( 44.79905630159557717, 1.958006841695987266, -42.17908975497248036 ) ) ;
#50988=CIRCLE ( 'NONE', #35069, 22.00000000000000000 ) ;
#50990=CARTESIAN_POINT ( 'NONE',  ( 19.61497263573680172, -40.47764751925419802, -35.14999999999999858 ) ) ;
#50994=EDGE_CURVE ( 'NONE', #23485, #6332, #1225, .T. ) ;
#50996=CIRCLE ( 'NONE', #33397, 2.999999999999999112 ) ;
#51002=ADVANCED_FACE ( 'NONE', ( #28208 ), #17214, .T. ) ;
#51010=CARTESIAN_POINT ( 'NONE',  ( 46.05101011062605920, -40.09655301607604372, -56.71146331062539758 ) ) ;
#51016=DIRECTION ( 'NONE',  ( -0.5897727341282608116, 0.3900873262218075288, 0.7071067811865454633 ) ) ;
#51018=ORIENTED_EDGE ( 'NONE', *, *, #3179, .F. ) ;
#51029=CARTESIAN_POINT ( 'NONE',  ( 0.1339373976962109913, -15.61618894467929941, -34.64999999999999858 ) ) ;
#51034=CARTESIAN_POINT ( 'NONE',  ( 0.3209249304026170480, -26.47788675693900018, -34.64999999999999858 ) ) ;
#51043=ORIENTED_EDGE ( 'NONE', *, *, #49422, .F. ) ;
#51046=CARTESIAN_POINT ( 'NONE',  ( 0.4047412638266219553, -8.844334399411719616, -35.14999999999999858 ) ) ;
#51047=EDGE_CURVE ( 'NONE', #24198, #14157, #44469, .T. ) ;
#51060=DIRECTION ( 'NONE',  ( 0.000000000000000000, -1.000000000000000000, 0.000000000000000000 ) ) ;
#51070=EDGE_CURVE ( 'NONE', #42105, #51177, #30961, .T. ) ;
#51080=CARTESIAN_POINT ( 'NONE',  ( 47.13346488154629554, -38.11675101726400072, -54.63444359475949597 ) ) ;
#51086=CARTESIAN_POINT ( 'NONE',  ( 47.12390138149789465, 6.751667908743102409, -54.63444595951939675 ) ) ;
#51093=DIRECTION ( 'NONE',  ( 1.000000000000000000, 0.000000000000000000, 0.000000000000000000 ) ) ;
#51103=DIRECTION ( 'NONE',  ( -1.000000000000000000, 0.000000000000000000, 0.000000000000000000 ) ) ;
#51114=EDGE_CURVE ( 'NONE', #46452, #29692, #50216, .T. ) ;
#51121=AXIS2_PLACEMENT_3D ( 'NONE', #5925, #13027, #37372 ) ;
#51123=LINE ( 'NONE', #38295, #11099 ) ;
#51125=EDGE_CURVE ( 'NONE', #51719, #4886, #45559, .T. ) ;
#51128=FACE_OUTER_BOUND ( 'NONE', #13755, .T. ) ;
#51133=CARTESIAN_POINT ( 'NONE',  ( 14.63393739769630031, 0.9255523191757060175, -34.64999999999999858 ) ) ;
#51151=VERTEX_POINT ( 'NONE', #1484 ) ;
#51152=CIRCLE ( 'NONE', #125, 134.7319120578750073 ) ;
#51156=EDGE_CURVE ( 'NONE', #43432, #42739, #17469, .T. ) ;
#51167=CARTESIAN_POINT ( 'NONE',  ( 13.05521822061487214, -49.46974233527257780, -34.79644660940672907 ) ) ;
#51170=DIRECTION ( 'NONE',  ( -0.3535533905932738974, 0.6123724356957941373, 0.7071067811865477948 ) ) ;
#51177=VERTEX_POINT ( 'NONE', #22149 ) ;
#51180=CARTESIAN_POINT ( 'NONE',  ( 55.13393739769630031, -15.61618894467929941, -34.64999999999999858 ) ) ;
#51181=ORIENTED_EDGE ( 'NONE', *, *, #19205, .F. ) ;
#51188=CARTESIAN_POINT ( 'NONE',  ( 43.11472998706207704, 6.562511154101421162, -74.74601975373923324 ) ) ;
#51201=DIRECTION ( 'NONE',  ( 0.7071067811865475727, 0.000000000000000000, 0.7071067811865475727 ) ) ;
#51208=ORIENTED_EDGE ( 'NONE', *, *, #6288, .F. ) ;
#51215=CARTESIAN_POINT ( 'NONE',  ( -0.1295185695942999982, 0.6472670226113349523, 4.943674098299870145 ) ) ;
#51225=ADVANCED_FACE ( 'NONE', ( #49453 ), #822, .T. ) ;
#51235=CARTESIAN_POINT ( 'NONE',  ( 22.20417850065088672, -53.99262654159362285, -34.79644414665607144 ) ) ;
#51239=CARTESIAN_POINT ( 'NONE',  ( 45.27709827453856661, 8.817119440491692828, -60.46762888545257653 ) ) ;
#51246=DIRECTION ( 'NONE',  ( 0.6975711590030510001, 0.7165155114351260401, 0.000000000000000000 ) ) ;
#51249=ORIENTED_EDGE ( 'NONE', *, *, #42050, .F. ) ;
#51250=EDGE_CURVE ( 'NONE', #31048, #37975, #10458, .T. ) ;
#51266=EDGE_LOOP ( 'NONE', ( #35028, #23179, #19197, #38678, #2918, #29168, #24722 ) ) ;
#51270=CARTESIAN_POINT ( 'NONE',  ( 45.89732069378420931, -40.08804502263331671, -57.45677221337471252 ) ) ;
#51283=ORIENTED_EDGE ( 'NONE', *, *, #30360, .F. ) ;
#51289=CARTESIAN_POINT ( 'NONE',  ( 46.25525774125583922, 2.762490711761015572, -44.64999999999999858 ) ) ;
#51290=CARTESIAN_POINT ( 'NONE',  ( 47.13393739769619373, -39.28050807707779768, -53.76790129988369671 ) ) ;
#51291=DIRECTION ( 'NONE',  ( 0.000000000000000000, 0.000000000000000000, 1.000000000000000000 ) ) ;
#51292=LINE ( 'NONE', #43684, #26934 ) ;
#51298=CARTESIAN_POINT ( 'NONE',  ( 37.88393739769619373, -41.76263555408612405, -34.79644660940672907 ) ) ;
#51299=VECTOR ( 'NONE', #36204, 1000.000000000000000 ) ;
#51307=CARTESIAN_POINT ( 'NONE',  ( 23.13393739769620083, -2.337132753317950229, -84.65000000000000568 ) ) ;
#51318=FACE_OUTER_BOUND ( 'NONE', #4552, .T. ) ;
#51325=CARTESIAN_POINT ( 'NONE',  ( 22.37318698975099807, -53.60726374558549878, -34.64999999999999858 ) ) ;
#51348=CARTESIAN_POINT ( 'NONE',  ( 42.31734421635291454, 6.282516177144741754, -78.71114254000248422 ) ) ;
#51355=LINE ( 'NONE', #47434, #47416 ) ;
#51370=ORIENTED_EDGE ( 'NONE', *, *, #35822, .T. ) ;
#51371=EDGE_CURVE ( 'NONE', #7528, #48439, #3290, .T. ) ;
#51375=AXIS2_PLACEMENT_3D ( 'NONE', #2496, #46013, #38139 ) ;
#51376=ORIENTED_EDGE ( 'NONE', *, *, #33157, .T. ) ;
#51381=DIRECTION ( 'NONE',  ( 1.000000000000000000, 0.000000000000000000, 0.000000000000000000 ) ) ;
#51388=CARTESIAN_POINT ( 'NONE',  ( 3.987490788289478783, -8.603434725040944642, -34.79644660940672907 ) ) ;
#51391=DIRECTION ( 'NONE',  ( 0.000000000000000000, 0.000000000000000000, -1.000000000000000000 ) ) ;
#51403=AXIS2_PLACEMENT_3D ( 'NONE', #37300, #13722, #50132 ) ;
#51408=ADVANCED_FACE ( 'NONE', ( #19266 ), #7228, .T. ) ;
#51411=EDGE_CURVE ( 'NONE', #45283, #35235, #43134, .T. ) ;
#51421=CARTESIAN_POINT ( 'NONE',  ( -0.3118748401327328668, -45.36041153914962365, -35.03826966092410089 ) ) ;
#51430=CARTESIAN_POINT ( 'NONE',  ( 41.61626771661330082, -36.11618894467930119, -82.23834840541459812 ) ) ;
#51433=VERTEX_POINT ( 'NONE', #15347 ) ;
#51440=CARTESIAN_POINT ( 'NONE',  ( 1.058369240368480124, -8.644356418428410294, -34.64999999999999858 ) ) ;
#51443=CARTESIAN_POINT ( 'NONE',  ( 42.66038805835393788, 6.494748731714828693, -77.01767951336998408 ) ) ;
#51449=VECTOR ( 'NONE', #2465, 1000.000000000000000 ) ;
#51460=DIRECTION ( 'NONE',  ( 0.000000000000000000, 1.000000000000000000, 0.000000000000000000 ) ) ;
#51469=CARTESIAN_POINT ( 'NONE',  ( 14.15276264669889983, 1.359379830875179884, -35.01387690002259490 ) ) ;
#51477=DIRECTION ( 'NONE',  ( 0.000000000000000000, 0.000000000000000000, -1.000000000000000000 ) ) ;
#51495=VERTEX_POINT ( 'NONE', #32576 ) ;
#51499=CARTESIAN_POINT ( 'NONE',  ( 16.13393739769620083, -15.61618894467929941, -34.64999999999999858 ) ) ;
#51501=ORIENTED_EDGE ( 'NONE', *, *, #34935, .F. ) ;
#51503=VERTEX_POINT ( 'NONE', #32322 ) ;
#51508=LINE ( 'NONE', #19010, #41762 ) ;
#51511=EDGE_CURVE ( 'NONE', #34773, #16490, #381, .T. ) ;
#51513=CARTESIAN_POINT ( 'NONE',  ( 0.3209249304026170480, -4.754491132419490285, -34.64999999999999858 ) ) ;
#51515=EDGE_CURVE ( 'NONE', #14662, #8293, #12049, .T. ) ;
#51517=FACE_OUTER_BOUND ( 'NONE', #29633, .T. ) ;
#51518=CARTESIAN_POINT ( 'NONE',  ( 11.63393739769600010, 10.38381105532060111, -35.14999999999999858 ) ) ;
#51524=CARTESIAN_POINT ( 'NONE',  ( 43.92098005941133465, -39.94817122821439881, -67.04241095931078576 ) ) ;
#51525=DIRECTION ( 'NONE',  ( 0.000000000000000000, 0.000000000000000000, 1.000000000000000000 ) ) ;
#51527=( BOUNDED_CURVE ( )  B_SPLINE_CURVE ( 3, ( #11822, #24341, #7629, #23573 ),
 .UNSPECIFIED., .F., .T. ) 
 B_SPLINE_CURVE_WITH_KNOTS ( ( 4, 4 ),
 ( 1.570796326794885678, 2.356194490192327962 ),
 .UNSPECIFIED. ) 
 CURVE ( )  GEOMETRIC_REPRESENTATION_ITEM ( )  RATIONAL_B_SPLINE_CURVE ( ( 1.000000000000000000, 0.9492530216741918991, 0.9492530216741918991, 1.000000000000000000 ) ) 
 REPRESENTATION_ITEM ( '' )  );
#51530=EDGE_CURVE ( 'NONE', #5719, #39196, #11744, .T. ) ;
#51537=ORIENTED_EDGE ( 'NONE', *, *, #32218, .T. ) ;
#51547=DIRECTION ( 'NONE',  ( 0.000000000000000000, 1.000000000000000000, 0.000000000000000000 ) ) ;
#51549=CARTESIAN_POINT ( 'NONE',  ( 23.13393739769620083, -28.89524513604070322, -84.65000000000000568 ) ) ;
#51550=VERTEX_POINT ( 'NONE', #27891 ) ;
#51555=EDGE_LOOP ( 'NONE', ( #50018, #17568, #10826, #18689, #22562, #8442, #19956 ) ) ;
#51556=DIRECTION ( 'NONE',  ( 0.000000000000000000, 0.000000000000000000, -1.000000000000000000 ) ) ;
#51563=LINE ( 'NONE', #40734, #39681 ) ;
#51564=ORIENTED_EDGE ( 'NONE', *, *, #29438, .F. ) ;
#51568=DIRECTION ( 'NONE',  ( 0.000000000000000000, 0.000000000000000000, 1.000000000000000000 ) ) ;
#51569=CIRCLE ( 'NONE', #5525, 2.500000000000000444 ) ;
#51571=VECTOR ( 'NONE', #44382, 1000.000000000000000 ) ;
#51572=EDGE_CURVE ( 'NONE', #1811, #24006, #44665, .T. ) ;
#51581=CARTESIAN_POINT ( 'NONE',  ( -13.39236625349559873, -30.35380722911099838, -54.64999999999999858 ) ) ;
#51582=VERTEX_POINT ( 'NONE', #8245 ) ;
#51588=VECTOR ( 'NONE', #25197, 1000.000000000000000 ) ;
#51589=LINE ( 'NONE', #47662, #20536 ) ;
#51591=CIRCLE ( 'NONE', #32293, 2.999999999999994227 ) ;
#51597=DIRECTION ( 'NONE',  ( 0.000000000000000000, -0.7071067811865466846, -0.7071067811865483499 ) ) ;
#51599=VERTEX_POINT ( 'NONE', #48605 ) ;
#51601=EDGE_LOOP ( 'NONE', ( #23998, #21186, #22977, #20973, #43231, #24906, #8814, #11010, #20226, #46666 ) ) ;
#51602=CARTESIAN_POINT ( 'NONE',  ( 46.88244175870809727, 6.730884966597995955, -55.84197583295708256 ) ) ;
#51611=VECTOR ( 'NONE', #43783, 1000.000000000000000 ) ;
#51620=CARTESIAN_POINT ( 'NONE',  ( -13.73674066540309902, -30.55263188852779876, -46.71145918530379504 ) ) ;
#51621=VERTEX_POINT ( 'NONE', #16623 ) ;
#51638=DIRECTION ( 'NONE',  ( 0.000000000000000000, 0.000000000000000000, 1.000000000000000000 ) ) ;
#51639=CARTESIAN_POINT ( 'NONE',  ( -0.3016046179078940015, -10.91500322974829906, -35.02873218748179340 ) ) ;
#51641=VERTEX_POINT ( 'NONE', #12710 ) ;
#51645=CIRCLE ( 'NONE', #34872, 6.999999999999999112 ) ;
#51646=CARTESIAN_POINT ( 'NONE',  ( -0.007164427059776000244, -8.408015226406421405, -34.77269723891829756 ) ) ;
#51650=CARTESIAN_POINT ( 'NONE',  ( 9.895190454275772041, 22.37603658786960281, -34.64999999999999858 ) ) ;
#51657=DIRECTION ( 'NONE',  ( 0.000000000000000000, 0.000000000000000000, -1.000000000000000000 ) ) ;
#51662=FACE_OUTER_BOUND ( 'NONE', #38868, .T. ) ;
#51671=CARTESIAN_POINT ( 'NONE',  ( 38.67452568954060155, -36.11618894467930119, -81.65000000000000568 ) ) ;
#51676=DIRECTION ( 'NONE',  ( 0.000000000000000000, -1.000000000000000000, 0.000000000000000000 ) ) ;
#51680=CARTESIAN_POINT ( 'NONE',  ( -10.98165337464593350, -35.31681881277557977, -44.31573110638452562 ) ) ;
#51683=DIRECTION ( 'NONE',  ( 0.5813178231270340612, 0.8136765871738268485, 0.000000000000000000 ) ) ;
#51689=EDGE_LOOP ( 'NONE', ( #38989, #11874, #10485, #19623, #42410, #72, #44646 ) ) ;
#51694=CARTESIAN_POINT ( 'NONE',  ( 44.48818529294619850, 6.748246523411627784, -67.87874373785433590 ) ) ;
#51700=EDGE_CURVE ( 'NONE', #885, #6210, #44410, .T. ) ;
#51712=ORIENTED_EDGE ( 'NONE', *, *, #26644, .T. ) ;
#51718=CARTESIAN_POINT ( 'NONE',  ( 2.422196078461530178, -5.407548561780520124, -35.02873218748179340 ) ) ;
#51719=VERTEX_POINT ( 'NONE', #30222 ) ;
#51736=CARTESIAN_POINT ( 'NONE',  ( 22.19769533645168025, -54.00735027852237380, -34.80997524099233686 ) ) ;
#51744=ORIENTED_EDGE ( 'NONE', *, *, #11470, .T. ) ;
#51753=CARTESIAN_POINT ( 'NONE',  ( -11.36606260230380094, -15.61618894467929941, -54.64999999999999858 ) ) ;
#51755=CARTESIAN_POINT ( 'NONE',  ( 18.13393739769639978, 6.292713355527299157, -54.64999999999999858 ) ) ;
#51759=DIRECTION ( 'NONE',  ( 0.000000000000000000, -1.000000000000000000, 0.000000000000000000 ) ) ;
#51763=B_SPLINE_CURVE_WITH_KNOTS ( 'NONE', 3,
 ( #44330, #27566, #44078, #32249, #4243, #7673 ),
 .UNSPECIFIED., .F., .F.,
 ( 4, 2, 4 ),
 ( -0.2608998691367954148, -0.2578313219245090271, -0.2220763490922390004 ),
 .UNSPECIFIED. ) ;
#51764=CYLINDRICAL_SURFACE ( 'NONE', #5494, 0.4999999999999985012 ) ;
#51767=CYLINDRICAL_SURFACE ( 'NONE', #35488, 2.999999999999994227 ) ;
#51770=ORIENTED_EDGE ( 'NONE', *, *, #34876, .F. ) ;
#51775=ADVANCED_FACE ( 'NONE', ( #26026 ), #47747, .T. ) ;
#51776=CARTESIAN_POINT ( 'NONE',  ( 43.30576519922845335, -39.89449908986776450, -70.02050220811160841 ) ) ;
#51786=VERTEX_POINT ( 'NONE', #9300 ) ;
#51794=CARTESIAN_POINT ( 'NONE',  ( 41.50605423569203367, 8.477321776405595699, -78.71501693997980453 ) ) ;
#51795=CARTESIAN_POINT ( 'NONE',  ( 44.81444952522934955, -33.19054756649958904, -41.91622283249964909 ) ) ;
#51797=DIRECTION ( 'NONE',  ( 1.000000000000000000, 0.000000000000000000, 0.000000000000000000 ) ) ;
#51802=ORIENTED_EDGE ( 'NONE', *, *, #46237, .T. ) ;
#51807=ORIENTED_EDGE ( 'NONE', *, *, #47182, .F. ) ;
#51808=VERTEX_POINT ( 'NONE', #25250 ) ;
#51817=ORIENTED_EDGE ( 'NONE', *, *, #24921, .T. ) ;
#51824=VECTOR ( 'NONE', #30659, 1000.000000000000114 ) ;
#51827=DIRECTION ( 'NONE',  ( 0.000000000000000000, 0.000000000000000000, 1.000000000000000000 ) ) ;
#51828=CARTESIAN_POINT ( 'NONE',  ( 29.13393739769619728, -33.11618894467940066, -81.65000000000000568 ) ) ;
#51829=AXIS2_PLACEMENT_3D ( 'NONE', #7657, #11330, #39618 ) ;
#51832=CARTESIAN_POINT ( 'NONE',  ( 8.731180243531472485, 17.69319178430564321, -34.79644561402098191 ) ) ;
#51833=( BOUNDED_SURFACE ( )  B_SPLINE_SURFACE ( 2, 3, ( 
 ( #21734, #6545, #18846, #42458, #34306, #38521, #30886, #6033, #30632, #41933, #21991, #50319, #2620, #18592, #10486, #34568, #46914, #34828, #49800, #25919, #14405, #18074, #9956, #26441, #46135, #14663, #46657, #37741, #50053, #17817, #1839, #33791, #50830, #10740, #26696, #11000, #30116 ),
 ( #42718, #42977, #38001, #22767, #38786, #13891, #29850, #10226, #26184, #42195, #3138, #31145, #11519, #27220, #3653, #39803, #48180, #23022, #43232, #15959, #40060, #36120, #19624, #51857, #27480, #3910, #43738, #15184, #35348, #7839, #15446, #4153, #19874, #31399, #11780, #39550, #32164 ),
 ( #23272, #35615, #31911, #39043, #51086, #43482, #47426, #7586, #23532, #7325, #51602, #23788, #35865, #47677, #47933, #223, #20127, #35083, #11258, #15697, #39293, #47170, #27739, #31652, #12034, #27987, #7072, #3399, #19106, #19366, #51348, #16206, #43990, #8095, #12282, #24039, #28244 ) ),
 .UNSPECIFIED., .F., .F., .T. ) 
 B_SPLINE_SURFACE_WITH_KNOTS ( ( 3, 3 ),
 ( 4, 3, 3, 3, 3, 3, 3, 3, 3, 3, 3, 3, 4 ),
 ( -0.3886185405137270177, 0.4281390595564339985 ),
 ( -1.401241294368219981, -1.393251294075019908, -1.393221429621980034, -1.392992571260399881, -1.384912848423149878, -1.376592006214460095, -1.368290935607660019, -1.360011799518540121, -1.351756755142390132, -1.343527953381050022, -1.335327538272319980, -1.327157646422050030, -1.318834645256290017 ),
 .UNSPECIFIED. ) 
 GEOMETRIC_REPRESENTATION_ITEM ( )  RATIONAL_B_SPLINE_SURFACE ( (
 ( 1.001164415209670144, 1.001164415209680136, 1.001164415209680136, 1.001164415209680136, 1.001164415209680136, 1.001164415209680136, 1.001164415209680136, 1.001164415209680136, 1.001164415209680136, 1.001164415209680136, 1.001164415209680136, 1.001164415209680136, 1.001164415209680136, 1.001164415209680136, 1.001164415209680136, 1.001164415209680136, 1.001164415209680136, 1.001164415209680136, 1.001164415209680136, 1.001164415209680136, 1.001164415209680136, 1.001164415209680136, 1.001164415209680136, 1.001164415209680136, 1.001164415209680136, 1.001164415209680136, 1.001164415209680136, 1.001164415209680136, 1.001164415209680136, 1.001164415209680136, 1.001164415209680136, 1.001164415209680136, 1.001164415209680136, 1.001164415209680136, 1.001164415209680136, 1.001164415209680136, 1.001164415209680136),
 ( 0.9227754158175089927, 0.9227754158167740250, 0.9227754158169680920, 0.9227754158169680920, 0.9227754158169680920, 0.9227754158169539922, 0.9227754158169539922, 0.9227754158169539922, 0.9227754158169710896, 0.9227754158169710896, 0.9227754158169710896, 0.9227754158169660936, 0.9227754158169660936, 0.9227754158169660936, 0.9227754158169569898, 0.9227754158169569898, 0.9227754158169569898, 0.9227754158169509946, 0.9227754158169509946, 0.9227754158169509946, 0.9227754158169620968, 0.9227754158169620968, 0.9227754158169620968, 0.9227754158169710896, 0.9227754158169710896, 0.9227754158169710896, 0.9227754158169569898, 0.9227754158169569898, 0.9227754158169569898, 0.9227754158169600984, 0.9227754158169600984, 0.9227754158169600984, 0.9227754158169760856, 0.9227754158169760856, 0.9227754158169750864, 0.9227754158143870455, 0.9227754159543060108),
 ( 1.009136175741510044, 1.009136175741579988, 1.009136175741560004, 1.009136175741560004, 1.009136175741560004, 1.009136175741560004, 1.009136175741560004, 1.009136175741560004, 1.009136175741560004, 1.009136175741560004, 1.009136175741560004, 1.009136175741560004, 1.009136175741560004, 1.009136175741560004, 1.009136175741560004, 1.009136175741560004, 1.009136175741560004, 1.009136175741560004, 1.009136175741560004, 1.009136175741560004, 1.009136175741560004, 1.009136175741560004, 1.009136175741560004, 1.009136175741560004, 1.009136175741560004, 1.009136175741560004, 1.009136175741560004, 1.009136175741560004, 1.009136175741560004, 1.009136175741560004, 1.009136175741560004, 1.009136175741560004, 1.009136175741560004, 1.009136175741560004, 1.009136175741560004, 1.009136175741900177, 1.009136175723519990) ) ) 
 REPRESENTATION_ITEM ( '' )  SURFACE ( )  );
#51836=CARTESIAN_POINT ( 'NONE',  ( 46.75606609761160115, -39.76767805705360104, -54.48523547516549570 ) ) ;
#51843=CARTESIAN_POINT ( 'NONE',  ( 8.919738259460670449, -49.28809633162239834, -34.65024031912469837 ) ) ;
#51844=CARTESIAN_POINT ( 'NONE',  ( 0.05120484486776299277, 19.58911166448121932, -34.72736369164719861 ) ) ;
#51857=CARTESIAN_POINT ( 'NONE',  ( 43.98278727443419456, 7.770898977125641593, -70.80343447450441374 ) ) ;
#51868=ORIENTED_EDGE ( 'NONE', *, *, #51411, .T. ) ;
#51871=EDGE_CURVE ( 'NONE', #425, #19145, #43585, .T. ) ;
ENDSEC;
END-ISO-10303-21;
